ISO-10303-21;
HEADER;
FILE_DESCRIPTION (('STEP AP214'),
    '1' );
FILE_NAME ('Lower Pivot Bracket.step',
    '2026-10-12T23:53:07',
    ( '' ),
    ( '' ),
    'SwSTEP 2.0',
    'SolidWorks 2024',
    '' );
FILE_SCHEMA (( 'AUTOMOTIVE_DESIGN' ));
ENDSEC;

DATA;
#9=ORIENTED_EDGE ( 'NONE', *, *, #10978, .F. ) ;
#19=CARTESIAN_POINT ( 'NONE',  ( 0.2420619479266831187, -1.321943518198432033, -0.3144976166544464768 ) ) ;
#20=CARTESIAN_POINT ( 'NONE',  ( 0.6117213743483401744, -1.432107776390856513, -0.6250000000000000000 ) ) ;
#23=CARTESIAN_POINT ( 'NONE',  ( 0.5982604594170003454, -1.483634568127149889, -0.3944719512476840273 ) ) ;
#28=CARTESIAN_POINT ( 'NONE',  ( 0.2462190030042624156, -1.768833963249898611, -0.6590625227467041825 ) ) ;
#39=EDGE_CURVE ( 'NONE', #17084, #9403, #40506, .T. ) ;
#48=ORIENTED_EDGE ( 'NONE', *, *, #29288, .T. ) ;
#53=CARTESIAN_POINT ( 'NONE',  ( 0.5200734380266420764, -1.679028703643771436, -0.4374651140121203485 ) ) ;
#60=DIRECTION ( 'NONE',  ( 0.8660512985181130219, 0.4999551463232377868, 0.000000000000000000 ) ) ;
#70=CARTESIAN_POINT ( 'NONE',  ( 0.4763501221259694440, -1.554011115824661893, -0.5166151207188711680 ) ) ;
#82=CARTESIAN_POINT ( 'NONE',  ( 0.4855256156385516775, -1.649569844525025530, -0.6308821889615696676 ) ) ;
#89=ORIENTED_EDGE ( 'NONE', *, *, #20270, .F. ) ;
#92=ORIENTED_EDGE ( 'NONE', *, *, #28854, .F. ) ;
#94=CARTESIAN_POINT ( 'NONE',  ( 0.3337487181682026183, -1.684227851221292038, -0.6212492361075898639 ) ) ;
#98=ORIENTED_EDGE ( 'NONE', *, *, #22101, .F. ) ;
#112=CARTESIAN_POINT ( 'NONE',  ( 0.4203826191881492313, -1.700944664958275343, -0.4172566670736511107 ) ) ;
#116=CARTESIAN_POINT ( 'NONE',  ( 0.3610818047233222972, -1.951413994126270257, -0.4993772958782550786 ) ) ;
#123=CIRCLE ( 'NONE', #23102, 0.02999999999999997113 ) ;
#137=CARTESIAN_POINT ( 'NONE',  ( 0.3648774902654713936, -1.763897834913869644, -0.5277763367469582301 ) ) ;
#140=DIRECTION ( 'NONE',  ( -0.9823715787225880680, 0.000000000000000000, -0.1869387100578417116 ) ) ;
#148=CARTESIAN_POINT ( 'NONE',  ( 0.5164807395112145372, -1.614047142484251740, -0.4728386827019681049 ) ) ;
#154=CARTESIAN_POINT ( 'NONE',  ( 0.2153966442130109959, -1.622051466259873287, -0.3272083645034317145 ) ) ;
#159=AXIS2_PLACEMENT_3D ( 'NONE', #8390, #5286, #20960 ) ;
#160=EDGE_CURVE ( 'NONE', #40387, #17181, #6292, .T. ) ;
#171=B_SPLINE_CURVE_WITH_KNOTS ( 'NONE', 3,
 ( #36912, #8724, #30944, #15317 ),
 .UNSPECIFIED., .F., .F.,
 ( 4, 4 ),
 ( 4.416736787580399614E-17, 0.0002767382645091641977 ),
 .UNSPECIFIED. ) ;
#172=CARTESIAN_POINT ( 'NONE',  ( 0.5874764043858021756, -1.597120814744488193, -0.4448059412197695184 ) ) ;
#178=CARTESIAN_POINT ( 'NONE',  ( 0.1779133654309061896, -1.234518891347017533, -0.6184399470714002645 ) ) ;
#181=CARTESIAN_POINT ( 'NONE',  ( 0.4006050890619684002, -1.646293961035435460, -0.3940011403029922699 ) ) ;
#184=CARTESIAN_POINT ( 'NONE',  ( 0.5203474827567471372, -1.645139592123281203, -0.4526729257047640287 ) ) ;
#214=CARTESIAN_POINT ( 'NONE',  ( 0.4697623592636160361, -1.061459377010899541, -0.6056023639864149821 ) ) ;
#217=CARTESIAN_POINT ( 'NONE',  ( 0.6518945859131652920, -1.452672594389344596, -0.6204649030305892099 ) ) ;
#219=CIRCLE ( 'NONE', #2141, 0.04330708661417340122 ) ;
#224=DIRECTION ( 'NONE',  ( 0.4999551463232372317, -0.8660512985181135770, 0.000000000000000000 ) ) ;
#227=CARTESIAN_POINT ( 'NONE',  ( -0.005948725901132494338, -2.107936428766274073, -0.7005084057759867200 ) ) ;
#228=CARTESIAN_POINT ( 'NONE',  ( 0.3622253751127874066, -1.756884464425453984, -0.4902987826081479650 ) ) ;
#234=CIRCLE ( 'NONE', #1526, 0.01499999999999997689 ) ;
#237=CARTESIAN_POINT ( 'NONE',  ( 0.1717449021412840726, -1.802002661843876696, -0.6814448880503549688 ) ) ;
#239=ORIENTED_EDGE ( 'NONE', *, *, #16957, .F. ) ;
#242=CARTESIAN_POINT ( 'NONE',  ( 0.6473787150721044270, -1.455279521797666176, -0.6250000000000000000 ) ) ;
#247=EDGE_CURVE ( 'NONE', #13465, #5600, #27350, .T. ) ;
#257=CARTESIAN_POINT ( 'NONE',  ( 0.5254844390776584051, -1.675905034379785441, -0.4432393896124048327 ) ) ;
#258=DIRECTION ( 'NONE',  ( -0.1520288461498812416, 0.000000000000000000, -0.9883760569430726228 ) ) ;
#262=AXIS2_PLACEMENT_3D ( 'NONE', #17751, #2132, #10998 ) ;
#277=EDGE_CURVE ( 'NONE', #20339, #32089, #8062, .T. ) ;
#281=CARTESIAN_POINT ( 'NONE',  ( 0.3787041472384312102, -1.708164842082610768, -0.4136294741777339912 ) ) ;
#304=ORIENTED_EDGE ( 'NONE', *, *, #18503, .T. ) ;
#305=FACE_OUTER_BOUND ( 'NONE', #5750, .T. ) ;
#314=CARTESIAN_POINT ( 'NONE',  ( 0.5747203984579013492, -1.612743926285909346, -0.5166151207188712791 ) ) ;
#322=AXIS2_PLACEMENT_3D ( 'NONE', #31448, #24882, #34726 ) ;
#333=AXIS2_PLACEMENT_3D ( 'NONE', #23656, #17661, #2039 ) ;
#338=CARTESIAN_POINT ( 'NONE',  ( 0.3516101416147200953, -1.741639419776285891, -0.7019724635597545115 ) ) ;
#341=EDGE_LOOP ( 'NONE', ( #30120, #14606, #19680, #33856 ) ) ;
#351=CARTESIAN_POINT ( 'NONE',  ( 0.3840974138826053763, -1.688245147359099363, -0.3350098725068151317 ) ) ;
#353=CARTESIAN_POINT ( 'NONE',  ( 0.1909286924077255032, -1.257064795538239022, -0.7462941026102624109 ) ) ;
#357=VERTEX_POINT ( 'NONE', #20912 ) ;
#359=ORIENTED_EDGE ( 'NONE', *, *, #38638, .T. ) ;
#365=LINE ( 'NONE', #31390, #21816 ) ;
#370=CARTESIAN_POINT ( 'NONE',  ( 0.3938780453836632223, -1.723328632354485634, -0.3054719800402591612 ) ) ;
#389=CARTESIAN_POINT ( 'NONE',  ( 0.2110034642138055860, -1.187742706213460453, -0.5155029497116575543 ) ) ;
#394=VERTEX_POINT ( 'NONE', #5240 ) ;
#398=CARTESIAN_POINT ( 'NONE',  ( 0.3641487592347181779, -1.992207614157224249, -0.4748857690446578461 ) ) ;
#399=CARTESIAN_POINT ( 'NONE',  ( 0.5319948190214550676, -1.638784817636518287, -0.4758175433331751081 ) ) ;
#403=CARTESIAN_POINT ( 'NONE',  ( 0.1999999999999787226, -2.097675824466502803, -0.4688691127277801463 ) ) ;
#417=ORIENTED_EDGE ( 'NONE', *, *, #17337, .F. ) ;
#421=CARTESIAN_POINT ( 'NONE',  ( 0.2484857473122376870, -1.339293634572156000, -0.5155029497116575543 ) ) ;
#422=CARTESIAN_POINT ( 'NONE',  ( 0.5054609057099638258, -1.017757956463559710, -0.5155029497116575543 ) ) ;
#429=B_SPLINE_CURVE_WITH_KNOTS ( 'NONE', 3,
 ( #33409, #30321, #2154, #27259, #8510, #21076, #33600, #25899, #40396, #39981, #9535, #33825, #37107, #27858, #12221, #14899, #24784, #31148, #37303, #15091, #9116, #21681, #34211, #36898, #18379, #6023 ),
 .UNSPECIFIED., .F., .F.,
 ( 4, 2, 2, 2, 2, 2, 2, 2, 2, 2, 2, 2, 4 ),
 ( 0.02890318467689641582, 0.02962064806864088753, 0.03033811146038536272, 0.03177303824387431308, 0.03320796502736327038, 0.03464289181085222769, 0.03607781859434118499, 0.03751274537783013535, 0.04038259894480807077, 0.04325245251178599926, 0.04612230607876392774, 0.04899215964574185622, 0.05186201321271978470 ),
 .UNSPECIFIED. ) ;
#430=CARTESIAN_POINT ( 'NONE',  ( 0.06724117332272876169, -1.895739979645849838, -0.3418766208214948921 ) ) ;
#438=ADVANCED_FACE ( 'NONE', ( #1586, #1798 ), #33433, .F. ) ;
#442=DIRECTION ( 'NONE',  ( 0.4999551463232373427, -0.8660512985181134660, 0.000000000000000000 ) ) ;
#454=CARTESIAN_POINT ( 'NONE',  ( 0.5843363353628658885, -1.492391990693552328, -0.4353912382336290188 ) ) ;
#457=ORIENTED_EDGE ( 'NONE', *, *, #17968, .F. ) ;
#459=ADVANCED_FACE ( 'NONE', ( #34241 ), #21807, .T. ) ;
#471=CARTESIAN_POINT ( 'NONE',  ( 0.5368241748133022462, -1.669358817950476137, -0.4818844110025696237 ) ) ;
#474=DIRECTION ( 'NONE',  ( 0.8660512985181135770, 0.4999551463232370652, 0.000000000000000000 ) ) ;
#477=ORIENTED_EDGE ( 'NONE', *, *, #21320, .F. ) ;
#479=CARTESIAN_POINT ( 'NONE',  ( 0.3902040701542698331, -1.764767632342756798, -0.4833641654129184895 ) ) ;
#491=CARTESIAN_POINT ( 'NONE',  ( 0.3998481532917401160, -1.682844229318920304, -0.4042724543747899246 ) ) ;
#504=CIRCLE ( 'NONE', #8333, 0.02999999999999995379 ) ;
#512=CARTESIAN_POINT ( 'NONE',  ( 0.4843318811940854340, -1.649192016167395192, -0.4000974106332781388 ) ) ;
#516=ORIENTED_EDGE ( 'NONE', *, *, #2607, .T. ) ;
#532=CARTESIAN_POINT ( 'NONE',  ( 0.4528004050422974602, -1.638392014206256020, -0.6172987386429681367 ) ) ;
#537=CARTESIAN_POINT ( 'NONE',  ( 0.4422358757816878816, -1.108045738334233254, -0.3965663110662911994 ) ) ;
#545=VERTEX_POINT ( 'NONE', #9758 ) ;
#546=CARTESIAN_POINT ( 'NONE',  ( 0.4409062655693438137, -1.690090444797295977, -0.7462941026102624109 ) ) ;
#551=AXIS2_PLACEMENT_3D ( 'NONE', #7637, #29451, #26365 ) ;
#554=ORIENTED_EDGE ( 'NONE', *, *, #5489, .T. ) ;
#556=VERTEX_POINT ( 'NONE', #32526 ) ;
#558=CARTESIAN_POINT ( 'NONE',  ( 0.2436109149983881617, -1.585023087768267169, -0.3520240440213115996 ) ) ;
#561=CARTESIAN_POINT ( 'NONE',  ( -2.112273405726188513E-14, -2.097675824466503691, -0.2588528740066097233 ) ) ;
#574=CARTESIAN_POINT ( 'NONE',  ( 0.3999999999999786504, -2.166079853131637201, -0.5407606602423821185 ) ) ;
#582=ORIENTED_EDGE ( 'NONE', *, *, #14495, .T. ) ;
#584=CARTESIAN_POINT ( 'NONE',  ( 0.3402959632056916650, -1.632552626064600165, -0.5940485371126216219 ) ) ;
#590=DIRECTION ( 'NONE',  ( -1.000000000000000000, 0.000000000000000000, 0.000000000000000000 ) ) ;
#593=CARTESIAN_POINT ( 'NONE',  ( 0.3892234394240923212, -1.604307713088686027, -0.4126549618408641429 ) ) ;
#600=CARTESIAN_POINT ( 'NONE',  ( 0.4002945597911881093, -1.748174800066815138, -0.4981529669132083171 ) ) ;
#602=CARTESIAN_POINT ( 'NONE',  ( 0.1809966328114128442, -1.222385076516254054, -0.5155029497116575543 ) ) ;
#611=DIRECTION ( 'NONE',  ( 0.8660512985181135770, 0.4999551463232370652, 0.000000000000000000 ) ) ;
#612=CARTESIAN_POINT ( 'NONE',  ( 0.1907332430659512135, -1.952008480481784547, -0.3293335493387484769 ) ) ;
#617=VERTEX_POINT ( 'NONE', #3589 ) ;
#618=CARTESIAN_POINT ( 'NONE',  ( 0.3885003709713005238, -1.773188177334034110, -0.5275292682893175655 ) ) ;
#619=CYLINDRICAL_SURFACE ( 'NONE', #2298, 0.2500000000000000000 ) ;
#623=CARTESIAN_POINT ( 'NONE',  ( 0.6634599440086400568, -1.584707707048322867, -0.5155029497116575543 ) ) ;
#625=CARTESIAN_POINT ( 'NONE',  ( 0.3868393977302779785, -1.755942212376543354, -0.5592601700348395211 ) ) ;
#627=DIRECTION ( 'NONE',  ( 0.8660512985181134660, 0.4999551463232371762, 0.000000000000000000 ) ) ;
#633=CARTESIAN_POINT ( 'NONE',  ( 0.6461037703316800940, -1.403558513617581660, -0.6142287214927136807 ) ) ;
#642=ORIENTED_EDGE ( 'NONE', *, *, #31346, .T. ) ;
#644=EDGE_CURVE ( 'NONE', #23751, #21815, #37287, .T. ) ;
#652=VERTEX_POINT ( 'NONE', #25416 ) ;
#659=LINE ( 'NONE', #6982, #22105 ) ;
#674=CARTESIAN_POINT ( 'NONE',  ( 0.3409152363046951129, -1.516880185093671063, -0.7462941026102624109 ) ) ;
#684=CARTESIAN_POINT ( 'NONE',  ( 0.3729107345132364748, -1.707610029665299178, -0.6887163269807711208 ) ) ;
#686=CARTESIAN_POINT ( 'NONE',  ( 0.3795613398208534384, -1.760143698493221942, -0.5723197561600823491 ) ) ;
#690=ORIENTED_EDGE ( 'NONE', *, *, #721, .T. ) ;
#694=CARTESIAN_POINT ( 'NONE',  ( 0.5119721139670522225, -1.648521794865212220, -0.4427754798362790734 ) ) ;
#695=ORIENTED_EDGE ( 'NONE', *, *, #38154, .F. ) ;
#703=EDGE_CURVE ( 'NONE', #23099, #24229, #34003, .T. ) ;
#710=ORIENTED_EDGE ( 'NONE', *, *, #5045, .F. ) ;
#711=CARTESIAN_POINT ( 'NONE',  ( 0.6205222882181153921, -1.535344779211800015, -0.6305106974072310910 ) ) ;
#718=DIRECTION ( 'NONE',  ( 0.7956551220374313838, 0.4593167559955297352, 0.3949190352937462234 ) ) ;
#721=EDGE_CURVE ( 'NONE', #15639, #25087, #28195, .T. ) ;
#732=CIRCLE ( 'NONE', #30256, 0.01500000000000007057 ) ;
#751=CARTESIAN_POINT ( 'NONE',  ( 0.4642169916328606205, -1.610048112669862030, -0.3779295768151388901 ) ) ;
#762=ADVANCED_FACE ( 'NONE', ( #3496 ), #29429, .T. ) ;
#763=B_SPLINE_CURVE_WITH_KNOTS ( 'NONE', 3,
 ( #13876, #38772, #7720, #17729, #29528, #2111, #13502 ),
 .UNSPECIFIED., .F., .F.,
 ( 4, 3, 4 ),
 ( -6.000000000366142690E-08, 1.760240343512842892E-21, 0.0002642484537205252570 ),
 .UNSPECIFIED. ) ;
#764=AXIS2_PLACEMENT_3D ( 'NONE', #30199, #23459, #26922 ) ;
#766=EDGE_CURVE ( 'NONE', #30726, #17298, #14950, .T. ) ;
#779=CYLINDRICAL_SURFACE ( 'NONE', #8863, 0.2500000000000000000 ) ;
#781=CARTESIAN_POINT ( 'NONE',  ( 0.5435064000818763397, -1.629330203429091739, -0.4449807330069644462 ) ) ;
#784=ORIENTED_EDGE ( 'NONE', *, *, #14738, .F. ) ;
#790=CIRCLE ( 'NONE', #27688, 0.2200000000000000844 ) ;
#791=EDGE_CURVE ( 'NONE', #21815, #617, #38610, .T. ) ;
#803=ORIENTED_EDGE ( 'NONE', *, *, #30064, .T. ) ;
#808=CARTESIAN_POINT ( 'NONE',  ( 0.3916693287292108416, -1.957780039576698217, -0.4986156861099343418 ) ) ;
#809=CARTESIAN_POINT ( 'NONE',  ( -0.004906298587631805104, -2.107936428766274073, -0.2870436526301869407 ) ) ;
#810=CARTESIAN_POINT ( 'NONE',  ( 0.3219636445852379070, -1.527820583036367141, -0.7368875844864777314 ) ) ;
#811=DIRECTION ( 'NONE',  ( 0.4999551463232373427, -0.8660512985181134660, 0.000000000000000000 ) ) ;
#812=CARTESIAN_POINT ( 'NONE',  ( -2.112273405726188513E-14, -1.835409001655643690, -0.3543101909453316156 ) ) ;
#816=DIRECTION ( 'NONE',  ( 0.000000000000000000, 0.3420201433256706003, -0.9396926207859077618 ) ) ;
#821=CARTESIAN_POINT ( 'NONE',  ( 0.6491414849553497346, -1.426744591349599967, -0.6169505267336127252 ) ) ;
#826=AXIS2_PLACEMENT_3D ( 'NONE', #29812, #40436, #14173 ) ;
#829=CARTESIAN_POINT ( 'NONE',  ( 0.5915319031500693159, -1.513102603207748365, -0.3972843660575071101 ) ) ;
#833=CARTESIAN_POINT ( 'NONE',  ( 0.2059273467974226945, -1.283046334493782803, -0.2869361388274795921 ) ) ;
#841=CARTESIAN_POINT ( 'NONE',  ( 0.5797229963041876655, -1.607661183008572969, -0.4675097618473461059 ) ) ;
#846=DIRECTION ( 'NONE',  ( 1.000000000000000000, 0.000000000000000000, 0.000000000000000000 ) ) ;
#848=DIRECTION ( 'NONE',  ( -0.1280454979611833077, 0.000000000000000000, 0.9917682947401941229 ) ) ;
#856=CARTESIAN_POINT ( 'NONE',  ( 0.07288795999653738256, -1.414255277265392907, -0.3388138788922953060 ) ) ;
#858=VERTEX_POINT ( 'NONE', #6373 ) ;
#870=DIRECTION ( 'NONE',  ( 1.000000000000000000, 0.000000000000000000, 0.000000000000000000 ) ) ;
#872=CARTESIAN_POINT ( 'NONE',  ( 0.4333792208851959815, -1.117102659751931792, -0.6448351790779591752 ) ) ;
#881=CARTESIAN_POINT ( 'NONE',  ( 0.1741751201940545390, -1.802433987137200599, -0.6515250642801660996 ) ) ;
#882=ADVANCED_FACE ( 'NONE', ( #3705 ), #35378, .F. ) ;
#886=B_SPLINE_CURVE_WITH_KNOTS ( 'NONE', 3,
 ( #29139, #8133, #1587, #11038, #14314, #7524, #10418, #35498, #20708, #13892, #33240, #14111, #16809, #20102, #39002, #7305, #32818, #7733, #17197, #13699, #10834, #35926, #4833, #26266, #4439, #16999 ),
 .UNSPECIFIED., .F., .F.,
 ( 4, 2, 2, 2, 2, 2, 2, 2, 2, 2, 2, 2, 4 ),
 ( 0.000000000000000000, 0.0006636363572759321466, 0.001327272714551864293, 0.001659090893189832426, 0.001990909071827800560, 0.002322727250465768476, 0.002654545429103736826, 0.003318181786379673093, 0.003649999965017641009, 0.003981818143655608058, 0.004313636322293576408, 0.004645454500931543891, 0.005309090858207477122 ),
 .UNSPECIFIED. ) ;
#899=ORIENTED_EDGE ( 'NONE', *, *, #34731, .T. ) ;
#901=DIRECTION ( 'NONE',  ( -0.8660512985181135770, -0.4999551463232370652, 0.000000000000000000 ) ) ;
#903=CIRCLE ( 'NONE', #4766, 0.02999999999999999195 ) ;
#905=CARTESIAN_POINT ( 'NONE',  ( 0.3757471142192211344, -1.766731021160330428, -0.5680748514784754732 ) ) ;
#907=CARTESIAN_POINT ( 'NONE',  ( 0.6273212425683272198, -1.617116560674602521, -0.5218031926565810386 ) ) ;
#917=AXIS2_PLACEMENT_3D ( 'NONE', #1456, #13588, #13971 ) ;
#919=CARTESIAN_POINT ( 'NONE',  ( 0.2927350798622619377, -1.544518291098220697, -0.6925464747855744063 ) ) ;
#930=EDGE_CURVE ( 'NONE', #7674, #5500, #39914, .T. ) ;
#935=ADVANCED_FACE ( 'NONE', ( #4687 ), #15006, .T. ) ;
#952=CARTESIAN_POINT ( 'NONE',  ( 0.3817983344580043181, -1.702428809890406125, -0.3364609660280786785 ) ) ;
#965=DIRECTION ( 'NONE',  ( -0.4999551463232373427, 0.8660512985181134660, -0.000000000000000000 ) ) ;
#969=CARTESIAN_POINT ( 'NONE',  ( 0.4634712904840416758, -1.711704060178988129, -0.5155029497116575543 ) ) ;
#971=CIRCLE ( 'NONE', #8802, 0.1033070866141734129 ) ;
#973=TOROIDAL_SURFACE ( 'NONE', #21338, 0.05000000000000000971, 0.2000000000000000111 ) ;
#975=EDGE_CURVE ( 'NONE', #4341, #5197, #7083, .T. ) ;
#977=CARTESIAN_POINT ( 'NONE',  ( 0.4872883505774054380, -1.680912827369504425, -0.6127499270552401178 ) ) ;
#984=ORIENTED_EDGE ( 'NONE', *, *, #9908, .F. ) ;
#992=ADVANCED_FACE ( 'NONE', ( #34911 ), #9813, .T. ) ;
#995=EDGE_CURVE ( 'NONE', #29245, #13061, #28783, .T. ) ;
#996=CARTESIAN_POINT ( 'NONE',  ( -2.115421433687637455E-14, -2.107936428766274073, -0.7005084057759867200 ) ) ;
#1006=CARTESIAN_POINT ( 'NONE',  ( 0.3784855106043947814, -1.091058466892998347, -0.5155029497116575543 ) ) ;
#1008=CIRCLE ( 'NONE', #33149, 0.1699999999999999012 ) ;
#1016=ORIENTED_EDGE ( 'NONE', *, *, #12873, .F. ) ;
#1020=AXIS2_PLACEMENT_3D ( 'NONE', #17478, #14372, #39469 ) ;
#1022=CARTESIAN_POINT ( 'NONE',  ( 0.03328606440775329356, -1.535999360653146573, -0.3785507177379214272 ) ) ;
#1024=DIRECTION ( 'NONE',  ( 0.7956551220374307176, 0.4593167559955306789, -0.3949190352937466675 ) ) ;
#1026=CARTESIAN_POINT ( 'NONE',  ( 0.3927990398488649393, -1.752501822930178310, -0.5454427608432544927 ) ) ;
#1028=CARTESIAN_POINT ( 'NONE',  ( 0.3916540994123360875, -1.783423193857804234, -0.4823378820693604574 ) ) ;
#1034=CARTESIAN_POINT ( 'NONE',  ( 0.6613984642527299673, -1.498580572238303876, -0.6190489083608020637 ) ) ;
#1044=CARTESIAN_POINT ( 'NONE',  ( 0.5932811311191399373, -1.498634114660479133, -0.3907251365715369573 ) ) ;
#1053=CARTESIAN_POINT ( 'NONE',  ( 0.5747203984579013492, -1.612743926285909346, -0.5166151207188712791 ) ) ;
#1058=CYLINDRICAL_SURFACE ( 'NONE', #21114, 0.2500000000000000000 ) ;
#1059=ORIENTED_EDGE ( 'NONE', *, *, #33898, .F. ) ;
#1063=CARTESIAN_POINT ( 'NONE',  ( 0.6335899703865320864, -1.596177751663357736, -0.4443638777805991591 ) ) ;
#1067=CARTESIAN_POINT ( 'NONE',  ( 0.1365034152848375870, -1.346425269259858615, -0.3192896525261769702 ) ) ;
#1079=DIRECTION ( 'NONE',  ( 0.4999551463232373427, -0.8660512985181134660, 0.000000000000000000 ) ) ;
#1080=CARTESIAN_POINT ( 'NONE',  ( 0.1999999999999789724, -2.183180860297921466, -0.4937760292030871079 ) ) ;
#1085=CARTESIAN_POINT ( 'NONE',  ( 0.2737193247896483328, -1.556389522379076906, -0.6850497769148254923 ) ) ;
#1087=CARTESIAN_POINT ( 'NONE',  ( 0.3580912810175859162, -1.816808367081122366, -0.4824505002470479420 ) ) ;
#1090=AXIS2_PLACEMENT_3D ( 'NONE', #30733, #23972, #2555 ) ;
#1091=CARTESIAN_POINT ( 'NONE',  ( 0.3625960434667531151, -1.762758894398492204, -0.5926935080085831142 ) ) ;
#1093=ORIENTED_EDGE ( 'NONE', *, *, #33885, .F. ) ;
#1097=CARTESIAN_POINT ( 'NONE',  ( 0.4799438572844808015, -1.658878325107475904, -0.4199344158348157774 ) ) ;
#1101=ORIENTED_EDGE ( 'NONE', *, *, #2482, .F. ) ;
#1105=CARTESIAN_POINT ( 'NONE',  ( 0.6291611629923075100, -1.616054409175744278, -0.4658884253126942543 ) ) ;
#1114=CARTESIAN_POINT ( 'NONE',  ( 0.4438420790631848467, -1.592365463309330709, -0.4209907625009123300 ) ) ;
#1117=CARTESIAN_POINT ( 'NONE',  ( 0.4999694634270406834, -1.038248053136179960, -0.5155029497116575543 ) ) ;
#1119=CARTESIAN_POINT ( 'NONE',  ( 0.5053588047760253499, -1.583603243833816787, -0.5401600205605632254 ) ) ;
#1120=AXIS2_PLACEMENT_3D ( 'NONE', #1706, #14226, #5154 ) ;
#1126=( CONVERSION_BASED_UNIT ( 'INCH', #10967 ) LENGTH_UNIT ( ) NAMED_UNIT ( #23398 ) );
#1133=ADVANCED_FACE ( 'NONE', ( #20922 ), #15017, .T. ) ;
#1138=CARTESIAN_POINT ( 'NONE',  ( 0.3666666666666453800, -2.097675824466503691, -0.7286991843995640483 ) ) ;
#1173=B_SPLINE_SURFACE_WITH_KNOTS ( 'NONE', 3, 3, ( 
 ( #14993, #37206, #12320, #5514, #18686, #2647, #37397, #27955, #24875, #18078, #15609, #9209, #21781 ),
 ( #34310, #27742, #40278, #9026, #6120, #30631, #12506, #27546, #8813, #3065, #21391, #21587, #28155 ),
 ( #19, #19692, #25478, #28557, #31637, #31846, #38409, #28346, #3452, #430, #16010, #22394, #26097 ),
 ( #12926, #18905, #25271, #16608, #38613, #1022, #28944, #13531, #32226, #21996, #22602, #31442, #809 ) ),
 .UNSPECIFIED., .F., .F., .F.,
 ( 4, 4 ),
 ( 4, 3, 3, 3, 4 ),
 ( 0.4849526895556616202, 1.012265746469021233 ),
 ( -2.219619483495854910E-15, 0.2500000000000086597, 0.5000000000000195399, 0.7500000000000304201, 1.000000000000041300 ),
 .UNSPECIFIED. ) ;
#1184=CARTESIAN_POINT ( 'NONE',  ( 0.4806319512830223850, -1.112120366466635257, -0.6266239386966213631 ) ) ;
#1194=DIRECTION ( 'NONE',  ( 0.000000000000000000, 0.000000000000000000, -1.000000000000000000 ) ) ;
#1202=DIRECTION ( 'NONE',  ( 0.4999551463232372317, -0.8660512985181135770, 0.000000000000000000 ) ) ;
#1204=CARTESIAN_POINT ( 'NONE',  ( 0.1980860629012485552, -1.670291652337890342, -0.3592990252404365537 ) ) ;
#1214=DIRECTION ( 'NONE',  ( 1.000000000000000000, 0.000000000000000000, 0.000000000000000000 ) ) ;
#1225=CARTESIAN_POINT ( 'NONE',  ( 0.6164351338053631890, -1.544991685130753911, -0.6274595476820803430 ) ) ;
#1233=CARTESIAN_POINT ( 'NONE',  ( 0.5951414857627569388, -1.550313246946717571, -0.4562001837530886839 ) ) ;
#1235=CARTESIAN_POINT ( 'NONE',  ( 0.4954266169953891463, -1.646634881173000720, -0.6269490058875392124 ) ) ;
#1239=VERTEX_POINT ( 'NONE', #13660 ) ;
#1257=CARTESIAN_POINT ( 'NONE',  ( 0.06734526529546210061, -1.429207128842583163, -0.3669778653616447839 ) ) ;
#1270=PLANE ( 'NONE',  #22723 ) ;
#1277=CARTESIAN_POINT ( 'NONE',  ( 0.3663377407856179269, -1.767777433818015220, -0.5763279985969705921 ) ) ;
#1280=ORIENTED_EDGE ( 'NONE', *, *, #19499, .F. ) ;
#1286=ORIENTED_EDGE ( 'NONE', *, *, #27088, .T. ) ;
#1306=CARTESIAN_POINT ( 'NONE',  ( 0.4243666725459964151, -1.591076223527387423, -0.4156371400837810537 ) ) ;
#1309=FACE_OUTER_BOUND ( 'NONE', #32759, .T. ) ;
#1325=DIRECTION ( 'NONE',  ( 0.000000000000000000, 0.000000000000000000, -1.000000000000000000 ) ) ;
#1333=CARTESIAN_POINT ( 'NONE',  ( 0.1315192713089369247, -1.308544259391007492, -0.6883081435772964163 ) ) ;
#1338=ORIENTED_EDGE ( 'NONE', *, *, #13424, .F. ) ;
#1357=CARTESIAN_POINT ( 'NONE',  ( 0.03070601528493977633, -1.915553355962458459, -0.3085447803061387995 ) ) ;
#1358=CARTESIAN_POINT ( 'NONE',  ( 0.5325603410779075064, -1.633963683135810641, -0.5997096917800632809 ) ) ;
#1387=ADVANCED_FACE ( 'NONE', ( #36491 ), #26647, .F. ) ;
#1390=CARTESIAN_POINT ( 'NONE',  ( 0.2047062219756962675, -1.651037923760164228, -0.3589593011634661934 ) ) ;
#1393=AXIS2_PLACEMENT_3D ( 'NONE', #8528, #18400, #17788 ) ;
#1398=CARTESIAN_POINT ( 'NONE',  ( 0.2914323826288400809, -1.233685883474753497, -0.5166151207188711680 ) ) ;
#1404=AXIS2_PLACEMENT_3D ( 'NONE', #9105, #17757, #21271 ) ;
#1412=PLANE ( 'NONE',  #6759 ) ;
#1417=EDGE_CURVE ( 'NONE', #20049, #23858, #4477, .T. ) ;
#1419=CARTESIAN_POINT ( 'NONE',  ( 0.5834653944837133732, -1.511631883459902514, -0.5858460414140914674 ) ) ;
#1429=CARTESIAN_POINT ( 'NONE',  ( 0.3650258023173150734, -1.764296560404615466, -0.5885076244517606359 ) ) ;
#1444=CARTESIAN_POINT ( 'NONE',  ( 0.2009277952559025970, -1.274385821372987060, -0.3194728440340255382 ) ) ;
#1447=CARTESIAN_POINT ( 'NONE',  ( 0.004899539180344515861, -1.812954824892113237, -0.3559391749954987083 ) ) ;
#1454=CIRCLE ( 'NONE', #27041, 0.02999999999999998848 ) ;
#1456=CARTESIAN_POINT ( 'NONE',  ( 0.2484857473122377980, -1.339293634572156000, -0.5155029497116575543 ) ) ;
#1467=DIRECTION ( 'NONE',  ( 0.7956551220374296074, 0.4593167559955304569, 0.3949190352937488879 ) ) ;
#1470=CARTESIAN_POINT ( 'NONE',  ( 0.3996493990393679696, -2.075761934976077860, -0.5159267940723109014 ) ) ;
#1473=EDGE_LOOP ( 'NONE', ( #19177, #35271, #27486, #31971 ) ) ;
#1478=CARTESIAN_POINT ( 'NONE',  ( 0.4359176154167935247, -1.577352042444816416, -0.5155029497116575543 ) ) ;
#1512=CARTESIAN_POINT ( 'NONE',  ( 0.4584717390208091770, -1.703043547193807017, -0.5155029497116575543 ) ) ;
#1520=AXIS2_PLACEMENT_3D ( 'NONE', #4415, #26851, #10804 ) ;
#1526=AXIS2_PLACEMENT_3D ( 'NONE', #1117, #26386, #29051 ) ;
#1529=CARTESIAN_POINT ( 'NONE',  ( 0.6413879784614744395, -1.405912376546664122, -0.6250000000000000000 ) ) ;
#1536=CARTESIAN_POINT ( 'NONE',  ( 0.04118663679044942683, -1.516485496198475946, -0.6452587487763896679 ) ) ;
#1538=ORIENTED_EDGE ( 'NONE', *, *, #36074, .F. ) ;
#1539=CARTESIAN_POINT ( 'NONE',  ( 0.3545963309600190794, -1.820992936139588458, -0.5160179355990298644 ) ) ;
#1544=CARTESIAN_POINT ( 'NONE',  ( 0.6089330441038812713, -1.477473485466218150, -0.6250000000000000000 ) ) ;
#1551=CARTESIAN_POINT ( 'NONE',  ( 0.3845608912840868254, -1.768804211478402166, -0.5723197561600831262 ) ) ;
#1563=AXIS2_PLACEMENT_3D ( 'NONE', #2879, #40310, #12140 ) ;
#1564=CARTESIAN_POINT ( 'NONE',  ( 0.03025752215418233901, -1.950362531980313285, -0.3012757290405999044 ) ) ;
#1565=CARTESIAN_POINT ( 'NONE',  ( 0.5454473090585744144, -1.628634442125448167, -0.5828508516191583944 ) ) ;
#1579=CARTESIAN_POINT ( 'NONE',  ( 0.4334739817046469601, -1.659740982267900566, -0.5155029497116575543 ) ) ;
#1586=FACE_BOUND ( 'NONE', #30002, .T. ) ;
#1587=CARTESIAN_POINT ( 'NONE',  ( 0.5839362087672538282, -1.507072137279306334, -0.5885553949852400102 ) ) ;
#1602=CARTESIAN_POINT ( 'NONE',  ( 0.3900356592778671527, -1.754097070625186605, -0.4603106969345188149 ) ) ;
#1610=ADVANCED_FACE ( 'NONE', ( #37094 ), #21785, .T. ) ;
#1614=TOROIDAL_SURFACE ( 'NONE', #8160, 0.04999999999999998196, 0.1700000000000000400 ) ;
#1615=CARTESIAN_POINT ( 'NONE',  ( 0.3992403239432529283, -1.683235622436187073, -0.6263438071736542323 ) ) ;
#1617=CARTESIAN_POINT ( 'NONE',  ( 0.6009539617556340918, -1.596610001391108868, -0.5128529812280162581 ) ) ;
#1625=CARTESIAN_POINT ( 'NONE',  ( 0.5750311553790389274, -1.568077294875266814, -0.4484120973757802497 ) ) ;
#1631=ORIENTED_EDGE ( 'NONE', *, *, #33062, .F. ) ;
#1634=CARTESIAN_POINT ( 'NONE',  ( 0.4670822870386998060, -1.088164015307882648, -0.6212900150988791559 ) ) ;
#1636=CARTESIAN_POINT ( 'NONE',  ( 0.4697228370620195048, -1.442521976758482261, -0.5166151207188711680 ) ) ;
#1637=ORIENTED_EDGE ( 'NONE', *, *, #23407, .T. ) ;
#1645=CYLINDRICAL_SURFACE ( 'NONE', #34216, 0.2500000000000000000 ) ;
#1646=VERTEX_POINT ( 'NONE', #9408 ) ;
#1647=CARTESIAN_POINT ( 'NONE',  ( 0.1734973056165642902, -1.209394307038482497, -0.5155029497116575543 ) ) ;
#1652=CARTESIAN_POINT ( 'NONE',  ( 0.2469141422421070875, -1.581573626495411444, -0.3511777555542848206 ) ) ;
#1653=FACE_OUTER_BOUND ( 'NONE', #6648, .T. ) ;
#1658=CARTESIAN_POINT ( 'NONE',  ( 0.3696433394773024350, -2.076155315806792245, -0.5157937231490886676 ) ) ;
#1660=CARTESIAN_POINT ( 'NONE',  ( 0.1364676818254310919, -1.302864912412562193, -0.3444472864111620125 ) ) ;
#1663=CARTESIAN_POINT ( 'NONE',  ( 0.5201389011762601600, -1.665685209299224923, -0.5911274130876347233 ) ) ;
#1665=AXIS2_PLACEMENT_3D ( 'NONE', #15901, #31142, #34625 ) ;
#1675=CARTESIAN_POINT ( 'NONE',  ( 0.3125627377754333081, -1.533273879788720429, -0.7004264455586597382 ) ) ;
#1676=CIRCLE ( 'NONE', #32502, 0.02999999999999998848 ) ;
#1677=DIRECTION ( 'NONE',  ( -0.4999551463232385085, 0.8660512985181127998, 0.000000000000000000 ) ) ;
#1678=EDGE_CURVE ( 'NONE', #14515, #30753, #28548, .T. ) ;
#1686=ORIENTED_EDGE ( 'NONE', *, *, #35073, .T. ) ;
#1687=CARTESIAN_POINT ( 'NONE',  ( 0.4710977142973246656, -1.661186711027922813, -0.4170720528719246700 ) ) ;
#1697=DIRECTION ( 'NONE',  ( 0.8660512985181135770, 0.4999551463232371207, 0.000000000000000000 ) ) ;
#1700=CARTESIAN_POINT ( 'NONE',  ( 0.4409062655693438137, -1.690090444797295977, -0.2869361388274795921 ) ) ;
#1702=CARTESIAN_POINT ( 'NONE',  ( 0.1934290844966307377, -1.261396119720670894, -0.7137149802747378979 ) ) ;
#1706=CARTESIAN_POINT ( 'NONE',  ( 0.3984114568195520345, -1.599003643269838904, -0.5155029497116575543 ) ) ;
#1709=( BOUNDED_SURFACE ( )  B_SPLINE_SURFACE ( 3, 2, ( 
 ( #33947, #12337, #5747 ),
 ( #18305, #30845, #2667 ),
 ( #15210, #27765, #12132 ),
 ( #6148, #24894, #18712 ) ),
 .UNSPECIFIED., .F., .F., .F. ) 
 B_SPLINE_SURFACE_WITH_KNOTS ( ( 4, 4 ),
 ( 3, 3 ),
 ( -1.734723475976807094E-18, 0.0003263618124877773626 ),
 ( 0.000000000000000000, 1.000000000000000000 ),
 .UNSPECIFIED. ) 
 GEOMETRIC_REPRESENTATION_ITEM ( )  RATIONAL_B_SPLINE_SURFACE ( (
 ( 1.000000000000000000, 0.7071496063340664273, 1.000000000000000000),
 ( 1.000000000000000000, 0.7071209263092794739, 1.000000000000000000),
 ( 1.000000000000000000, 0.7071067771900807486, 1.000000000000000000),
 ( 1.000000000000000000, 0.7071067811865479058, 1.000000000000000000) ) ) 
 REPRESENTATION_ITEM ( '' )  SURFACE ( )  );
#1714=EDGE_CURVE ( 'NONE', #30709, #1646, #24190, .T. ) ;
#1715=CARTESIAN_POINT ( 'NONE',  ( 0.3927316539789887928, -1.706278926685924180, -0.4292189291772694482 ) ) ;
#1719=CARTESIAN_POINT ( 'NONE',  ( 0.3699999999999788458, -2.097675824466504135, -0.4688691127277798687 ) ) ;
#1723=EDGE_CURVE ( 'NONE', #28841, #5281, #13390, .T. ) ;
#1724=DIRECTION ( 'NONE',  ( -0.4999551463232377313, 0.8660512985181132439, -0.000000000000000000 ) ) ;
#1736=CARTESIAN_POINT ( 'NONE',  ( 0.4112193008908943126, -1.591609915475965975, -0.6177460231409253044 ) ) ;
#1741=CARTESIAN_POINT ( 'NONE',  ( 0.2999999999999791167, -2.097675824466505023, -0.7286991843995648255 ) ) ;
#1743=CARTESIAN_POINT ( 'NONE',  ( -2.112273405726188513E-14, -2.107936428766274073, -0.2870436526301869962 ) ) ;
#1745=EDGE_LOOP ( 'NONE', ( #12346, #3380, #15937, #13795 ) ) ;
#1751=CARTESIAN_POINT ( 'NONE',  ( 0.06561571374232599840, -1.525176766320938793, -0.6748652540125912314 ) ) ;
#1776=CARTESIAN_POINT ( 'NONE',  ( 0.3911589123679613533, -1.952241739367067019, -0.4946140563714283567 ) ) ;
#1780=DIRECTION ( 'NONE',  ( 1.000000000000000000, 0.000000000000000000, 0.000000000000000000 ) ) ;
#1788=CARTESIAN_POINT ( 'NONE',  ( 0.2629665421248923995, -1.157745397434066126, -0.5155029497116575543 ) ) ;
#1798=FACE_OUTER_BOUND ( 'NONE', #5960, .T. ) ;
#1802=VERTEX_POINT ( 'NONE', #11047 ) ;
#1806=CARTESIAN_POINT ( 'NONE',  ( 0.4644259937802360239, -1.101352082929256682, -0.6430948353041650023 ) ) ;
#1808=ORIENTED_EDGE ( 'NONE', *, *, #14754, .F. ) ;
#1815=CARTESIAN_POINT ( 'NONE',  ( 0.4023438766660552557, -1.746991767930276884, -0.4399290715031914933 ) ) ;
#1822=CARTESIAN_POINT ( 'NONE',  ( 0.5793421593297778394, -1.608008675138359100, -0.4698213068957341476 ) ) ;
#1828=CARTESIAN_POINT ( 'NONE',  ( 0.5616945454376203184, -1.585497279018332373, -0.5227682507658810707 ) ) ;
#1829=FACE_OUTER_BOUND ( 'NONE', #8432, .T. ) ;
#1833=ORIENTED_EDGE ( 'NONE', *, *, #32015, .F. ) ;
#1842=CARTESIAN_POINT ( 'NONE',  ( 0.0006049580205936592146, -1.952245379408770187, -0.3315140204742151320 ) ) ;
#1850=CARTESIAN_POINT ( 'NONE',  ( 0.3699999999999786793, -2.107936428766273185, -0.7005084057759870531 ) ) ;
#1853=CARTESIAN_POINT ( 'NONE',  ( 0.02934857795850940448, -1.577273124788314052, -0.6407384231926183116 ) ) ;
#1856=CARTESIAN_POINT ( 'NONE',  ( -2.112273405726188513E-14, -2.104526171302527171, -0.6992671735679987233 ) ) ;
#1869=ADVANCED_FACE ( 'NONE', ( #4632 ), #17208, .F. ) ;
#1870=CARTESIAN_POINT ( 'NONE',  ( 0.4278413765848551042, -1.120299553241070001, -0.3830631589809550541 ) ) ;
#1871=CARTESIAN_POINT ( 'NONE',  ( 0.4095694756667743186, -1.742820565356182794, -0.5801262846953157970 ) ) ;
#1883=B_SPLINE_CURVE_WITH_KNOTS ( 'NONE', 3,
 ( #33216, #14474, #4211, #24362, #5630, #27650 ),
 .UNSPECIFIED., .F., .F.,
 ( 4, 2, 4 ),
 ( 0.000000000000000000, 0.0001845344150746688959, 0.0003690688301493377918 ),
 .UNSPECIFIED. ) ;
#1903=CARTESIAN_POINT ( 'NONE',  ( -2.119743302583864240E-14, -2.104521498059988449, -0.6992654726654029540 ) ) ;
#1908=FACE_OUTER_BOUND ( 'NONE', #14660, .T. ) ;
#1912=CARTESIAN_POINT ( 'NONE',  ( 0.3445219659096331322, -1.630113034086819290, -0.4330379103484555126 ) ) ;
#1918=CARTESIAN_POINT ( 'NONE',  ( 0.3950057241659845064, -1.613548743562832843, -0.6688636923212416541 ) ) ;
#1922=CARTESIAN_POINT ( 'NONE',  ( 0.3540349203463854511, -1.725807860701394691, -0.5334517722040031940 ) ) ;
#1926=CARTESIAN_POINT ( 'NONE',  ( 0.3853296036239867162, -1.884128910060018702, -0.4867200447654468354 ) ) ;
#1927=ORIENTED_EDGE ( 'NONE', *, *, #27088, .F. ) ;
#1934=CARTESIAN_POINT ( 'NONE',  ( 0.09888984647273572903, -1.356722515137474439, -0.6730291679367702562 ) ) ;
#1954=DIRECTION ( 'NONE',  ( 0.8660512985181134660, 0.4999551463232372317, 0.000000000000000000 ) ) ;
#1955=CARTESIAN_POINT ( 'NONE',  ( 0.3699999999999786793, -2.080203412138651231, -0.4693458302813933170 ) ) ;
#1956=DIRECTION ( 'NONE',  ( 0.8660512985181142431, 0.4999551463232357884, 0.000000000000000000 ) ) ;
#1959=CARTESIAN_POINT ( 'NONE',  ( 0.1816520550910808995, -1.697676133517970420, -0.6833403372426165578 ) ) ;
#1963=CARTESIAN_POINT ( 'NONE',  ( 0.05360578929985907598, -1.598838039970692737, -0.3436840987125299174 ) ) ;
#1972=CYLINDRICAL_SURFACE ( 'NONE', #35085, 0.03000000000000003358 ) ;
#1974=ORIENTED_EDGE ( 'NONE', *, *, #31902, .F. ) ;
#1978=CARTESIAN_POINT ( 'NONE',  ( 0.1799149647795341422, -1.765837058809831106, -0.3253848170194846845 ) ) ;
#1990=CARTESIAN_POINT ( 'NONE',  ( 0.4700898499424847055, -1.130550283242669485, -0.6581804127022372608 ) ) ;
#2010=CARTESIAN_POINT ( 'NONE',  ( 0.5751363246278207164, -1.612441950723962458, -0.5313468545301665014 ) ) ;
#2011=CARTESIAN_POINT ( 'NONE',  ( 0.1456664551191460266, -1.333113330760314907, -0.7163645201341654056 ) ) ;
#2016=CARTESIAN_POINT ( 'NONE',  ( 0.5733332956384830092, -1.543075624777708210, -0.4912759999829157675 ) ) ;
#2025=CIRCLE ( 'NONE', #13833, 0.1033070866141734268 ) ;
#2027=VERTEX_POINT ( 'NONE', #13066 ) ;
#2039=DIRECTION ( 'NONE',  ( 0.8660512985181130219, 0.4999551463232378978, -6.610988856618928922E-16 ) ) ;
#2042=CARTESIAN_POINT ( 'NONE',  ( 0.1250267426322058117, -1.317120597453650621, -0.3493847494023202271 ) ) ;
#2050=AXIS2_PLACEMENT_3D ( 'NONE', #40055, #11879, #5712 ) ;
#2056=CARTESIAN_POINT ( 'NONE',  ( 0.3999999739562093981, -2.086702397455008295, -0.5179432086380986178 ) ) ;
#2060=VERTEX_POINT ( 'NONE', #22151 ) ;
#2061=EDGE_LOOP ( 'NONE', ( #35113, #17797 ) ) ;
#2063=VERTEX_POINT ( 'NONE', #34250 ) ;
#2064=CARTESIAN_POINT ( 'NONE',  ( 0.4139756487772989768, -1.674437384244100713, -0.3990444774096185143 ) ) ;
#2065=VERTEX_POINT ( 'NONE', #37959 ) ;
#2089=CARTESIAN_POINT ( 'NONE',  ( 0.3951517471592372877, -1.686279057714856311, -0.4060406207988965788 ) ) ;
#2091=EDGE_CURVE ( 'NONE', #1239, #34108, #365, .T. ) ;
#2092=CARTESIAN_POINT ( 'NONE',  ( 0.3699999999999797895, -2.107936428766272741, -0.2870436526301863300 ) ) ;
#2104=B_SPLINE_CURVE_WITH_KNOTS ( 'NONE', 3,
 ( #29595, #13952, #30011, #1842, #14358, #11279, #23846, #17652, #14560, #27127, #39657, #39871, #36769, #11691, #30409, #25045, #24245, #40264, #2240, #27533, #27729, #18271, #27342, #15385, #33478, #12097 ),
 .UNSPECIFIED., .F., .F.,
 ( 4, 2, 2, 2, 2, 2, 2, 2, 2, 2, 2, 2, 4 ),
 ( -5.999999999672944161E-08, 0.002879311815431165582, 0.005758683630862327339, 0.008638055446293490397, 0.01151742726172465259, 0.01439679907715581304, 0.01727617089258697697, 0.01871585680030255633, 0.02015554270801813916, 0.02159522861573372199, 0.02231507156959151167, 0.02267499304652039957, 0.02303491452344929094 ),
 .UNSPECIFIED. ) ;
#2111=CARTESIAN_POINT ( 'NONE',  ( 0.02999864137222190211, -2.091146312649429628, -0.7263531585133695678 ) ) ;
#2113=CARTESIAN_POINT ( 'NONE',  ( 0.03333333333331318926, -1.848796465755284668, -0.6381145059054189606 ) ) ;
#2118=CARTESIAN_POINT ( 'NONE',  ( 0.3853411735685215445, -1.756807109041784054, -0.4499573014714178809 ) ) ;
#2123=VERTEX_POINT ( 'NONE', #19245 ) ;
#2125=CARTESIAN_POINT ( 'NONE',  ( 0.08989322008881010795, -1.439897079492934440, -0.6871119803270818727 ) ) ;
#2131=ORIENTED_EDGE ( 'NONE', *, *, #6660, .T. ) ;
#2132=DIRECTION ( 'NONE',  ( 0.4999551463232373427, -0.8660512985181134660, 0.000000000000000000 ) ) ;
#2136=DIRECTION ( 'NONE',  ( -0.4999551463232373427, 0.8660512985181134660, -0.000000000000000000 ) ) ;
#2140=EDGE_LOOP ( 'NONE', ( #29079, #6459, #6924 ) ) ;
#2141=AXIS2_PLACEMENT_3D ( 'NONE', #5354, #17917, #17532 ) ;
#2147=EDGE_CURVE ( 'NONE', #21815, #23348, #6629, .T. ) ;
#2151=CIRCLE ( 'NONE', #27110, 0.1700000000000001232 ) ;
#2154=CARTESIAN_POINT ( 'NONE',  ( 0.1761599653103556595, -1.266290592972142193, -0.7065742620306031396 ) ) ;
#2167=EDGE_CURVE ( 'NONE', #27329, #16906, #31221, .T. ) ;
#2175=CIRCLE ( 'NONE', #13965, 0.01499999999999999598 ) ;
#2179=CARTESIAN_POINT ( 'NONE',  ( 0.1838426283055374921, -1.725872612985020593, -0.3279395879214231924 ) ) ;
#2187=VERTEX_POINT ( 'NONE', #28102 ) ;
#2195=ORIENTED_EDGE ( 'NONE', *, *, #26046, .F. ) ;
#2197=CARTESIAN_POINT ( 'NONE',  ( 0.1993854619498310055, -2.037305861891523850, -0.2781182464799481502 ) ) ;
#2200=CARTESIAN_POINT ( 'NONE',  ( 0.3999999999999787059, -2.143549940236731288, -0.4549916158381476228 ) ) ;
#2203=DIRECTION ( 'NONE',  ( 0.000000000000000000, 0.3268939817722816832, -0.9450610163799283425 ) ) ;
#2206=CARTESIAN_POINT ( 'NONE',  ( 0.3935416462523685932, -1.752073130202900897, -0.5293634714477323255 ) ) ;
#2214=ADVANCED_FACE ( 'NONE', ( #4741 ), #31310, .T. ) ;
#2215=CARTESIAN_POINT ( 'NONE',  ( 0.6468257105432076992, -1.563888897256662469, -0.6077625487223605738 ) ) ;
#2218=CARTESIAN_POINT ( 'NONE',  ( 0.4100456123093286775, -1.725225710419908243, -0.4268450903248972028 ) ) ;
#2221=EDGE_CURVE ( 'NONE', #7743, #33803, #18827, .T. ) ;
#2224=CARTESIAN_POINT ( 'NONE',  ( 0.4034443304043100476, -1.732073763044814196, -0.5980905150073216880 ) ) ;
#2230=CARTESIAN_POINT ( 'NONE',  ( 0.4655516839591847256, -1.068397176280596161, -0.6095936865603254207 ) ) ;
#2240=CARTESIAN_POINT ( 'NONE',  ( 0.1353039243655410340, -1.303414152582186736, -0.3416695301304896737 ) ) ;
#2241=EDGE_LOOP ( 'NONE', ( #31181, #2131, #4288, #7036 ) ) ;
#2248=DIRECTION ( 'NONE',  ( -0.8660512985181132439, -0.4999551463232375093, 0.000000000000000000 ) ) ;
#2269=DIRECTION ( 'NONE',  ( -1.000000000000000000, 0.000000000000000000, 0.000000000000000000 ) ) ;
#2284=ORIENTED_EDGE ( 'NONE', *, *, #12181, .F. ) ;
#2292=CARTESIAN_POINT ( 'NONE',  ( 0.1734973056165642902, -1.209394307038482497, -0.5155029497116575543 ) ) ;
#2298=AXIS2_PLACEMENT_3D ( 'NONE', #13113, #25674, #38209 ) ;
#2299=CARTESIAN_POINT ( 'NONE',  ( 0.2469141422421070875, -1.581573626495411444, -0.3511777555542848206 ) ) ;
#2306=CARTESIAN_POINT ( 'NONE',  ( 0.4002255668615350426, -1.695126185520418938, -0.4229178359567086765 ) ) ;
#2309=CARTESIAN_POINT ( 'NONE',  ( 0.3544525855955990568, -1.628498139902175401, -0.6593841416021928303 ) ) ;
#2310=CARTESIAN_POINT ( 'NONE',  ( 0.3699999999999788458, -2.120743408781763595, -0.4622665795123166999 ) ) ;
#2313=CARTESIAN_POINT ( 'NONE',  ( 0.4634712904840416203, -1.711704060178988129, -0.5155029497116575543 ) ) ;
#2315=CARTESIAN_POINT ( 'NONE',  ( 0.1999999999999789724, -2.166079853131637645, -0.5407606602423824516 ) ) ;
#2324=AXIS2_PLACEMENT_3D ( 'NONE', #39345, #1325, #32964 ) ;
#2339=CARTESIAN_POINT ( 'NONE',  ( 0.4941573835580928553, -1.197472013777949540, -0.4122610257295771796 ) ) ;
#2345=CARTESIAN_POINT ( 'NONE',  ( 0.2211959769661343000, -1.309495541150525799, -0.5931747813493346566 ) ) ;
#2359=CARTESIAN_POINT ( 'NONE',  ( 0.1999999999999789724, -2.183180860297921466, -0.4937760292030871079 ) ) ;
#2366=CARTESIAN_POINT ( 'NONE',  ( 0.3690696315487195789, -2.046121508319152849, -0.6829205282668205923 ) ) ;
#2370=CARTESIAN_POINT ( 'NONE',  ( 0.3759405909208060059, -1.611975652049966179, -0.3607904488862428982 ) ) ;
#2371=DIRECTION ( 'NONE',  ( -0.4999551463232377313, 0.8660512985181132439, -0.000000000000000000 ) ) ;
#2377=EDGE_CURVE ( 'NONE', #31608, #30897, #36602, .T. ) ;
#2382=CARTESIAN_POINT ( 'NONE',  ( 0.1867562162627207645, -1.721001719842840227, -0.3581518700804716127 ) ) ;
#2386=CARTESIAN_POINT ( 'NONE',  ( 0.1909286924077255032, -1.257064795538239022, -0.4400554600884079015 ) ) ;
#2389=ORIENTED_EDGE ( 'NONE', *, *, #40640, .F. ) ;
#2390=EDGE_LOOP ( 'NONE', ( #695, #2455 ) ) ;
#2395=DIRECTION ( 'NONE',  ( -1.000000000000000000, 0.000000000000000000, 0.000000000000000000 ) ) ;
#2397=CARTESIAN_POINT ( 'NONE',  ( 0.3544525855956190963, -1.628498139902242681, -0.6593841416022943047 ) ) ;
#2400=VERTEX_POINT ( 'NONE', #32278 ) ;
#2401=CARTESIAN_POINT ( 'NONE',  ( 0.4905912024403834559, -1.589136493782425719, -0.5753219298350721322 ) ) ;
#2402=ORIENTED_EDGE ( 'NONE', *, *, #8817, .F. ) ;
#2403=CARTESIAN_POINT ( 'NONE',  ( 0.3871031770338608791, -1.873715675035283024, -0.3077635280768467596 ) ) ;
#2417=CARTESIAN_POINT ( 'NONE',  ( 0.6202635901223110260, -1.561719534786903729, -0.5933892023552781447 ) ) ;
#2418=CARTESIAN_POINT ( 'NONE',  ( 0.05257579864948812298, -1.595298430439333393, -0.6695260341086051170 ) ) ;
#2419=CARTESIAN_POINT ( 'NONE',  ( 0.02999999999997891853, -2.097675824466501915, -0.2588528740066096678 ) ) ;
#2423=B_SPLINE_CURVE_WITH_KNOTS ( 'NONE', 3,
 ( #12434, #24601, #6816, #34450, #38507, #905 ),
 .UNSPECIFIED., .F., .F.,
 ( 4, 2, 4 ),
 ( -4.995199405858393678E-06, 0.0003667636180932637305, 0.0007385224355923858657 ),
 .UNSPECIFIED. ) ;
#2428=CARTESIAN_POINT ( 'NONE',  ( 0.4751758298663431024, -1.652426242819088342, -0.6334442537810195395 ) ) ;
#2429=ORIENTED_EDGE ( 'NONE', *, *, #25857, .T. ) ;
#2440=CIRCLE ( 'NONE', #14904, 0.03000000000000000930 ) ;
#2449=FACE_OUTER_BOUND ( 'NONE', #32911, .T. ) ;
#2455=ORIENTED_EDGE ( 'NONE', *, *, #995, .F. ) ;
#2457=CARTESIAN_POINT ( 'NONE',  ( 0.3622253751127874066, -1.756884464425453984, -0.4902987826081479650 ) ) ;
#2460=CARTESIAN_POINT ( 'NONE',  ( 0.5860390410503526493, -1.538367470261696957, -0.4143366047946381858 ) ) ;
#2463=CARTESIAN_POINT ( 'NONE',  ( 0.5053588047760252389, -1.583603243833816565, -0.5401600205605632254 ) ) ;
#2465=EDGE_CURVE ( 'NONE', #21660, #30753, #22663, .T. ) ;
#2472=CARTESIAN_POINT ( 'NONE',  ( 0.5943483229377598542, -1.499644859401920938, -0.6402273302934655685 ) ) ;
#2476=CARTESIAN_POINT ( 'NONE',  ( 0.3918164284306930312, -1.740509091685305876, -0.5895034584783541698 ) ) ;
#2482=EDGE_CURVE ( 'NONE', #23421, #22699, #33673, .T. ) ;
#2493=CARTESIAN_POINT ( 'NONE',  ( 0.1984286359563034452, -1.270056632699685162, -0.7137153576319578141 ) ) ;
#2494=ORIENTED_EDGE ( 'NONE', *, *, #9500, .F. ) ;
#2497=CARTESIAN_POINT ( 'NONE',  ( 0.3853411735687863326, -1.756807109041631509, -0.4499573014711771846 ) ) ;
#2506=CARTESIAN_POINT ( 'NONE',  ( 0.3761284049005145236, -1.714742088754553029, -0.4155147620960898958 ) ) ;
#2509=AXIS2_PLACEMENT_3D ( 'NONE', #16655, #20161, #26527 ) ;
#2510=CARTESIAN_POINT ( 'NONE',  ( 0.4915260346479126685, -1.695508583366576616, -0.4333519947141560857 ) ) ;
#2511=CARTESIAN_POINT ( 'NONE',  ( 0.3699999999999797895, -2.166079853131637645, -0.4467913981637911536 ) ) ;
#2514=CARTESIAN_POINT ( 'NONE',  ( 0.3706793757908091735, -1.615012852715395741, -0.4172838525897034079 ) ) ;
#2540=ORIENTED_EDGE ( 'NONE', *, *, #26985, .F. ) ;
#2551=DIRECTION ( 'NONE',  ( 0.8660512985181134660, 0.4999551463232372317, 0.000000000000000000 ) ) ;
#2555=DIRECTION ( 'NONE',  ( 0.8660512985181131329, 0.4999551463232376758, 0.000000000000000000 ) ) ;
#2576=CARTESIAN_POINT ( 'NONE',  ( 0.3569675822956203115, -1.858790014656386491, -0.3401391051804745769 ) ) ;
#2589=CARTESIAN_POINT ( 'NONE',  ( 0.1996772853583087814, -2.073393704582455310, -0.6889727466378606779 ) ) ;
#2591=CARTESIAN_POINT ( 'NONE',  ( 0.4622815974667671690, -1.593090396639457396, -0.6012589109344715910 ) ) ;
#2592=CARTESIAN_POINT ( 'NONE',  ( 0.3873602817592721181, -1.882673143022665752, -0.5129299851078027439 ) ) ;
#2595=CARTESIAN_POINT ( 'NONE',  ( 0.3999999999999787059, -2.097675824466503691, -0.4688691127277797022 ) ) ;
#2602=EDGE_CURVE ( 'NONE', #7643, #23563, #29217, .T. ) ;
#2607=EDGE_CURVE ( 'NONE', #25087, #617, #23867, .T. ) ;
#2609=CARTESIAN_POINT ( 'NONE',  ( 0.6479666109875431568, -1.454022938183795022, -0.4116638256851784528 ) ) ;
#2612=ADVANCED_FACE ( 'NONE', ( #18284 ), #1173, .F. ) ;
#2615=ORIENTED_EDGE ( 'NONE', *, *, #6363, .T. ) ;
#2616=CARTESIAN_POINT ( 'NONE',  ( 0.3593346688482155771, -1.735925422213635771, -0.5010936962835149666 ) ) ;
#2617=CARTESIAN_POINT ( 'NONE',  ( 0.3920818884216891176, -1.687900591995562083, -0.6232001118445732457 ) ) ;
#2618=B_SPLINE_CURVE_WITH_KNOTS ( 'NONE', 3,
 ( #29133, #7726, #13884, #23590, #26260, #32625, #26072, #26459, #7913, #16993 ),
 .UNSPECIFIED., .F., .F.,
 ( 4, 2, 2, 2, 4 ),
 ( 0.000000000000000000, 0.001019199890480618860, 0.002038399780961237719, 0.003057599671441856362, 0.004076799561922475439 ),
 .UNSPECIFIED. ) ;
#2619=CARTESIAN_POINT ( 'NONE',  ( 0.4149016700121535006, -1.651544695139253172, -0.6216189332894249686 ) ) ;
#2622=CARTESIAN_POINT ( 'NONE',  ( 0.4957703318102697487, -1.693058430341604081, -0.5958887926595133333 ) ) ;
#2647=CARTESIAN_POINT ( 'NONE',  ( 0.2189962940802840652, -1.687333423092645779, -0.3582481089917773365 ) ) ;
#2650=CARTESIAN_POINT ( 'NONE',  ( 0.5970072641691556159, -1.484358014203126297, -0.4176640727536428677 ) ) ;
#2652=EDGE_CURVE ( 'NONE', #19627, #30237, #31718, .T. ) ;
#2655=CARTESIAN_POINT ( 'NONE',  ( 0.09667290451365230519, -1.302890901820756620, -0.6687017097452528924 ) ) ;
#2662=DIRECTION ( 'NONE',  ( 0.8660512985181134660, 0.4999551463232372317, 0.000000000000000000 ) ) ;
#2667=CARTESIAN_POINT ( 'NONE',  ( 0.1943613428509314289, -1.255083190917881675, -0.3178470422210406543 ) ) ;
#2668=ORIENTED_EDGE ( 'NONE', *, *, #15423, .F. ) ;
#2677=CARTESIAN_POINT ( 'NONE',  ( 0.2059273467974228333, -1.283046334493783025, -0.7462941026102624109 ) ) ;
#2678=ORIENTED_EDGE ( 'NONE', *, *, #17977, .T. ) ;
#2683=CARTESIAN_POINT ( 'NONE',  ( 0.4962914637724937794, -1.692757590648997557, -0.4193976862638447711 ) ) ;
#2699=ADVANCED_FACE ( 'NONE', ( #10246 ), #619, .T. ) ;
#2700=CIRCLE ( 'NONE', #33545, 0.1033070866141734129 ) ;
#2705=AXIS2_PLACEMENT_3D ( 'NONE', #33179, #7856, #26815 ) ;
#2716=CARTESIAN_POINT ( 'NONE',  ( 0.3447589852832846913, -1.668942397003103650, -0.4516098998207526694 ) ) ;
#2718=CARTESIAN_POINT ( 'NONE',  ( 0.1999999999999789724, -2.183180860297921466, -0.2437760292030870524 ) ) ;
#2720=EDGE_CURVE ( 'NONE', #13521, #23751, #10803, .T. ) ;
#2731=DIRECTION ( 'NONE',  ( 0.000000000000000000, 0.000000000000000000, -1.000000000000000000 ) ) ;
#2748=SHAPE_REPRESENTATION_RELATIONSHIP ( 'NONE' , 'NONE' ,  #8026, #11298 ) ;
#2760=CARTESIAN_POINT ( 'NONE',  ( 0.1734973056165642902, -1.209394307038482497, -0.5155029497116575543 ) ) ;
#2766=DIRECTION ( 'NONE',  ( 1.000000000000000000, 0.000000000000000000, 0.000000000000000000 ) ) ;
#2778=CARTESIAN_POINT ( 'NONE',  ( 0.3583460058031623929, -1.906970946538292910, -0.5088717446659136723 ) ) ;
#2782=CARTESIAN_POINT ( 'NONE',  ( 0.2211959769661342168, -1.309495541150525799, -0.2869361388274796476 ) ) ;
#2787=AXIS2_PLACEMENT_3D ( 'NONE', #37656, #37254, #15455 ) ;
#2794=CARTESIAN_POINT ( 'NONE',  ( 0.1575440928747191827, -1.280321311252621497, -0.3327596545001944017 ) ) ;
#2797=CARTESIAN_POINT ( 'NONE',  ( 0.3977485604613671955, -1.756321122263676093, -0.3111787470529240873 ) ) ;
#2814=CARTESIAN_POINT ( 'NONE',  ( 0.3699999999999786793, -2.166079853131637645, -0.4467913981637915422 ) ) ;
#2818=CARTESIAN_POINT ( 'NONE',  ( 0.5843377990077387452, -1.469343909573061158, -0.6034783832058462361 ) ) ;
#2819=CIRCLE ( 'NONE', #32347, 0.1033070866141734129 ) ;
#2823=CARTESIAN_POINT ( 'NONE',  ( 0.5335660117596170426, -1.671239694278476628, -0.5770658812888499467 ) ) ;
#2825=CARTESIAN_POINT ( 'NONE',  ( 0.7059656540691128246, -1.571716619208481935, -0.5155029497116575543 ) ) ;
#2829=CARTESIAN_POINT ( 'NONE',  ( -2.112273405726188513E-14, -2.097675824466503691, -0.4937760292030871079 ) ) ;
#2841=TOROIDAL_SURFACE ( 'NONE', #31126, 0.05330708661417323663, 0.01000000000000000021 ) ;
#2847=ORIENTED_EDGE ( 'NONE', *, *, #15014, .F. ) ;
#2852=CARTESIAN_POINT ( 'NONE',  ( 0.5774070013789848188, -1.563126340145571058, -0.4407173397374128387 ) ) ;
#2875=AXIS2_PLACEMENT_3D ( 'NONE', #36764, #15380, #27528 ) ;
#2879=CARTESIAN_POINT ( 'NONE',  ( 0.3999999999999787059, -2.183180860297921466, -0.4937760292030871079 ) ) ;
#2884=ORIENTED_EDGE ( 'NONE', *, *, #2720, .F. ) ;
#2892=CARTESIAN_POINT ( 'NONE',  ( 0.1999999999999789724, -2.097675824466503247, -0.7286991843995637153 ) ) ;
#2894=EDGE_CURVE ( 'NONE', #19872, #37556, #29243, .T. ) ;
#2897=VERTEX_POINT ( 'NONE', #8359 ) ;
#2899=CARTESIAN_POINT ( 'NONE',  ( 0.4675740435013452934, -1.069464823588083036, -0.4221806871052409815 ) ) ;
#2904=CARTESIAN_POINT ( 'NONE',  ( 0.5389700097005715174, -1.668120067778418258, -0.4887748460763289837 ) ) ;
#2911=ADVANCED_FACE ( 'NONE', ( #30974 ), #8826, .T. ) ;
#2922=CARTESIAN_POINT ( 'NONE',  ( 0.2134937173224229212, -1.278678410919930730, -0.5155029497116575543 ) ) ;
#2934=ORIENTED_EDGE ( 'NONE', *, *, #31085, .F. ) ;
#2939=CARTESIAN_POINT ( 'NONE',  ( 0.3530204145741916433, -1.722873630718287252, -0.5364141961698728478 ) ) ;
#2957=CARTESIAN_POINT ( 'NONE',  ( 0.7384722612031221489, -1.541404505398278779, -0.5155029497116575543 ) ) ;
#2961=DIRECTION ( 'NONE',  ( 0.000000000000000000, 0.000000000000000000, 1.000000000000000000 ) ) ;
#2971=DIRECTION ( 'NONE',  ( 0.4999551463232373427, -0.8660512985181134660, 0.000000000000000000 ) ) ;
#2978=CARTESIAN_POINT ( 'NONE',  ( -2.112273405726188513E-14, -2.183180860297921466, -0.4937760292030871079 ) ) ;
#2983=VERTEX_POINT ( 'NONE', #35469 ) ;
#2986=ORIENTED_EDGE ( 'NONE', *, *, #10133, .T. ) ;
#2988=CARTESIAN_POINT ( 'NONE',  ( 0.1992056882179587540, -2.039857513870245054, -0.3085428006972014692 ) ) ;
#2993=CARTESIAN_POINT ( 'NONE',  ( 0.2211959769661343000, -1.309495541150525799, -0.5931747813493346566 ) ) ;
#2995=ORIENTED_EDGE ( 'NONE', *, *, #14478, .T. ) ;
#3004=CARTESIAN_POINT ( 'NONE',  ( 0.2923286432308245808, -1.660243258845594649, -0.3694143330441917450 ) ) ;
#3005=CARTESIAN_POINT ( 'NONE',  ( 0.1321224643482970806, -1.307861179043269040, -0.3150116852443416438 ) ) ;
#3009=CARTESIAN_POINT ( 'NONE',  ( 0.1817222246005483210, -1.860686054201275086, -0.3146317322992087662 ) ) ;
#3014=B_SPLINE_CURVE_WITH_KNOTS ( 'NONE', 3,
 ( #27698, #14947, #40230, #18236 ),
 .UNSPECIFIED., .F., .F.,
 ( 4, 4 ),
 ( 0.02321896957645076462, 0.02481944680398503328 ),
 .UNSPECIFIED. ) ;
#3025=CARTESIAN_POINT ( 'NONE',  ( 0.6331866186374228711, -1.597140103118768195, -0.4450843881964172688 ) ) ;
#3027=DIRECTION ( 'NONE',  ( 0.4999551463232372317, -0.8660512985181133550, 0.000000000000000000 ) ) ;
#3030=DIRECTION ( 'NONE',  ( 0.4999551463232377313, -0.8660512985181132439, -0.000000000000000000 ) ) ;
#3036=CARTESIAN_POINT ( 'NONE',  ( 0.5249748772169798849, -1.642917355740116214, -0.4600979152061163702 ) ) ;
#3049=ORIENTED_EDGE ( 'NONE', *, *, #37564, .T. ) ;
#3059=ORIENTED_EDGE ( 'NONE', *, *, #24977, .T. ) ;
#3060=ORIENTED_EDGE ( 'NONE', *, *, #30864, .F. ) ;
#3065=CARTESIAN_POINT ( 'NONE',  ( 0.1360281309732884192, -1.916305331242646570, -0.3368804578019788387 ) ) ;
#3069=CARTESIAN_POINT ( 'NONE',  ( 0.3666666666666451579, -1.960071684622068489, -0.3089366850217884486 ) ) ;
#3071=LINE ( 'NONE', #6340, #38373 ) ;
#3082=CARTESIAN_POINT ( 'NONE',  ( 0.1898786726785968715, -1.668530212669821600, -0.6859658009302209702 ) ) ;
#3083=AXIS2_PLACEMENT_3D ( 'NONE', #2922, #25134, #15475 ) ;
#3088=EDGE_LOOP ( 'NONE', ( #20961, #19214, #19599, #24152 ) ) ;
#3098=FACE_OUTER_BOUND ( 'NONE', #36640, .T. ) ;
#3099=DIRECTION ( 'NONE',  ( -0.4999551463232372317, 0.8660512985181135770, -0.000000000000000000 ) ) ;
#3103=ORIENTED_EDGE ( 'NONE', *, *, #16045, .F. ) ;
#3105=CYLINDRICAL_SURFACE ( 'NONE', #10937, 0.04330708661417322775 ) ;
#3123=EDGE_CURVE ( 'NONE', #5600, #23137, #20065, .T. ) ;
#3134=DIRECTION ( 'NONE',  ( 1.000000000000000000, 0.000000000000000000, 0.000000000000000000 ) ) ;
#3140=DIRECTION ( 'NONE',  ( 0.4999551463232372317, -0.8660512985181135770, 0.000000000000000000 ) ) ;
#3145=CARTESIAN_POINT ( 'NONE',  ( 0.1999999999999789724, -2.183180860297921466, -0.4937760292030871079 ) ) ;
#3146=EDGE_LOOP ( 'NONE', ( #38694, #6423, #4424, #19178 ) ) ;
#3150=CARTESIAN_POINT ( 'NONE',  ( 0.6430590169175627313, -1.417851464528291139, -0.6270229543717609211 ) ) ;
#3152=CARTESIAN_POINT ( 'NONE',  ( 0.1759300380180282841, -1.231083256582695906, -0.6184399470714002645 ) ) ;
#3155=CARTESIAN_POINT ( 'NONE',  ( 0.4121964764379724144, -1.591045810388358905, -0.3442890830420804460 ) ) ;
#3161=EDGE_CURVE ( 'NONE', #3269, #8639, #34493, .T. ) ;
#3182=CARTESIAN_POINT ( 'NONE',  ( 0.1804425756904262101, -1.792597923215050182, -0.3531089307126511478 ) ) ;
#3186=ORIENTED_EDGE ( 'NONE', *, *, #37813, .F. ) ;
#3189=ORIENTED_EDGE ( 'NONE', *, *, #28075, .F. ) ;
#3192=CARTESIAN_POINT ( 'NONE',  ( 0.5194227709487030387, -1.611319201048296623, -0.4830683290006882458 ) ) ;
#3194=DIRECTION ( 'NONE',  ( -0.4999551463232372317, 0.8660512985181134660, -0.000000000000000000 ) ) ;
#3197=CARTESIAN_POINT ( 'NONE',  ( 0.4008157502961269270, -1.730613119872131733, -0.3050311287808085692 ) ) ;
#3202=CARTESIAN_POINT ( 'NONE',  ( 0.3340217598881563554, -1.134046545150164009, -0.5155029497116575543 ) ) ;
#3203=DIRECTION ( 'NONE',  ( 0.8660512985181133550, 0.4999551463232372317, 0.000000000000000000 ) ) ;
#3208=CARTESIAN_POINT ( 'NONE',  ( 0.6264012344811226152, -1.546116565118341057, -0.4272351601427545331 ) ) ;
#3212=CARTESIAN_POINT ( 'NONE',  ( 0.6409058204046232943, -1.459016202299332710, -0.5155029497116575543 ) ) ;
#3213=ORIENTED_EDGE ( 'NONE', *, *, #3465, .F. ) ;
#3214=CARTESIAN_POINT ( 'NONE',  ( 0.3622253751127866850, -1.756884464425456205, -0.4902987826081466327 ) ) ;
#3216=CARTESIAN_POINT ( 'NONE',  ( 0.3660688374457184424, -2.015896937187397597, -0.4887634650597760255 ) ) ;
#3218=CARTESIAN_POINT ( 'NONE',  ( 0.3699999999999786793, -2.166079853131637645, -0.5407606602423824516 ) ) ;
#3222=DIRECTION ( 'NONE',  ( -0.4999551463232377313, 0.8660512985181132439, -0.000000000000000000 ) ) ;
#3227=CARTESIAN_POINT ( 'NONE',  ( 0.5455881031540378290, -1.595019605959082654, -0.5473203437262895710 ) ) ;
#3235=ORIENTED_EDGE ( 'NONE', *, *, #27838, .F. ) ;
#3243=ORIENTED_EDGE ( 'NONE', *, *, #3123, .F. ) ;
#3244=ORIENTED_EDGE ( 'NONE', *, *, #25035, .T. ) ;
#3245=FACE_OUTER_BOUND ( 'NONE', #18679, .T. ) ;
#3251=CARTESIAN_POINT ( 'NONE',  ( 0.5616682974235900350, -1.585511599874633193, -0.5166151207188732775 ) ) ;
#3257=CARTESIAN_POINT ( 'NONE',  ( 0.2414668910093290266, -2.060278424428106270, -0.6831623107723641120 ) ) ;
#3260=ADVANCED_FACE ( 'NONE', ( #36499 ), #14685, .T. ) ;
#3264=FACE_BOUND ( 'NONE', #22642, .T. ) ;
#3269=VERTEX_POINT ( 'NONE', #33405 ) ;
#3272=ORIENTED_EDGE ( 'NONE', *, *, #10704, .F. ) ;
#3284=DIRECTION ( 'NONE',  ( 1.000000000000000000, 0.000000000000000000, 0.000000000000000000 ) ) ;
#3287=DIRECTION ( 'NONE',  ( 0.000000000000000000, 0.000000000000000000, -1.000000000000000000 ) ) ;
#3297=CARTESIAN_POINT ( 'NONE',  ( 0.4469283285619459201, -1.099869350908816878, -0.4033480720695140631 ) ) ;
#3307=CIRCLE ( 'NONE', #3977, 0.01499999999999999424 ) ;
#3312=CARTESIAN_POINT ( 'NONE',  ( 0.4694390894638814093, -1.155687545037050956, -0.4112888527604742772 ) ) ;
#3320=VERTEX_POINT ( 'NONE', #9111 ) ;
#3321=CARTESIAN_POINT ( 'NONE',  ( 0.3322271507484021447, -1.669294652568602988, -0.6327274659999716500 ) ) ;
#3324=AXIS2_PLACEMENT_3D ( 'NONE', #11987, #21473, #2731 ) ;
#3325=DIRECTION ( 'NONE',  ( -0.4999551463232372872, 0.8660512985181134660, 0.000000000000000000 ) ) ;
#3335=AXIS2_PLACEMENT_3D ( 'NONE', #11867, #5275, #11482 ) ;
#3338=EDGE_CURVE ( 'NONE', #19341, #545, #19844, .T. ) ;
#3354=AXIS2_PLACEMENT_3D ( 'NONE', #9615, #10231, #22801 ) ;
#3363=AXIS2_PLACEMENT_3D ( 'NONE', #8148, #7749, #39015 ) ;
#3373=CARTESIAN_POINT ( 'NONE',  ( 0.3826493285555479518, -1.694417038293525524, -0.3356002933695534374 ) ) ;
#3377=ORIENTED_EDGE ( 'NONE', *, *, #35859, .T. ) ;
#3380=ORIENTED_EDGE ( 'NONE', *, *, #7469, .T. ) ;
#3384=ORIENTED_EDGE ( 'NONE', *, *, #4625, .T. ) ;
#3386=FACE_BOUND ( 'NONE', #25931, .T. ) ;
#3389=CARTESIAN_POINT ( 'NONE',  ( 0.3031470318619229887, -1.653998006306516055, -0.3710263027724181040 ) ) ;
#3393=ADVANCED_FACE ( 'NONE', ( #5405 ), #25324, .F. ) ;
#3409=CARTESIAN_POINT ( 'NONE',  ( 0.6126544994249021325, -1.576059959616806561, -0.4529311371484831539 ) ) ;
#3411=CARTESIAN_POINT ( 'NONE',  ( 0.3984114568195522010, -1.599003643269838904, -0.5155029497116575543 ) ) ;
#3413=CARTESIAN_POINT ( 'NONE',  ( 0.7749447939048204059, -1.514576267321142256, -0.5155029497116575543 ) ) ;
#3417=CARTESIAN_POINT ( 'NONE',  ( 0.1999999999999794720, -2.097675824466503247, -0.2588528740066096678 ) ) ;
#3419=DIRECTION ( 'NONE',  ( 0.8660512985181136880, 0.4999551463232369541, 0.000000000000000000 ) ) ;
#3423=CARTESIAN_POINT ( 'NONE',  ( 0.5445533481859567981, -1.664896911350843389, -0.5554955765310773952 ) ) ;
#3438=EDGE_CURVE ( 'NONE', #39658, #5888, #18802, .T. ) ;
#3440=DIRECTION ( 'NONE',  ( 0.8660512985181136880, 0.4999551463232368431, 0.000000000000000000 ) ) ;
#3445=EDGE_LOOP ( 'NONE', ( #3186, #24154, #21307, #36770 ) ) ;
#3451=CARTESIAN_POINT ( 'NONE',  ( 0.3901895921616377327, -1.764522914000479670, -0.5281946013978575660 ) ) ;
#3452=CARTESIAN_POINT ( 'NONE',  ( 0.06943685245347047674, -1.818941598116789793, -0.3556487151594290297 ) ) ;
#3454=FACE_OUTER_BOUND ( 'NONE', #19720, .T. ) ;
#3455=ORIENTED_EDGE ( 'NONE', *, *, #3338, .F. ) ;
#3462=CARTESIAN_POINT ( 'NONE',  ( 0.3989074838267503975, -2.038165485489161988, -0.7120309709640824103 ) ) ;
#3463=CIRCLE ( 'NONE', #26458, 0.03000000000000003011 ) ;
#3465=EDGE_CURVE ( 'NONE', #39975, #28758, #19391, .T. ) ;
#3466=DIRECTION ( 'NONE',  ( 0.7432428574091918261, 0.4290601401620685040, 0.5133200278913008230 ) ) ;
#3470=VECTOR ( 'NONE', #28984, 39.37007874015748854 ) ;
#3477=CARTESIAN_POINT ( 'NONE',  ( 0.5935452302802395330, -1.483994409378550206, -0.3858431232416580370 ) ) ;
#3479=ORIENTED_EDGE ( 'NONE', *, *, #14836, .T. ) ;
#3481=( BOUNDED_SURFACE ( )  B_SPLINE_SURFACE ( 3, 2, ( 
 ( #5182, #8481, #11777 ),
 ( #39348, #39757, #39537 ),
 ( #11169, #17736, #1926 ),
 ( #21042, #33379, #5382 ),
 ( #23725, #4987, #10984 ),
 ( #33567, #14442, #23543 ),
 ( #36253, #39157, #8286 ),
 ( #27010, #24334, #20856 ) ),
 .UNSPECIFIED., .F., .F., .T. ) 
 B_SPLINE_SURFACE_WITH_KNOTS ( ( 4, 2, 2, 4 ),
 ( 3, 3 ),
 ( -1.735946658636840947E-05, 0.003182886954856570336, 0.004783010165578039860, 0.006383133376299508950 ),
 ( 0.000000000000000000, 1.000000000000000000 ),
 .UNSPECIFIED. ) 
 GEOMETRIC_REPRESENTATION_ITEM ( )  RATIONAL_B_SPLINE_SURFACE ( (
 ( 1.000000000000000000, 1.000000000000000000, 1.000000000000000000),
 ( 1.000000000000000000, 0.9999683261267254819, 1.000000000000000000),
 ( 1.000000000000000000, 0.9925635664889210785, 1.000000000000000000),
 ( 1.000000000000000000, 0.9822629114585049726, 1.000000000000000000),
 ( 1.000000000000000000, 0.9789426092108594046, 1.000000000000000000),
 ( 1.000000000000000000, 0.9749055716457132315, 1.000000000000000000),
 ( 1.000000000000000000, 0.9741944405893343539, 1.000000000000000000),
 ( 1.000000000000000000, 0.9760960752155037889, 1.000000000000000000) ) ) 
 REPRESENTATION_ITEM ( '' )  SURFACE ( )  );
#3484=DIRECTION ( 'NONE',  ( 0.000000000000000000, -1.000000000000000000, 0.000000000000000000 ) ) ;
#3488=VERTEX_POINT ( 'NONE', #31352 ) ;
#3496=FACE_OUTER_BOUND ( 'NONE', #9241, .T. ) ;
#3503=ORIENTED_EDGE ( 'NONE', *, *, #6468, .T. ) ;
#3504=EDGE_CURVE ( 'NONE', #26250, #24229, #10192, .T. ) ;
#3505=CYLINDRICAL_SURFACE ( 'NONE', #11265, 0.1033070866141732880 ) ;
#3521=CARTESIAN_POINT ( 'NONE',  ( 0.2138705976722455049, -1.623983589469084832, -0.6628954696135268554 ) ) ;
#3525=CARTESIAN_POINT ( 'NONE',  ( 0.3867682591249857471, -1.703546894211353413, -0.4950309488039767447 ) ) ;
#3530=ORIENTED_EDGE ( 'NONE', *, *, #38868, .F. ) ;
#3534=CARTESIAN_POINT ( 'NONE',  ( 0.5114276962200751120, -1.674740791407443918, -0.4312833531603950665 ) ) ;
#3540=CARTESIAN_POINT ( 'NONE',  ( 0.6442087495854491586, -1.607367720096421815, -0.5688382314396814854 ) ) ;
#3542=AXIS2_PLACEMENT_3D ( 'NONE', #16995, #19282, #35107 ) ;
#3547=CARTESIAN_POINT ( 'NONE',  ( 0.3622253751127874066, -1.756884464425453984, -0.4902987826081479650 ) ) ;
#3550=CARTESIAN_POINT ( 'NONE',  ( 0.3999999999999787059, -2.183180860297921466, -0.4937760292030871079 ) ) ;
#3552=ORIENTED_EDGE ( 'NONE', *, *, #11100, .T. ) ;
#3555=B_SPLINE_CURVE_WITH_KNOTS ( 'NONE', 3,
 ( #37452, #19159, #9269, #31492, #15860, #281, #31698, #16079, #28622, #12990, #491, #29009 ),
 .UNSPECIFIED., .F., .F.,
 ( 4, 2, 2, 2, 2, 4 ),
 ( 0.0001995102558408363557, 0.0007825151425067985826, 0.001365520029172760837, 0.001948524915838722874, 0.002240027359171694026, 0.002531529802504664962 ),
 .UNSPECIFIED. ) ;
#3557=CARTESIAN_POINT ( 'NONE',  ( 0.4262438152663739488, -1.592651821845863624, -0.6151431148613255573 ) ) ;
#3563=CARTESIAN_POINT ( 'NONE',  ( 0.4357360948072305229, -1.114964732312023532, -0.3896066595063904514 ) ) ;
#3573=ORIENTED_EDGE ( 'NONE', *, *, #19114, .F. ) ;
#3578=VERTEX_POINT ( 'NONE', #2957 ) ;
#3583=VERTEX_POINT ( 'NONE', #38304 ) ;
#3589=CARTESIAN_POINT ( 'NONE',  ( 0.4219866632171650478, -1.610104465087853765, -0.3647299066799348233 ) ) ;
#3600=CARTESIAN_POINT ( 'NONE',  ( 0.4958944217707210722, -1.624354045237602184, -0.4405887224042038808 ) ) ;
#3602=CARTESIAN_POINT ( 'NONE',  ( 0.3356530659809335848, -1.635232883418107797, -0.3718853885041787932 ) ) ;
#3605=CIRCLE ( 'NONE', #39745, 0.01000000000000002970 ) ;
#3607=CARTESIAN_POINT ( 'NONE',  ( 0.4195799131931469139, -1.708669366397955081, -0.5215014756514103622 ) ) ;
#3629=ADVANCED_FACE ( 'NONE', ( #22298 ), #33163, .F. ) ;
#3630=DIRECTION ( 'NONE',  ( -0.4999551463232372317, 0.8660512985181135770, -0.000000000000000000 ) ) ;
#3641=CARTESIAN_POINT ( 'NONE',  ( 0.1809287994913510722, -1.262837545876212886, -0.7414037396183944528 ) ) ;
#3649=ORIENTED_EDGE ( 'NONE', *, *, #16732, .T. ) ;
#3656=ORIENTED_EDGE ( 'NONE', *, *, #16842, .T. ) ;
#3661=CARTESIAN_POINT ( 'NONE',  ( 0.5221712590809916010, -1.637363247671663746, -0.4217897737303722971 ) ) ;
#3663=CARTESIAN_POINT ( 'NONE',  ( 0.5967683701461131696, -1.379674245310775760, -0.6250000000000000000 ) ) ;
#3665=CARTESIAN_POINT ( 'NONE',  ( 0.1909286924077255587, -1.257064795538239022, -0.6485234391946320676 ) ) ;
#3668=AXIS2_PLACEMENT_3D ( 'NONE', #2359, #24360, #37105 ) ;
#3672=CARTESIAN_POINT ( 'NONE',  ( 0.3972310942533077704, -2.031578862939333430, -0.5076924364714133775 ) ) ;
#3676=FACE_OUTER_BOUND ( 'NONE', #17737, .T. ) ;
#3679=AXIS2_PLACEMENT_3D ( 'NONE', #16780, #35087, #26237 ) ;
#3687=CARTESIAN_POINT ( 'NONE',  ( 0.2059254672957554211, -1.283047419494637520, -0.2869370717035634177 ) ) ;
#3691=CARTESIAN_POINT ( 'NONE',  ( 0.3795613398208534384, -1.760143698493221720, -0.5723197561600635863 ) ) ;
#3694=CARTESIAN_POINT ( 'NONE',  ( 0.5751110296356755081, -1.612475604602671808, -0.4967019341012566258 ) ) ;
#3703=ADVANCED_FACE ( 'NONE', ( #1908 ), #9232, .F. ) ;
#3705=FACE_OUTER_BOUND ( 'NONE', #10575, .T. ) ;
#3709=CARTESIAN_POINT ( 'NONE',  ( 0.09582489096432343645, -1.363102397044379632, -0.3305558606734421701 ) ) ;
#3713=CARTESIAN_POINT ( 'NONE',  ( 0.3885328309914510281, -1.773491243725594746, -0.4828692758189210843 ) ) ;
#3730=CARTESIAN_POINT ( 'NONE',  ( 0.1950600887472297151, -2.009716898148788733, -0.6737934748930497486 ) ) ;
#3734=CARTESIAN_POINT ( 'NONE',  ( 0.3567436193415031154, -1.868336587247005021, -0.6649533621369776437 ) ) ;
#3740=VERTEX_POINT ( 'NONE', #2510 ) ;
#3762=CARTESIAN_POINT ( 'NONE',  ( 0.6353491900406211812, -1.612482177399554351, -0.4775148253361261030 ) ) ;
#3784=DIRECTION ( 'NONE',  ( 0.000000000000000000, 0.000000000000000000, -1.000000000000000000 ) ) ;
#3790=DIRECTION ( 'NONE',  ( -0.4999551463232372317, 0.8660512985181135770, -0.000000000000000000 ) ) ;
#3791=CARTESIAN_POINT ( 'NONE',  ( 0.2369676045672858555, -1.593428264216547596, -0.3535318458821304355 ) ) ;
#3799=CARTESIAN_POINT ( 'NONE',  ( 0.4852701934511425286, -1.589624916429106971, -0.4498566476972361006 ) ) ;
#3804=CARTESIAN_POINT ( 'NONE',  ( 0.6630839938131345423, -1.446213159395746128, -0.6155857397476032222 ) ) ;
#3805=CARTESIAN_POINT ( 'NONE',  ( 0.4147044437876460932, -1.715472123057989684, -0.5245963139501007566 ) ) ;
#3820=CARTESIAN_POINT ( 'NONE',  ( 0.4243666725459964151, -1.591076223527387423, -0.4156371400837810537 ) ) ;
#3827=CARTESIAN_POINT ( 'NONE',  ( 0.1333333333333120430, -2.107936428766273629, -0.7005084057759864979 ) ) ;
#3839=ORIENTED_EDGE ( 'NONE', *, *, #13267, .F. ) ;
#3841=ORIENTED_EDGE ( 'NONE', *, *, #38081, .F. ) ;
#3846=CARTESIAN_POINT ( 'NONE',  ( 0.3926032618789407347, -1.756026311479913948, -0.5284552501753293496 ) ) ;
#3849=CARTESIAN_POINT ( 'NONE',  ( 0.6089166525218913106, -1.414157958342789234, -0.6250000000000001110 ) ) ;
#3855=CARTESIAN_POINT ( 'NONE',  ( 0.2117601568378603694, -1.293150266309827101, -0.2869361388274795921 ) ) ;
#3856=CARTESIAN_POINT ( 'NONE',  ( 0.3885621086388810763, -1.758569517285561767, -0.5425237269221726555 ) ) ;
#3857=ADVANCED_FACE ( 'NONE', ( #28766 ), #13460, .F. ) ;
#3858=DIRECTION ( 'NONE',  ( 0.8660512985181132439, 0.4999551463232376758, 0.000000000000000000 ) ) ;
#3868=EDGE_CURVE ( 'NONE', #25706, #19455, #27960, .T. ) ;
#3872=CARTESIAN_POINT ( 'NONE',  ( -2.134462193483032131E-14, -2.087756091470926112, -0.2623975632731759267 ) ) ;
#3875=ORIENTED_EDGE ( 'NONE', *, *, #8921, .F. ) ;
#3876=ORIENTED_EDGE ( 'NONE', *, *, #5114, .F. ) ;
#3880=DIRECTION ( 'NONE',  ( -0.8660512985181132439, -0.4999551463232375648, 0.000000000000000000 ) ) ;
#3888=EDGE_LOOP ( 'NONE', ( #39830, #32213, #34349, #27878 ) ) ;
#3894=CARTESIAN_POINT ( 'NONE',  ( 0.04964375069992935791, -1.483475046233223571, -0.3718814836353687703 ) ) ;
#3901=CARTESIAN_POINT ( 'NONE',  ( -2.112273405726188513E-14, -2.107936428766274073, -0.2870436526301869962 ) ) ;
#3909=DIRECTION ( 'NONE',  ( 0.8660512985181135770, 0.4999551463232372317, 0.000000000000000000 ) ) ;
#3914=CARTESIAN_POINT ( 'NONE',  ( 0.1988232060422361613, -2.043630805496089220, -0.6812398176055290966 ) ) ;
#3917=CARTESIAN_POINT ( 'NONE',  ( 0.2571002409661083954, -1.568717443816634693, -0.6786148624936777507 ) ) ;
#3926=ORIENTED_EDGE ( 'NONE', *, *, #14495, .F. ) ;
#3927=ORIENTED_EDGE ( 'NONE', *, *, #16488, .T. ) ;
#3936=EDGE_LOOP ( 'NONE', ( #6314, #18562, #36072, #36695, #22075, #6715, #6407 ) ) ;
#3942=CARTESIAN_POINT ( 'NONE',  ( 0.6441828724856649702, -1.607382658460039471, -0.5688074945424951290 ) ) ;
#3946=CIRCLE ( 'NONE', #32192, 0.05330708661417321581 ) ;
#3948=CARTESIAN_POINT ( 'NONE',  ( 0.3475958263379387292, -1.626714668491045401, -0.3321210449665553122 ) ) ;
#3955=CARTESIAN_POINT ( 'NONE',  ( 0.6620678144876760429, -1.446799780631947252, -0.4151272395384200675 ) ) ;
#3969=AXIS2_PLACEMENT_3D ( 'NONE', #22525, #6862, #31974 ) ;
#3977=AXIS2_PLACEMENT_3D ( 'NONE', #26958, #8622, #39911 ) ;
#3979=CARTESIAN_POINT ( 'NONE',  ( 0.3560871317620682985, -1.891711383486874620, -0.4908775415153238120 ) ) ;
#3981=CIRCLE ( 'NONE', #25018, 0.03000000000000002318 ) ;
#3982=DIRECTION ( 'NONE',  ( 0.8660512985181134660, 0.4999551463232372317, 0.000000000000000000 ) ) ;
#3988=CARTESIAN_POINT ( 'NONE',  ( 0.4912428832138920343, -1.588451637922100312, -0.4575737628907398657 ) ) ;
#3995=CARTESIAN_POINT ( 'NONE',  ( 0.2751874179112033247, -1.553387066878797240, -0.3124965672173706244 ) ) ;
#4005=AXIS2_PLACEMENT_3D ( 'NONE', #403, #12901, #9797 ) ;
#4008=CARTESIAN_POINT ( 'NONE',  ( 0.5366821535715222691, -1.667685771915632165, -0.5737988098678608040 ) ) ;
#4021=CARTESIAN_POINT ( 'NONE',  ( 0.3640814558764833286, -1.622621548676258518, -0.3679310410494832095 ) ) ;
#4023=CARTESIAN_POINT ( 'NONE',  ( 0.1959265899308196557, -1.288818386415671036, -0.7414046965098797237 ) ) ;
#4025=AXIS2_PLACEMENT_3D ( 'NONE', #39821, #37144, #36728 ) ;
#4052=CARTESIAN_POINT ( 'NONE',  ( 0.3931437146781530667, -1.977407099708731408, -0.4983079568841896623 ) ) ;
#4057=CARTESIAN_POINT ( 'NONE',  ( 0.6414788747720358009, -1.458704226864308451, -0.6334847565629259103 ) ) ;
#4061=CARTESIAN_POINT ( 'NONE',  ( 0.3812071769896587803, -1.763750790280042002, -0.4536492913031247021 ) ) ;
#4063=( BOUNDED_SURFACE ( )  B_SPLINE_SURFACE ( 3, 2, ( 
 ( #3691, #25699, #35165 ),
 ( #6966, #20342, #17645 ),
 ( #10880, #26512, #29793 ),
 ( #13740, #4480, #16853 ),
 ( #20146, #1429, #17452 ),
 ( #38639, #14350, #36359 ) ),
 .UNSPECIFIED., .F., .F., .T. ) 
 B_SPLINE_SURFACE_WITH_KNOTS ( ( 4, 2, 4 ),
 ( 3, 3 ),
 ( 0.000000000000000000, 0.0003830006634344629507, 0.0007660013268689259015 ),
 ( 0.000000000000000000, 1.000000000000000000 ),
 .UNSPECIFIED. ) 
 GEOMETRIC_REPRESENTATION_ITEM ( )  RATIONAL_B_SPLINE_SURFACE ( (
 ( 1.000000000000000000, 0.9000550641259897899, 1.000000000000000000),
 ( 1.000000000000000000, 0.9180209094310995965, 1.000000000000000000),
 ( 1.000000000000000000, 0.9393933891286406768, 1.000000000000000000),
 ( 1.000000000000000000, 0.9796198219468460477, 1.000000000000000000),
 ( 1.000000000000000000, 0.9990870677679748457, 1.000000000000000000),
 ( 1.000000000000000000, 1.000000000000000000, 1.000000000000000000) ) ) 
 REPRESENTATION_ITEM ( '' )  SURFACE ( )  );
#4064=AXIS2_PLACEMENT_3D ( 'NONE', #70, #12563, #18957 ) ;
#4080=CARTESIAN_POINT ( 'NONE',  ( 0.3402959632056912764, -1.632552626064601053, -0.5940485371126206227 ) ) ;
#4082=CARTESIAN_POINT ( 'NONE',  ( 0.5980161951564891831, -1.483775577296369219, -0.6139673809116643621 ) ) ;
#4089=CARTESIAN_POINT ( 'NONE',  ( 0.1102069964470346886, -1.338716096010474477, -0.3246197190526466936 ) ) ;
#4099=CARTESIAN_POINT ( 'NONE',  ( 0.4781934768423676818, -1.682642038360962600, -0.6151431148613257793 ) ) ;
#4106=AXIS2_PLACEMENT_3D ( 'NONE', #33652, #24219, #2203 ) ;
#4112=CARTESIAN_POINT ( 'NONE',  ( 0.3619431082889854046, -1.779064720687063783, -0.4822877365339464095 ) ) ;
#4115=DIRECTION ( 'NONE',  ( 0.8660512985181134660, 0.4999551463232371762, 0.000000000000000000 ) ) ;
#4119=AXIS2_PLACEMENT_3D ( 'NONE', #26666, #18547, #14703 ) ;
#4127=ADVANCED_FACE ( 'NONE', ( #14530 ), #26098, .F. ) ;
#4128=CARTESIAN_POINT ( 'NONE',  ( 0.5605867575437351036, -1.621001144914625991, -0.5473203437262892379 ) ) ;
#4134=CARTESIAN_POINT ( 'NONE',  ( 0.5014952879285534681, -1.689753520714762924, -0.5927250296114048300 ) ) ;
#4137=CARTESIAN_POINT ( 'NONE',  ( 0.6185380437909798745, -1.622186936341058372, -0.5032892897206091565 ) ) ;
#4171=ORIENTED_EDGE ( 'NONE', *, *, #21227, .F. ) ;
#4177=EDGE_LOOP ( 'NONE', ( #11866, #31462, #11042, #34917 ) ) ;
#4182=VERTEX_POINT ( 'NONE', #27312 ) ;
#4196=AXIS2_PLACEMENT_3D ( 'NONE', #13405, #34042, #21705 ) ;
#4199=EDGE_CURVE ( 'NONE', #3320, #28175, #13504, .T. ) ;
#4209=CIRCLE ( 'NONE', #3542, 0.02999999999999997113 ) ;
#4211=CARTESIAN_POINT ( 'NONE',  ( 0.3599247992643459515, -1.738746112742540095, -0.5101476835507584573 ) ) ;
#4221=DIRECTION ( 'NONE',  ( 0.4999551463232372317, -0.8660512985181135770, 0.000000000000000000 ) ) ;
#4229=DIRECTION ( 'NONE',  ( -0.8660512985181132439, -0.4999551463232374537, 0.000000000000000000 ) ) ;
#4236=CARTESIAN_POINT ( 'NONE',  ( 0.1876026560395943066, -1.258984853855668717, -0.7446432427863726167 ) ) ;
#4245=ORIENTED_EDGE ( 'NONE', *, *, #26886, .F. ) ;
#4253=ORIENTED_EDGE ( 'NONE', *, *, #18256, .F. ) ;
#4261=CARTESIAN_POINT ( 'NONE',  ( 0.4758899578691964116, -1.652635878263318148, -0.6322492986411032412 ) ) ;
#4263=CARTESIAN_POINT ( 'NONE',  ( -2.112273405726188513E-14, -2.097675824466503691, -0.2588528740066097233 ) ) ;
#4265=CARTESIAN_POINT ( 'NONE',  ( 0.3935416462524252146, -1.752073130202867812, -0.5293634714478211434 ) ) ;
#4270=DIRECTION ( 'NONE',  ( 0.8660512985181127998, 0.4999551463232382309, 0.000000000000000000 ) ) ;
#4276=AXIS2_PLACEMENT_3D ( 'NONE', #24188, #36712, #21089 ) ;
#4279=CARTESIAN_POINT ( 'NONE',  ( 0.5872889424020651949, -1.566257061117608984, -0.4890099139335282730 ) ) ;
#4288=ORIENTED_EDGE ( 'NONE', *, *, #7001, .F. ) ;
#4290=CARTESIAN_POINT ( 'NONE',  ( 0.5853817121637504561, -1.600135414900193620, -0.4500950668952165001 ) ) ;
#4292=DIRECTION ( 'NONE',  ( -0.4999551463232372317, 0.8660512985181133550, -0.000000000000000000 ) ) ;
#4297=B_SPLINE_CURVE_WITH_KNOTS ( 'NONE', 3,
 ( #32149, #16325, #13434, #35434, #7046, #19803, #31745, #16518 ),
 .UNSPECIFIED., .F., .F.,
 ( 4, 2, 2, 4 ),
 ( -7.633036733528553394E-06, 0.0006124121369014247709, 0.0009224347237189015102, 0.001232457310536378466 ),
 .UNSPECIFIED. ) ;
#4298=DIRECTION ( 'NONE',  ( -0.5196209861461466017, 0.8543968812890798681, 0.000000000000000000 ) ) ;
#4304=CARTESIAN_POINT ( 'NONE',  ( 0.06643860465239320723, -1.431902482846566516, -0.3407847385126873130 ) ) ;
#4324=CARTESIAN_POINT ( 'NONE',  ( 0.3511758406044653280, -1.510956930971387724, -0.7187326247832955817 ) ) ;
#4338=CARTESIAN_POINT ( 'NONE',  ( 0.5074366505258062210, -1.675708488637823068, -0.4286118871247626694 ) ) ;
#4340=CIRCLE ( 'NONE', #31954, 0.1333070866141731758 ) ;
#4341=VERTEX_POINT ( 'NONE', #19257 ) ;
#4347=CARTESIAN_POINT ( 'NONE',  ( 0.6206746333706361085, -1.620953523311430944, -0.4903377927301240669 ) ) ;
#4360=CARTESIAN_POINT ( 'NONE',  ( 0.3528298061772759953, -1.603578276458837104, -0.7003206377943665961 ) ) ;
#4362=CARTESIAN_POINT ( 'NONE',  ( 0.4711420575750281947, -1.592335044512171782, -0.5952420774259647995 ) ) ;
#4373=AXIS2_PLACEMENT_3D ( 'NONE', #7539, #26887, #20115 ) ;
#4381=CARTESIAN_POINT ( 'NONE',  ( 0.2999999999999782840, -1.939620212199285598, -0.6711716461755767860 ) ) ;
#4387=CARTESIAN_POINT ( 'NONE',  ( 0.5156877488165810819, -1.667601403840327734, -0.4359157956494498776 ) ) ;
#4391=FACE_OUTER_BOUND ( 'NONE', #27343, .T. ) ;
#4392=EDGE_LOOP ( 'NONE', ( #19976, #21437, #5938, #32322 ) ) ;
#4407=CARTESIAN_POINT ( 'NONE',  ( 0.2093596354519730585, -1.281064938727221714, -0.3178472134378123592 ) ) ;
#4413=DIRECTION ( 'NONE',  ( 0.000000000000000000, 0.000000000000000000, -1.000000000000000000 ) ) ;
#4415=CARTESIAN_POINT ( 'NONE',  ( 0.4209912206648682154, -1.078067379053157193, -0.5155029497116575543 ) ) ;
#4420=CARTESIAN_POINT ( 'NONE',  ( 0.5170632769343359580, -1.646684529498529503, -0.5823716739448009383 ) ) ;
#4423=ADVANCED_FACE ( 'NONE', ( #22554, #6682 ), #6288, .T. ) ;
#4424=ORIENTED_EDGE ( 'NONE', *, *, #36822, .T. ) ;
#4425=DIRECTION ( 'NONE',  ( 0.8308509739180691689, 0.4796346601509333119, 0.2822007298383447660 ) ) ;
#4428=CARTESIAN_POINT ( 'NONE',  ( 0.3654468122243346162, -1.742897531900985175, -0.4899584472101493060 ) ) ;
#4437=DIRECTION ( 'NONE',  ( 1.000000000000000000, 0.000000000000000000, 0.000000000000000000 ) ) ;
#4439=CARTESIAN_POINT ( 'NONE',  ( 0.5838900649597887904, -1.499867930881839007, -0.4391511121979080889 ) ) ;
#4441=DIRECTION ( 'NONE',  ( 0.000000000000000000, 0.000000000000000000, -1.000000000000000000 ) ) ;
#4445=CARTESIAN_POINT ( 'NONE',  ( 0.4739903723793378321, -1.126753373801576252, -0.6501307139337872965 ) ) ;
#4453=DIRECTION ( 'NONE',  ( 0.8660512985181135770, 0.4999551463232370652, 0.000000000000000000 ) ) ;
#4455=CARTESIAN_POINT ( 'NONE',  ( 0.4147930180073937656, -1.739805112484396954, -0.4462242041100615286 ) ) ;
#4464=CARTESIAN_POINT ( 'NONE',  ( 0.6483372838204546351, -1.461228087998845959, -0.6196388347441599276 ) ) ;
#4470=CARTESIAN_POINT ( 'NONE',  ( 0.5835378010919568537, -1.549988096145974215, -0.6077179222230424394 ) ) ;
#4477=CIRCLE ( 'NONE', #19602, 0.01000000000000002102 ) ;
#4480=CARTESIAN_POINT ( 'NONE',  ( 0.3673730737733172935, -1.765061228214683364, -0.5843795697180308446 ) ) ;
#4486=EDGE_LOOP ( 'NONE', ( #33811, #23243, #6814, #9007 ) ) ;
#4496=CARTESIAN_POINT ( 'NONE',  ( 0.1153579089856115875, -1.330707596229020462, -0.3224262535835399901 ) ) ;
#4499=CARTESIAN_POINT ( 'NONE',  ( 0.1039773195064908201, -1.347850002784139578, -0.6754723133399438417 ) ) ;
#4500=DIRECTION ( 'NONE',  ( 0.8660512985181134660, 0.4999551463232372317, 0.000000000000000000 ) ) ;
#4515=CARTESIAN_POINT ( 'NONE',  ( 0.3699999999999786793, -2.183180860297921466, -0.4437760292030870635 ) ) ;
#4519=ORIENTED_EDGE ( 'NONE', *, *, #25035, .F. ) ;
#4522=ORIENTED_EDGE ( 'NONE', *, *, #247, .T. ) ;
#4525=EDGE_CURVE ( 'NONE', #16583, #30458, #36521, .T. ) ;
#4529=ORIENTED_EDGE ( 'NONE', *, *, #2652, .F. ) ;
#4559=CARTESIAN_POINT ( 'NONE',  ( 0.3971737171416530598, -1.599718167121974677, -0.6188829515567775275 ) ) ;
#4570=CARTESIAN_POINT ( 'NONE',  ( 0.004755934575889525159, -1.810517711902423166, -0.6424739212913328501 ) ) ;
#4578=CARTESIAN_POINT ( 'NONE',  ( 0.4259907721281001036, -1.086727892038337417, -0.5155029497116575543 ) ) ;
#4593=CARTESIAN_POINT ( 'NONE',  ( 0.1999999999999789724, -2.183180860297921466, -0.4937760292030871079 ) ) ;
#4605=ORIENTED_EDGE ( 'NONE', *, *, #25393, .F. ) ;
#4612=ORIENTED_EDGE ( 'NONE', *, *, #15432, .T. ) ;
#4613=EDGE_CURVE ( 'NONE', #30897, #25550, #29952, .T. ) ;
#4625=EDGE_CURVE ( 'NONE', #23421, #37075, #38415, .T. ) ;
#4632=FACE_OUTER_BOUND ( 'NONE', #28325, .T. ) ;
#4638=ORIENTED_EDGE ( 'NONE', *, *, #791, .T. ) ;
#4643=CARTESIAN_POINT ( 'NONE',  ( 0.3839366250755201215, -1.757617928503105720, -0.4411224224773397373 ) ) ;
#4646=AXIS2_PLACEMENT_3D ( 'NONE', #12104, #27947, #22592 ) ;
#4650=CARTESIAN_POINT ( 'NONE',  ( 0.3731036225605881551, -1.710599156003107968, -0.6119997028479188250 ) ) ;
#4652=CARTESIAN_POINT ( 'NONE',  ( 0.6165640848131422880, -1.623198970764877735, -0.5229364404254283061 ) ) ;
#4658=CARTESIAN_POINT ( 'NONE',  ( 0.5735563720977525648, -1.542970242066289188, -0.5407299351178547209 ) ) ;
#4669=DIRECTION ( 'NONE',  ( -0.4999551463232372317, 0.8660512985181135770, -0.000000000000000000 ) ) ;
#4673=CIRCLE ( 'NONE', #27699, 0.05000000000000000971 ) ;
#4683=CARTESIAN_POINT ( 'NONE',  ( 0.5959725435374871871, -1.484955338987114182, -0.6097788050097984192 ) ) ;
#4687=FACE_OUTER_BOUND ( 'NONE', #19989, .T. ) ;
#4689=CARTESIAN_POINT ( 'NONE',  ( 0.1308074600572272372, -1.309647876697553004, -0.3434689383624984771 ) ) ;
#4693=CARTESIAN_POINT ( 'NONE',  ( 0.3624061103390691096, -1.968824918581854932, -0.4968426515055719972 ) ) ;
#4700=ADVANCED_FACE ( 'NONE', ( #21498, #30926 ), #12220, .F. ) ;
#4704=EDGE_CURVE ( 'NONE', #27529, #2400, #27987, .T. ) ;
#4708=DIRECTION ( 'NONE',  ( 0.7956551220374312727, 0.4593167559955310120, -0.3949190352937456128 ) ) ;
#4712=DIRECTION ( 'NONE',  ( 1.000000000000000000, 0.000000000000000000, 0.000000000000000000 ) ) ;
#4715=CARTESIAN_POINT ( 'NONE',  ( 0.4080762053856966109, -1.743682602239191137, -0.5952039892428494516 ) ) ;
#4721=VERTEX_POINT ( 'NONE', #33822 ) ;
#4722=CARTESIAN_POINT ( 'NONE',  ( 0.4514031511399141383, -1.667537665946740466, -0.4121731472126302642 ) ) ;
#4737=DIRECTION ( 'NONE',  ( 0.8660512985181132439, 0.4999551463232376758, 0.000000000000000000 ) ) ;
#4741=FACE_OUTER_BOUND ( 'NONE', #9197, .T. ) ;
#4747=CARTESIAN_POINT ( 'NONE',  ( 0.4203826191882746866, -1.700944664958486507, -0.4172566670736500560 ) ) ;
#4748=CARTESIAN_POINT ( 'NONE',  ( 0.4342601836552755223, -1.675175375883231954, -0.4163388096883527956 ) ) ;
#4749=CARTESIAN_POINT ( 'NONE',  ( 0.5437751503972781952, -1.596066189530210178, -0.5599633018817742336 ) ) ;
#4751=CARTESIAN_POINT ( 'NONE',  ( 0.1997919287435963309, -2.061796588699760235, -0.2711072614840514539 ) ) ;
#4756=CARTESIAN_POINT ( 'NONE',  ( 0.4511668698691139179, -1.684167190675012415, -0.3144976166544468099 ) ) ;
#4762=AXIS2_PLACEMENT_3D ( 'NONE', #13083, #4221, #13282 ) ;
#4763=AXIS2_PLACEMENT_3D ( 'NONE', #1647, #7784, #20353 ) ;
#4764=CARTESIAN_POINT ( 'NONE',  ( 0.4139909421053795113, -1.650376109496379140, -0.6250900372738893429 ) ) ;
#4766=AXIS2_PLACEMENT_3D ( 'NONE', #8258, #37047, #14627 ) ;
#4773=CARTESIAN_POINT ( 'NONE',  ( 0.3853411735687863326, -1.756807109041631509, -0.4499573014711771846 ) ) ;
#4777=CARTESIAN_POINT ( 'NONE',  ( 0.1263619274532199466, -1.314871306717832367, -0.7136791684005103775 ) ) ;
#4778=( BOUNDED_SURFACE ( )  B_SPLINE_SURFACE ( 3, 2, ( 
 ( #36647, #23912, #11950 ),
 ( #1903, #27592, #27798 ),
 ( #11750, #33347, #8255 ),
 ( #33154, #24514, #14415 ) ),
 .UNSPECIFIED., .F., .F., .T. ) 
 B_SPLINE_SURFACE_WITH_KNOTS ( ( 4, 4 ),
 ( 3, 3 ),
 ( 0.000000000000000000, 0.0002728543041759452824 ),
 ( 0.000000000000000000, 1.000000000000000000 ),
 .UNSPECIFIED. ) 
 GEOMETRIC_REPRESENTATION_ITEM ( )  RATIONAL_B_SPLINE_SURFACE ( (
 ( 1.000000000000000000, 0.7071067811865477948, 1.000000000000000000),
 ( 1.000000000000000000, 0.7071067862473439103, 1.000000000000000000),
 ( 1.000000000000000000, 0.7071227907078153629, 1.000000000000000000),
 ( 1.000000000000000000, 0.7071530416912256145, 1.000000000000000000) ) ) 
 REPRESENTATION_ITEM ( '' )  SURFACE ( )  );
#4792=DIRECTION ( 'NONE',  ( -0.4686504021719342661, -0.2705430738262412649, -0.8409359343902087502 ) ) ;
#4795=ORIENTED_EDGE ( 'NONE', *, *, #35631, .T. ) ;
#4802=CARTESIAN_POINT ( 'NONE',  ( 0.1716982692503948582, -1.801629902383738324, -0.6814167475625579895 ) ) ;
#4805=CARTESIAN_POINT ( 'NONE',  ( 0.3699999999999786793, -2.097675824466503691, -0.5027161252448985040 ) ) ;
#4806=CIRCLE ( 'NONE', #1563, 0.05000000000000000971 ) ;
#4807=CARTESIAN_POINT ( 'NONE',  ( 0.1308641205180471057, -1.355064818086789025, -0.3217643887045131268 ) ) ;
#4808=CARTESIAN_POINT ( 'NONE',  ( 0.4853385542066005476, -1.649621470899823583, -0.6309284955820858576 ) ) ;
#4810=CARTESIAN_POINT ( 'NONE',  ( 0.4534739523000680950, -1.220957794426671406, -0.5155029497116575543 ) ) ;
#4811=DIRECTION ( 'NONE',  ( -0.4999551463232373427, 0.8660512985181134660, -0.000000000000000000 ) ) ;
#4813=CIRCLE ( 'NONE', #19332, 0.009999999999999995004 ) ;
#4822=ORIENTED_EDGE ( 'NONE', *, *, #27778, .F. ) ;
#4828=CARTESIAN_POINT ( 'NONE',  ( 0.1993125180077263137, -2.032910743388167685, -0.2793764414722799683 ) ) ;
#4833=CARTESIAN_POINT ( 'NONE',  ( 0.5816004637761955642, -1.517907389782662042, -0.4510474287064656918 ) ) ;
#4837=CYLINDRICAL_SURFACE ( 'NONE', #14106, 0.1033070866141732880 ) ;
#4843=AXIS2_PLACEMENT_3D ( 'NONE', #35315, #20098, #6707 ) ;
#4850=AXIS2_PLACEMENT_3D ( 'NONE', #14312, #32630, #17607 ) ;
#4851=EDGE_CURVE ( 'NONE', #858, #29150, #8983, .T. ) ;
#4852=CARTESIAN_POINT ( 'NONE',  ( 0.3720910755108596812, -1.764456141754468188, -0.4343423851154138982 ) ) ;
#4855=CARTESIAN_POINT ( 'NONE',  ( 0.3957353887311833018, -1.753985813695325247, -0.5139772769213331038 ) ) ;
#4865=CARTESIAN_POINT ( 'NONE',  ( 0.5839561686609843205, -1.602591383399306624, -0.5767004275490535958 ) ) ;
#4872=CARTESIAN_POINT ( 'NONE',  ( 0.5856933011632973196, -1.570058762653790518, -0.5108706408130125887 ) ) ;
#4881=AXIS2_PLACEMENT_3D ( 'NONE', #37993, #22185, #19490 ) ;
#4895=ORIENTED_EDGE ( 'NONE', *, *, #10016, .F. ) ;
#4901=DIRECTION ( 'NONE',  ( 0.8660512985181133550, 0.4999551463232372317, 0.000000000000000000 ) ) ;
#4903=MANIFOLD_SOLID_BREP ( 'Fillet7', #15507 ) ;
#4911=CIRCLE ( 'NONE', #15452, 0.02999999999999997460 ) ;
#4924=VECTOR ( 'NONE', #24027, 39.37007874015748854 ) ;
#4925=CARTESIAN_POINT ( 'NONE',  ( 0.6430098986722891929, -1.590739804012314185, -0.4546931408925402041 ) ) ;
#4927=CARTESIAN_POINT ( 'NONE',  ( 0.3576546886276804615, -1.772789996722293537, -0.5848438031758242950 ) ) ;
#4931=VERTEX_POINT ( 'NONE', #3955 ) ;
#4944=ORIENTED_EDGE ( 'NONE', *, *, #32611, .F. ) ;
#4949=CARTESIAN_POINT ( 'NONE',  ( 0.6353491899451704228, -1.612482177454656496, -0.4775148252911664004 ) ) ;
#4952=VERTEX_POINT ( 'NONE', #19417 ) ;
#4962=CARTESIAN_POINT ( 'NONE',  ( 0.3713793989799819562, -1.734397752681366534, -0.4210101696510674119 ) ) ;
#4964=CARTESIAN_POINT ( 'NONE',  ( 0.3766924275363039976, -1.659541107949447980, -0.6295622186357943129 ) ) ;
#4965=CARTESIAN_POINT ( 'NONE',  ( 0.3699999999982759302, -2.089770822019046292, -0.2936553927183578883 ) ) ;
#4968=CARTESIAN_POINT ( 'NONE',  ( 0.3569552165733603233, -1.627031886803703919, -0.3705999156339398470 ) ) ;
#4972=CARTESIAN_POINT ( 'NONE',  ( 0.6301045230376582928, -1.599306761647289354, -0.4491897841421867987 ) ) ;
#4978=FACE_OUTER_BOUND ( 'NONE', #39219, .T. ) ;
#4982=CARTESIAN_POINT ( 'NONE',  ( 0.4184753273149497965, -1.633759443312357007, -0.5155029497116575543 ) ) ;
#4987=CARTESIAN_POINT ( 'NONE',  ( 0.3885726445799232431, -1.811795032242741632, -0.5028984591946519256 ) ) ;
#4990=CARTESIAN_POINT ( 'NONE',  ( 0.4961012839380697370, -1.676527870641093987, -0.4225323133350444849 ) ) ;
#4994=CARTESIAN_POINT ( 'NONE',  ( 0.09602014362969647776, -1.423132328501501620, -0.6903307521141727188 ) ) ;
#5001=CARTESIAN_POINT ( 'NONE',  ( 0.1995529058109158649, -2.050896138459939344, -0.3054326997595754878 ) ) ;
#5018=EDGE_CURVE ( 'NONE', #25046, #31057, #20773, .T. ) ;
#5021=CARTESIAN_POINT ( 'NONE',  ( 0.1729041008443502614, -1.754908398349515952, -0.6809640004795894930 ) ) ;
#5025=CARTESIAN_POINT ( 'NONE',  ( 0.1815643315344221131, -1.297094087716649025, -0.2985759631856487739 ) ) ;
#5030=LINE ( 'NONE', #20691, #27781 ) ;
#5037=AXIS2_PLACEMENT_3D ( 'NONE', #39230, #5060, #8145 ) ;
#5039=VERTEX_POINT ( 'NONE', #16927 ) ;
#5043=CARTESIAN_POINT ( 'NONE',  ( 0.1800577004789429558, -1.845764677012176724, -0.3170475007989994598 ) ) ;
#5045=EDGE_CURVE ( 'NONE', #5149, #4721, #10253, .T. ) ;
#5047=CARTESIAN_POINT ( 'NONE',  ( 0.3622253751127874066, -1.756884464425453984, -0.4902987826081479650 ) ) ;
#5049=ORIENTED_EDGE ( 'NONE', *, *, #21937, .F. ) ;
#5060=DIRECTION ( 'NONE',  ( 1.000000000000000000, 0.000000000000000000, 0.000000000000000000 ) ) ;
#5067=CARTESIAN_POINT ( 'NONE',  ( 0.3956653418828486868, -1.754139636876368424, -0.4989181662982050125 ) ) ;
#5070=CARTESIAN_POINT ( 'NONE',  ( 0.3656049513378988314, -1.732259804546445681, -0.6036892049131413751 ) ) ;
#5073=CARTESIAN_POINT ( 'NONE',  ( 0.6022157181008760407, -1.594425423205000580, -0.5367861729570986284 ) ) ;
#5076=CARTESIAN_POINT ( 'NONE',  ( 0.5755854119334320451, -1.646982683870169328, -0.5473203437262896820 ) ) ;
#5079=CARTESIAN_POINT ( 'NONE',  ( 0.5644318452406892339, -1.583177861798296115, -0.4893328019707191556 ) ) ;
#5087=CARTESIAN_POINT ( 'NONE',  ( 0.6000000852309536059, -1.576678414952007445, -0.4214712295370082740 ) ) ;
#5107=CARTESIAN_POINT ( 'NONE',  ( 0.3686258320291115886, -2.054720120239651671, -0.5116857311949160048 ) ) ;
#5114=EDGE_CURVE ( 'NONE', #8591, #25550, #19736, .T. ) ;
#5119=B_SPLINE_CURVE_WITH_KNOTS ( 'NONE', 3,
 ( #9170, #14753, #5470, #21347 ),
 .UNSPECIFIED., .F., .F.,
 ( 4, 4 ),
 ( 0.002631652860467224766, 0.002956730596035610920 ),
 .UNSPECIFIED. ) ;
#5123=CARTESIAN_POINT ( 'NONE',  ( 0.1999999999999789724, -2.183180860297921466, -0.4937760292030871079 ) ) ;
#5125=CARTESIAN_POINT ( 'NONE',  ( 0.3782504645320439174, -1.760900442173329195, -0.5806069901403015932 ) ) ;
#5145=CARTESIAN_POINT ( 'NONE',  ( 0.6380336481227063539, -1.610932490174762366, -0.4493560576004195783 ) ) ;
#5147=EDGE_CURVE ( 'NONE', #29909, #33903, #659, .T. ) ;
#5149=VERTEX_POINT ( 'NONE', #6374 ) ;
#5153=DIRECTION ( 'NONE',  ( 0.8660512985181126888, 0.4999551463232385085, 0.000000000000000000 ) ) ;
#5154=DIRECTION ( 'NONE',  ( 0.8660512985181142431, 0.4999551463232357884, 0.000000000000000000 ) ) ;
#5162=CARTESIAN_POINT ( 'NONE',  ( 0.3699999999999787903, -2.050772785069567838, -0.3050017341552441197 ) ) ;
#5163=DIRECTION ( 'NONE',  ( 0.4999551463232372317, -0.8660512985181133550, 0.000000000000000000 ) ) ;
#5168=CARTESIAN_POINT ( 'NONE',  ( 0.6307892698844480561, -1.598909026140060918, -0.5827525826989481406 ) ) ;
#5174=CARTESIAN_POINT ( 'NONE',  ( 0.3632268640774227175, -1.623167453423570050, -0.6631189784283982869 ) ) ;
#5178=CARTESIAN_POINT ( 'NONE',  ( 0.2534230856981304347, -1.365321207853003926, -0.7462941026102631881 ) ) ;
#5182=CARTESIAN_POINT ( 'NONE',  ( 0.3923243630925589143, -1.966611948492527073, -0.4968729097669083439 ) ) ;
#5183=ORIENTED_EDGE ( 'NONE', *, *, #13209, .T. ) ;
#5188=CARTESIAN_POINT ( 'NONE',  ( 0.07370827096331192263, -1.490549976626241557, -0.6787781514709749775 ) ) ;
#5197=VERTEX_POINT ( 'NONE', #22040 ) ;
#5211=CARTESIAN_POINT ( 'NONE',  ( 0.4170115945640069932, -1.702980413955156758, -0.6123808887097255127 ) ) ;
#5215=EDGE_CURVE ( 'NONE', #13200, #11734, #37915, .T. ) ;
#5216=CARTESIAN_POINT ( 'NONE',  ( 0.3695052819757340123, -1.758428263776099287, -0.4278193900811940176 ) ) ;
#5218=CARTESIAN_POINT ( 'NONE',  ( 0.3839258146201624533, -1.730368705836311083, -0.7198767004735652231 ) ) ;
#5229=ORIENTED_EDGE ( 'NONE', *, *, #31657, .F. ) ;
#5230=CARTESIAN_POINT ( 'NONE',  ( 0.2923286432308245808, -1.660243258845594649, -0.6250000000000000000 ) ) ;
#5236=CARTESIAN_POINT ( 'NONE',  ( 0.1963846320365078280, -1.666482349971158072, -0.3293983578754329233 ) ) ;
#5240=CARTESIAN_POINT ( 'NONE',  ( 0.2729656450513567312, -1.175066423404427463, -0.5155029497116575543 ) ) ;
#5250=CARTESIAN_POINT ( 'NONE',  ( 0.4333248279805138603, -1.117134059754063102, -0.6448776663562968414 ) ) ;
#5253=CARTESIAN_POINT ( 'NONE',  ( 0.3999999999999789280, -2.042495778117166427, -0.2760839614659714170 ) ) ;
#5259=CARTESIAN_POINT ( 'NONE',  ( 0.3969982963057281378, -1.750077671058421824, -0.4821875037442182599 ) ) ;
#5260=CARTESIAN_POINT ( 'NONE',  ( 0.3815368266015568555, -1.759003287083186651, -0.4522571440128324571 ) ) ;
#5265=CARTESIAN_POINT ( 'NONE',  ( 0.5781127729594031095, -1.609402375371582261, -0.4754652686900157632 ) ) ;
#5268=CARTESIAN_POINT ( 'NONE',  ( 0.3867756831795865491, -1.746236785580605799, -0.4374737505989281794 ) ) ;
#5271=CARTESIAN_POINT ( 'NONE',  ( 0.4025254666410605919, -1.691731883620783972, -0.6096246207440890741 ) ) ;
#5275=DIRECTION ( 'NONE',  ( -0.4999551463232373427, 0.8660512985181134660, -0.000000000000000000 ) ) ;
#5281=VERTEX_POINT ( 'NONE', #1652 ) ;
#5286=DIRECTION ( 'NONE',  ( -0.4999551463232377313, 0.8660512985181132439, 0.000000000000000000 ) ) ;
#5287=AXIS2_PLACEMENT_3D ( 'NONE', #16382, #38591, #10413 ) ;
#5306=CIRCLE ( 'NONE', #3354, 0.02999999999999998501 ) ;
#5314=CIRCLE ( 'NONE', #2705, 0.08830708661417320526 ) ;
#5335=CARTESIAN_POINT ( 'NONE',  ( 0.5277393960915062188, -1.600937019047668386, -0.4329714461315667950 ) ) ;
#5342=DIRECTION ( 'NONE',  ( 0.4999551463232373427, -0.8660512985181134660, 0.000000000000000000 ) ) ;
#5349=CARTESIAN_POINT ( 'NONE',  ( 0.2914323826288400254, -1.233685883474753497, -0.5166151207188711680 ) ) ;
#5353=CARTESIAN_POINT ( 'NONE',  ( 0.3327215102334385999, -1.655855958731206279, -0.6422681889546366651 ) ) ;
#5354=CARTESIAN_POINT ( 'NONE',  ( 0.4584717390208091770, -1.703043547193807017, -0.5155029497116575543 ) ) ;
#5358=CARTESIAN_POINT ( 'NONE',  ( 0.3397077535880360655, -1.654685348432989089, -0.3858274525146618839 ) ) ;
#5366=ADVANCED_FACE ( 'NONE', ( #37389 ), #11887, .F. ) ;
#5369=ADVANCED_FACE ( 'NONE', ( #2449 ), #9625, .F. ) ;
#5373=( BOUNDED_SURFACE ( )  B_SPLINE_SURFACE ( 3, 2, ( 
 ( #919, #10534, #13423 ),
 ( #26597, #4360, #25997 ),
 ( #10351, #10959, #22912 ),
 ( #13624, #23106, #16921 ) ),
 .UNSPECIFIED., .F., .F., .F. ) 
 B_SPLINE_SURFACE_WITH_KNOTS ( ( 4, 4 ),
 ( 3, 3 ),
 ( -3.816391647148975608E-16, 0.002151548051257937220 ),
 ( 0.000000000000000000, 0.5629264174124741782 ),
 .UNSPECIFIED. ) 
 GEOMETRIC_REPRESENTATION_ITEM ( )  RATIONAL_B_SPLINE_SURFACE ( (
 ( 1.000000000000000000, 0.8349447961261939888, 0.8557174614363223242),
 ( 1.000000000000000000, 0.8351496430544862459, 0.8558965277979837527),
 ( 1.000000000000000000, 0.8351234014981824272, 0.8558735888159310079),
 ( 1.000000000000000000, 0.8351226696489343349, 0.8558729490719854116) ) ) 
 REPRESENTATION_ITEM ( '' )  SURFACE ( )  );
#5382=CARTESIAN_POINT ( 'NONE',  ( 0.3840624009215719559, -1.828512337075534067, -0.4831679149489520042 ) ) ;
#5387=CARTESIAN_POINT ( 'NONE',  ( 0.05005283029671573486, -1.480230044530827183, -0.6492973086577381592 ) ) ;
#5389=CARTESIAN_POINT ( 'NONE',  ( 0.3641350647596797163, -1.746033381779148685, -0.5249093166418893341 ) ) ;
#5390=EDGE_CURVE ( 'NONE', #33903, #1802, #37202, .T. ) ;
#5402=ORIENTED_EDGE ( 'NONE', *, *, #21576, .T. ) ;
#5405=FACE_OUTER_BOUND ( 'NONE', #18669, .T. ) ;
#5411=CARTESIAN_POINT ( 'NONE',  ( 0.3905383237075480407, -1.946889847283715502, -0.6985532018724728287 ) ) ;
#5419=CARTESIAN_POINT ( 'NONE',  ( 0.1989987071918978556, -2.049746683003707659, -0.6828288310443214604 ) ) ;
#5424=CARTESIAN_POINT ( 'NONE',  ( 0.2209260011871197193, -1.309027873449325918, -0.4125659523519145666 ) ) ;
#5455=CARTESIAN_POINT ( 'NONE',  ( 0.3660264286422114655, -1.617698911701153541, -0.3269368557715229273 ) ) ;
#5457=CARTESIAN_POINT ( 'NONE',  ( 0.4013789418293162159, -1.744061236993332598, -0.3095045109458399168 ) ) ;
#5470=CARTESIAN_POINT ( 'NONE',  ( 0.4809559340294914387, -1.681307585311514030, -0.4166691164814795845 ) ) ;
#5472=CARTESIAN_POINT ( 'NONE',  ( 0.6250251996679087041, -1.551063519682329916, -0.6012742504684129852 ) ) ;
#5475=EDGE_CURVE ( 'NONE', #23598, #19341, #7653, .T. ) ;
#5479=VECTOR ( 'NONE', #5163, 39.37007874015748854 ) ;
#5482=CARTESIAN_POINT ( 'NONE',  ( 0.4054951491981567679, -1.758726281608485875, -0.5878757131129308533 ) ) ;
#5483=CARTESIAN_POINT ( 'NONE',  ( 0.4186432780919986940, -1.612034538517058246, -0.6668481824684705517 ) ) ;
#5484=DIRECTION ( 'NONE',  ( 0.8660512985181134660, 0.4999551463232372317, 0.000000000000000000 ) ) ;
#5489=EDGE_CURVE ( 'NONE', #38598, #19021, #16783, .T. ) ;
#5500=VERTEX_POINT ( 'NONE', #21771 ) ;
#5502=ORIENTED_EDGE ( 'NONE', *, *, #28027, .F. ) ;
#5514=CARTESIAN_POINT ( 'NONE',  ( 0.2484378334537183652, -1.581318528659484191, -0.3509054470090272604 ) ) ;
#5515=LINE ( 'NONE', #24876, #19154 ) ;
#5518=CARTESIAN_POINT ( 'NONE',  ( 0.0006028978349475794165, -1.952399615628604757, -0.3318938993356948530 ) ) ;
#5528=EDGE_CURVE ( 'NONE', #15019, #39255, #31307, .T. ) ;
#5532=CARTESIAN_POINT ( 'NONE',  ( 0.5724688059860902900, -1.573362539590891229, -0.5731659206011648910 ) ) ;
#5548=ORIENTED_EDGE ( 'NONE', *, *, #3465, .T. ) ;
#5553=CARTESIAN_POINT ( 'NONE',  ( 0.1943609810622756173, -1.255083399771677266, -0.3178472134378122482 ) ) ;
#5567=CIRCLE ( 'NONE', #10155, 0.1050228153667111808 ) ;
#5572=CARTESIAN_POINT ( 'NONE',  ( 0.4116746766561834581, -1.754103855848320626, -0.4360744270256505239 ) ) ;
#5577=DIRECTION ( 'NONE',  ( 0.4999551463232372317, -0.8660512985181135770, 0.000000000000000000 ) ) ;
#5581=DIRECTION ( 'NONE',  ( -0.000000000000000000, 0.9396926207859070956, 0.3420201433256722101 ) ) ;
#5588=CARTESIAN_POINT ( 'NONE',  ( 0.4184753273149498520, -1.633759443312357229, -0.5155029497116575543 ) ) ;
#5591=ORIENTED_EDGE ( 'NONE', *, *, #9908, .T. ) ;
#5600=VERTEX_POINT ( 'NONE', #11502 ) ;
#5624=CARTESIAN_POINT ( 'NONE',  ( 0.3690031775293027283, -2.059871137024939625, -0.4867069271398427599 ) ) ;
#5630=CARTESIAN_POINT ( 'NONE',  ( 0.3597322771628292393, -1.737184542215604033, -0.5031181248198197675 ) ) ;
#5633=( BOUNDED_SURFACE ( )  B_SPLINE_SURFACE ( 3, 2, ( 
 ( #26197, #23116, #10356 ),
 ( #16132, #37923, #7446 ),
 ( #537, #25790, #19615 ),
 ( #3563, #38314, #6837 ),
 ( #35027, #10143, #12831 ),
 ( #22716, #13631, #16728 ) ),
 .UNSPECIFIED., .F., .F., .F. ) 
 B_SPLINE_SURFACE_WITH_KNOTS ( ( 4, 2, 4 ),
 ( 3, 3 ),
 ( 0.000000000000000000, 0.0006488076353390061744, 0.001297615270678012349 ),
 ( 0.000000000000000000, 1.000000000000000000 ),
 .UNSPECIFIED. ) 
 GEOMETRIC_REPRESENTATION_ITEM ( )  RATIONAL_B_SPLINE_SURFACE ( (
 ( 1.000000000000000000, 0.8219793159978276975, 1.000000000000000000),
 ( 1.000000000000000000, 0.8058033770605222967, 1.000000000000000000),
 ( 1.000000000000000000, 0.7882677358999856665, 1.000000000000000000),
 ( 1.000000000000000000, 0.7498419410649512784, 1.000000000000000000),
 ( 1.000000000000000000, 0.7296076275689642454, 1.000000000000000000),
 ( 1.000000000000000000, 0.7071067811865446862, 1.000000000000000000) ) ) 
 REPRESENTATION_ITEM ( '' )  SURFACE ( )  );
#5637=CARTESIAN_POINT ( 'NONE',  ( 0.3662805103927266881, -2.019948479727926571, -0.5051633158473676222 ) ) ;
#5654=CARTESIAN_POINT ( 'NONE',  ( 0.2456699162554547011, -1.579418306085378143, -0.3207381830095928921 ) ) ;
#5669=CARTESIAN_POINT ( 'NONE',  ( 0.3699999999999786793, -2.166079853131637201, -0.5407606602423821185 ) ) ;
#5672=CARTESIAN_POINT ( 'NONE',  ( 0.4357251440965448919, -1.593374815047817750, -0.6129939512658331147 ) ) ;
#5673=CARTESIAN_POINT ( 'NONE',  ( 0.3988316749348294610, -2.033309342251372165, -0.2786258215130219540 ) ) ;
#5677=CARTESIAN_POINT ( 'NONE',  ( 0.4234909963964844648, -1.082397635545747638, -0.5155029497116575543 ) ) ;
#5681=DIRECTION ( 'NONE',  ( 0.8660512985181126888, 0.4999551463232385085, 0.000000000000000000 ) ) ;
#5689=CARTESIAN_POINT ( 'NONE',  ( 0.6093641782434934262, -1.558562247244742016, -0.4097570653135631513 ) ) ;
#5694=ORIENTED_EDGE ( 'NONE', *, *, #35631, .F. ) ;
#5696=CARTESIAN_POINT ( 'NONE',  ( 0.3955714498361173059, -1.685393650580701674, -0.6248087526158117022 ) ) ;
#5697=CARTESIAN_POINT ( 'NONE',  ( 0.2456699162554547011, -1.579418306085378143, -0.3207381830095928921 ) ) ;
#5700=CARTESIAN_POINT ( 'NONE',  ( 0.4697623592636159806, -1.061459377010899541, -0.6056023639864148711 ) ) ;
#5712=DIRECTION ( 'NONE',  ( 0.8660512985181140211, 0.4999551463232362880, 0.000000000000000000 ) ) ;
#5722=B_SPLINE_CURVE_WITH_KNOTS ( 'NONE', 3,
 ( #30388, #27103, #11672, #33662, #5268, #18040, #29992, #14758, #11860, #2218 ),
 .UNSPECIFIED., .F., .F.,
 ( 4, 2, 2, 2, 4 ),
 ( 2.928550287019058723E-17, 0.0003680060388662723830, 0.0007360120777325154925, 0.001104018116598758656, 0.001472024155465001712 ),
 .UNSPECIFIED. ) ;
#5730=FACE_OUTER_BOUND ( 'NONE', #12863, .T. ) ;
#5739=EDGE_CURVE ( 'NONE', #39763, #33249, #28080, .T. ) ;
#5747=CARTESIAN_POINT ( 'NONE',  ( 0.1909286924077253367, -1.257064795538238577, -0.3194715457588298002 ) ) ;
#5750=EDGE_LOOP ( 'NONE', ( #23965, #1059, #23365, #6251 ) ) ;
#5756=ORIENTED_EDGE ( 'NONE', *, *, #11155, .F. ) ;
#5767=EDGE_LOOP ( 'NONE', ( #28652, #4612, #14707 ) ) ;
#5773=B_SPLINE_SURFACE_WITH_KNOTS ( 'NONE', 3, 3, ( 
 ( #24681, #37210, #12511, #5918 ),
 ( #18690, #31251, #3069, #15612 ),
 ( #9421, #31445, #22001, #18908 ),
 ( #15802, #38212, #19514, #10250 ),
 ( #31851, #32044, #22819, #6941 ),
 ( #3855, #10036, #16407, #25680 ),
 ( #31642, #13322, #812, #4263 ) ),
 .UNSPECIFIED., .F., .F., .F.,
 ( 4, 1, 1, 1, 4 ),
 ( 4, 4 ),
 ( 0.000000000000000000, 0.2500000000000000000, 0.5000000000000000000, 0.7500000000000000000, 1.000000000000000000 ),
 ( 0.000000000000000000, 1.000000000000000000 ),
 .UNSPECIFIED. ) ;
#5791=CARTESIAN_POINT ( 'NONE',  ( 0.3888422987255840124, -1.656336475002445852, -0.4124152405210352867 ) ) ;
#5808=CARTESIAN_POINT ( 'NONE',  ( 0.2211959769661343000, -1.309495541150525799, -0.7462941026102624109 ) ) ;
#5814=CARTESIAN_POINT ( 'NONE',  ( 0.2059273467974225835, -1.283046334493782359, -0.6184399470714002645 ) ) ;
#5817=CARTESIAN_POINT ( 'NONE',  ( 0.3675290616383497522, -2.037944530059963899, -0.5194381825500766769 ) ) ;
#5823=CARTESIAN_POINT ( 'NONE',  ( 0.3597251525720394638, -1.934001777038073966, -0.5018490200258421963 ) ) ;
#5824=CARTESIAN_POINT ( 'NONE',  ( 0.1977396076612820686, -2.033875238904685911, -0.6790160287402571271 ) ) ;
#5841=CARTESIAN_POINT ( 'NONE',  ( 0.2388826316829160967, -1.586798636953708153, -0.3224480331617204376 ) ) ;
#5851=EDGE_CURVE ( 'NONE', #13497, #33249, #2440, .T. ) ;
#5852=CARTESIAN_POINT ( 'NONE',  ( 0.3357988224803010735, -1.647249694224340644, -0.6476600625557819013 ) ) ;
#5855=CARTESIAN_POINT ( 'NONE',  ( 0.3700000000034951997, -2.073259481263499904, -0.6892711341747153053 ) ) ;
#5859=CARTESIAN_POINT ( 'NONE',  ( 0.3958825554100721122, -1.762582803447005464, -0.5282878467486828988 ) ) ;
#5872=CARTESIAN_POINT ( 'NONE',  ( 0.6481235002692135039, -1.442380924828635447, -0.4125509721431598886 ) ) ;
#5873=CARTESIAN_POINT ( 'NONE',  ( 0.1173046356037009130, -1.376169800289570366, -0.7015791660361966331 ) ) ;
#5874=EDGE_CURVE ( 'NONE', #2060, #25189, #23481, .T. ) ;
#5881=CARTESIAN_POINT ( 'NONE',  ( 0.3855795899639143376, -1.693646422290408848, -0.6199096498204479389 ) ) ;
#5884=EDGE_CURVE ( 'NONE', #33803, #10331, #30138, .T. ) ;
#5885=CARTESIAN_POINT ( 'NONE',  ( 0.4081716264380484960, -1.688076292791303334, -0.6123051696410528599 ) ) ;
#5888=VERTEX_POINT ( 'NONE', #4810 ) ;
#5889=FACE_OUTER_BOUND ( 'NONE', #13516, .T. ) ;
#5895=CARTESIAN_POINT ( 'NONE',  ( 0.5435933681566625930, -1.596171129003035150, -0.5612309872450876869 ) ) ;
#5901=ORIENTED_EDGE ( 'NONE', *, *, #27040, .T. ) ;
#5904=CARTESIAN_POINT ( 'NONE',  ( 0.4137599315576335757, -1.590143257116447995, -0.4137273532990812797 ) ) ;
#5908=CIRCLE ( 'NONE', #7896, 0.2200000000000000844 ) ;
#5910=ORIENTED_EDGE ( 'NONE', *, *, #17691, .T. ) ;
#5917=CARTESIAN_POINT ( 'NONE',  ( 0.5827850094984949880, -1.549234897118938248, -0.4241087081391718971 ) ) ;
#5918=CARTESIAN_POINT ( 'NONE',  ( 0.3999999999999787059, -2.097675824466503691, -0.2588528740066097233 ) ) ;
#5922=CARTESIAN_POINT ( 'NONE',  ( 0.04579397197547097759, -1.450962534347209898, -0.6396520520129289622 ) ) ;
#5938=ORIENTED_EDGE ( 'NONE', *, *, #6468, .F. ) ;
#5956=CARTESIAN_POINT ( 'NONE',  ( 0.4264202721361137760, -1.467519734074644200, -0.5166151207188711680 ) ) ;
#5960=EDGE_LOOP ( 'NONE', ( #33297, #39298 ) ) ;
#5963=CARTESIAN_POINT ( 'NONE',  ( 0.3861171055049215095, -1.790989158299715500, -0.4824067298016651573 ) ) ;
#5968=CARTESIAN_POINT ( 'NONE',  ( 0.5271998568954198161, -1.674914755896795837, -0.4628290575504125925 ) ) ;
#5974=CARTESIAN_POINT ( 'NONE',  ( 0.3409152363046951129, -1.516880185093671063, -0.7462941026102624109 ) ) ;
#5975=CARTESIAN_POINT ( 'NONE',  ( 0.3969982963057278047, -1.750077671058422046, -0.4821875037442182599 ) ) ;
#5988=CARTESIAN_POINT ( 'NONE',  ( 0.3700641620961017120, -1.680321446636507954, -0.4309109543678180665 ) ) ;
#5992=AXIS2_PLACEMENT_3D ( 'NONE', #28995, #13367, #6988 ) ;
#5998=ORIENTED_EDGE ( 'NONE', *, *, #14680, .T. ) ;
#6009=CARTESIAN_POINT ( 'NONE',  ( 0.2059273467974225835, -1.283046334493782359, -0.2869361388274796476 ) ) ;
#6018=CARTESIAN_POINT ( 'NONE',  ( 0.5014513378216763906, -1.607116428610278369, -0.6294611457982872693 ) ) ;
#6023=CARTESIAN_POINT ( 'NONE',  ( -2.112273405726188513E-14, -2.097675824466503691, -0.6968637352380161465 ) ) ;
#6027=AXIS2_PLACEMENT_3D ( 'NONE', #24820, #9154, #34251 ) ;
#6032=CARTESIAN_POINT ( 'NONE',  ( 0.3572717916512525571, -1.888853545459783234, -0.6650645762259550509 ) ) ;
#6035=ORIENTED_EDGE ( 'NONE', *, *, #277, .T. ) ;
#6038=FACE_OUTER_BOUND ( 'NONE', #341, .T. ) ;
#6046=CARTESIAN_POINT ( 'NONE',  ( 0.5096379620664639454, -1.685052907890733698, -0.5155029497116575543 ) ) ;
#6048=CARTESIAN_POINT ( 'NONE',  ( 0.1825719458642482418, -1.864899009783420158, -0.3443257192141048750 ) ) ;
#6058=AXIS2_PLACEMENT_3D ( 'NONE', #10702, #32900, #29227 ) ;
#6067=CARTESIAN_POINT ( 'NONE',  ( 0.1866634323211664725, -1.707720045599271819, -0.3287304398696229146 ) ) ;
#6078=CARTESIAN_POINT ( 'NONE',  ( 0.6505092258671375527, -1.603730573490085964, -0.4546931408925402041 ) ) ;
#6079=CARTESIAN_POINT ( 'NONE',  ( 0.3979572690256317213, -2.042933421733604149, -0.4802053186314065858 ) ) ;
#6087=AXIS2_PLACEMENT_3D ( 'NONE', #4578, #21056, #17151 ) ;
#6089=CARTESIAN_POINT ( 'NONE',  ( 0.5490567416132084988, -1.662297187303882984, -0.4838776693470574486 ) ) ;
#6096=DIRECTION ( 'NONE',  ( 0.8660512985181135770, 0.4999551463232370097, 0.000000000000000000 ) ) ;
#6099=CARTESIAN_POINT ( 'NONE',  ( 0.4887808337931878744, -1.608878316057391400, -0.6385965546679245319 ) ) ;
#6107=( BOUNDED_SURFACE ( )  B_SPLINE_SURFACE ( 3, 2, ( 
 ( #38032, #9844, #28781 ),
 ( #34544, #10055, #25694 ),
 ( #38227, #38632, #13340 ),
 ( #16848, #13936, #14148 ) ),
 .UNSPECIFIED., .F., .F., .T. ) 
 B_SPLINE_SURFACE_WITH_KNOTS ( ( 4, 4 ),
 ( 3, 3 ),
 ( 0.000000000000000000, 0.0003300252796214654259 ),
 ( 0.000000000000000000, 1.000000000000000000 ),
 .UNSPECIFIED. ) 
 GEOMETRIC_REPRESENTATION_ITEM ( )  RATIONAL_B_SPLINE_SURFACE ( (
 ( 1.000000000000000000, 0.4928180116091757101, 1.000000000000000000),
 ( 1.000000000000000000, 0.4791232869326966792, 1.000000000000000000),
 ( 1.000000000000000000, 0.4652192647841347783, 1.000000000000000000),
 ( 1.000000000000000000, 0.4512702095610768294, 1.000000000000000000) ) ) 
 REPRESENTATION_ITEM ( '' )  SURFACE ( )  );
#6111=DIRECTION ( 'NONE',  ( -0.02995152272103777241, 0.7083160032631821146, -0.7052597718627959811 ) ) ;
#6112=ORIENTED_EDGE ( 'NONE', *, *, #31657, .T. ) ;
#6113=B_SPLINE_CURVE_WITH_KNOTS ( 'NONE', 3,
 ( #27709, #27513, #12285, #24841 ),
 .UNSPECIFIED., .F., .F.,
 ( 4, 4 ),
 ( 0.8401805954000729493, 1.000000000000000000 ),
 .UNSPECIFIED. ) ;
#6119=ORIENTED_EDGE ( 'NONE', *, *, #20219, .T. ) ;
#6120=CARTESIAN_POINT ( 'NONE',  ( 0.1707094546937565349, -1.571949860022747947, -0.3635054096306748472 ) ) ;
#6133=VECTOR ( 'NONE', #40392, 39.37007874015748143 ) ;
#6134=CARTESIAN_POINT ( 'NONE',  ( 0.07652314640226315356, -2.046395885474036724, -0.6781094798170426152 ) ) ;
#6138=B_SPLINE_CURVE_WITH_KNOTS ( 'NONE', 3,
 ( #28990, #12971, #16447, #25103, #12546, #10840 ),
 .UNSPECIFIED., .F., .F.,
 ( 4, 2, 4 ),
 ( 7.983724395024593614E-16, 0.0005669661630755714037, 0.001133932326150344401 ),
 .UNSPECIFIED. ) ;
#6141=CARTESIAN_POINT ( 'NONE',  ( 0.5763338155049589906, -1.566475856062379934, -0.5858421376246120138 ) ) ;
#6142=EDGE_CURVE ( 'NONE', #13011, #28606, #23642, .T. ) ;
#6146=TOROIDAL_SURFACE ( 'NONE', #39651, 0.05000000000000000971, 0.2000000000000000111 ) ;
#6147=CARTESIAN_POINT ( 'NONE',  ( 0.1726184415752066714, -1.824553594176122617, -0.6822955034825700649 ) ) ;
#6148=CARTESIAN_POINT ( 'NONE',  ( 0.2059273467974227778, -1.283046334493782803, -0.2869361388274796476 ) ) ;
#6150=AXIS2_PLACEMENT_3D ( 'NONE', #19812, #36053, #7453 ) ;
#6156=DIRECTION ( 'NONE',  ( 0.4999551463232373427, -0.8660512985181134660, 0.000000000000000000 ) ) ;
#6160=VECTOR ( 'NONE', #31393, 39.37007874015748143 ) ;
#6168=DIRECTION ( 'NONE',  ( 0.8660512985181135770, 0.4999551463232370652, 0.000000000000000000 ) ) ;
#6169=CARTESIAN_POINT ( 'NONE',  ( 0.4109281692855286106, -1.716037778611097409, -0.4237749387638956033 ) ) ;
#6173=CARTESIAN_POINT ( 'NONE',  ( 0.4159916692016358830, -1.069406866067976081, -0.5155029497116575543 ) ) ;
#6180=EDGE_CURVE ( 'NONE', #25148, #39255, #38117, .T. ) ;
#6201=CARTESIAN_POINT ( 'NONE',  ( 0.3706793757908085074, -1.615012852715396408, -0.4172838525897036854 ) ) ;
#6227=CARTESIAN_POINT ( 'NONE',  ( 0.6421235886874124832, -1.453936924866673364, -0.6328608320660102926 ) ) ;
#6251=ORIENTED_EDGE ( 'NONE', *, *, #22501, .F. ) ;
#6262=CARTESIAN_POINT ( 'NONE',  ( 0.3592281729446684113, -1.923857150176657260, -0.3319732337371206765 ) ) ;
#6273=DIRECTION ( 'NONE',  ( 0.000000000000000000, 0.4798762827498445072, -0.8773361688966159200 ) ) ;
#6277=CARTESIAN_POINT ( 'NONE',  ( 0.5184883810048313002, -1.679943727288017552, -0.5950377653840827064 ) ) ;
#6281=CARTESIAN_POINT ( 'NONE',  ( 0.3925781617411475133, -1.721137056870122750, -0.3057750134661929020 ) ) ;
#6287=CARTESIAN_POINT ( 'NONE',  ( 0.6394081393571972027, -1.397021802722361095, -0.6249999999999998890 ) ) ;
#6288=PLANE ( 'NONE',  #13537 ) ;
#6292=CIRCLE ( 'NONE', #35848, 0.1033070866141732880 ) ;
#6293=CARTESIAN_POINT ( 'NONE',  ( 0.6436032348275867454, -1.487421782847565321, -0.4117819510330663624 ) ) ;
#6295=CARTESIAN_POINT ( 'NONE',  ( 0.3986316166335497901, -2.053829379683854039, -0.4777570796616223414 ) ) ;
#6298=DIRECTION ( 'NONE',  ( 0.000000000000000000, 0.000000000000000000, -1.000000000000000000 ) ) ;
#6301=CARTESIAN_POINT ( 'NONE',  ( 0.3630210457930825307, -1.758320821885930751, -0.4950703529717556117 ) ) ;
#6302=CARTESIAN_POINT ( 'NONE',  ( 0.4001970250685381592, -1.597972868323746187, -0.4118702688307778192 ) ) ;
#6305=DIRECTION ( 'NONE',  ( 1.060606950627616773E-16, 6.122684696619993730E-17, 1.000000000000000000 ) ) ;
#6307=VERTEX_POINT ( 'NONE', #29477 ) ;
#6308=CARTESIAN_POINT ( 'NONE',  ( 0.3795613398208534384, -1.760143698493221942, -0.5723197561600823491 ) ) ;
#6311=CARTESIAN_POINT ( 'NONE',  ( 0.5264113014007612001, -1.640729993778266893, -0.5166151207188711680 ) ) ;
#6314=ORIENTED_EDGE ( 'NONE', *, *, #6683, .T. ) ;
#6323=CARTESIAN_POINT ( 'NONE',  ( 0.3543078412078040085, -1.629008732304762397, -0.3717187814789204570 ) ) ;
#6335=CARTESIAN_POINT ( 'NONE',  ( 0.07251299243635034308, -1.415239065497081006, -0.3692912077930444736 ) ) ;
#6336=CARTESIAN_POINT ( 'NONE',  ( 0.5872629042297322632, -1.489983250153556815, -0.4326885114256821541 ) ) ;
#6338=CIRCLE ( 'NONE', #11613, 0.2500000000000000000 ) ;
#6340=CARTESIAN_POINT ( 'NONE',  ( 0.2110034642138055860, -1.187742706213460453, -0.5155029497116575543 ) ) ;
#6342=DIRECTION ( 'NONE',  ( -0.8660512985181141321, -0.4999551463232362325, 0.000000000000000000 ) ) ;
#6350=FACE_OUTER_BOUND ( 'NONE', #13855, .T. ) ;
#6351=CARTESIAN_POINT ( 'NONE',  ( 0.1945550857237052511, -2.003382580491667841, -0.7031198838846081101 ) ) ;
#6361=CARTESIAN_POINT ( 'NONE',  ( 0.5215316005982619796, -1.181669392490712456, -0.6250000000000000000 ) ) ;
#6363=EDGE_CURVE ( 'NONE', #14915, #6802, #30009, .T. ) ;
#6373=CARTESIAN_POINT ( 'NONE',  ( 0.3695052819757340123, -1.758428263776099287, -0.4278193900811940176 ) ) ;
#6374=CARTESIAN_POINT ( 'NONE',  ( 0.5849095050029387011, -1.491341823319836335, -0.5960747874205124530 ) ) ;
#6376=CARTESIAN_POINT ( 'NONE',  ( 0.4100456123093286775, -1.725225710419908243, -0.4268450903248972028 ) ) ;
#6379=FACE_OUTER_BOUND ( 'NONE', #9022, .T. ) ;
#6383=ADVANCED_FACE ( 'NONE', ( #4978 ), #26914, .F. ) ;
#6391=DIRECTION ( 'NONE',  ( -0.000000000000000000, 0.9679004486746793923, 0.2513338844154409668 ) ) ;
#6400=CARTESIAN_POINT ( 'NONE',  ( 0.3402612271582353687, -1.674021245575775696, -0.3988557406434431463 ) ) ;
#6401=ORIENTED_EDGE ( 'NONE', *, *, #21504, .F. ) ;
#6402=DIRECTION ( 'NONE',  ( 0.8660512985181129109, 0.4999551463232381199, 0.000000000000000000 ) ) ;
#6407=ORIENTED_EDGE ( 'NONE', *, *, #32103, .T. ) ;
#6418=CARTESIAN_POINT ( 'NONE',  ( 0.1757500541653520820, -1.230771478115229245, -0.2869361388274796476 ) ) ;
#6420=CARTESIAN_POINT ( 'NONE',  ( 0.5802494246892667684, -1.607235576111437636, -0.5644493929225152806 ) ) ;
#6423=ORIENTED_EDGE ( 'NONE', *, *, #15220, .T. ) ;
#6428=DIRECTION ( 'NONE',  ( -0.4999551463232362325, 0.8660512985181140211, 0.000000000000000000 ) ) ;
#6454=B_SPLINE_CURVE_WITH_KNOTS ( 'NONE', 3,
 ( #32299, #22267, #10501, #25748 ),
 .UNSPECIFIED., .F., .F.,
 ( 4, 4 ),
 ( 3.576224061345491846E-18, 0.003042297940109665259 ),
 .UNSPECIFIED. ) ;
#6455=CARTESIAN_POINT ( 'NONE',  ( 0.2655705318850531960, -1.562522136089427471, -0.3463398766974524201 ) ) ;
#6459=ORIENTED_EDGE ( 'NONE', *, *, #6660, .F. ) ;
#6462=VERTEX_POINT ( 'NONE', #31104 ) ;
#6468=EDGE_CURVE ( 'NONE', #34414, #6462, #38538, .T. ) ;
#6471=CARTESIAN_POINT ( 'NONE',  ( 0.4173105138104912237, -1.590421242443905037, -0.4142386051757726007 ) ) ;
#6474=DIRECTION ( 'NONE',  ( 0.8660512985181134660, 0.4999551463232371207, 0.000000000000000000 ) ) ;
#6476=CARTESIAN_POINT ( 'NONE',  ( 0.4298148400247139844, -1.697909782648775678, -0.5124330163259216420 ) ) ;
#6486=CARTESIAN_POINT ( 'NONE',  ( 0.5936523516255933774, -1.587486488880259339, -0.4320271970693849717 ) ) ;
#6487=DIRECTION ( 'NONE',  ( 0.000000000000000000, 4.966996352116840709E-15, -1.000000000000000000 ) ) ;
#6490=CARTESIAN_POINT ( 'NONE',  ( 0.1909286924077255587, -1.257064795538239022, -0.6485234391946320676 ) ) ;
#6494=CARTESIAN_POINT ( 'NONE',  ( 0.3660575152562974277, -2.015971804995021710, -0.5197529562823309801 ) ) ;
#6495=ADVANCED_FACE ( 'NONE', ( #40557 ), #30039, .F. ) ;
#6500=CARTESIAN_POINT ( 'NONE',  ( 0.3903816190474082570, -1.614399842932418894, -0.6685306478358077342 ) ) ;
#6512=EDGE_LOOP ( 'NONE', ( #29644, #31212, #38895, #20689, #19181, #3503, #25850, #15181, #28480 ) ) ;
#6516=CARTESIAN_POINT ( 'NONE',  ( 0.3475531016022769815, -1.635599610428785766, -0.3752212724818577705 ) ) ;
#6519=ORIENTED_EDGE ( 'NONE', *, *, #10978, .T. ) ;
#6522=ORIENTED_EDGE ( 'NONE', *, *, #16568, .F. ) ;
#6530=CARTESIAN_POINT ( 'NONE',  ( 0.3795613398208533273, -1.760143698493221942, -0.5723197561600822381 ) ) ;
#6534=CARTESIAN_POINT ( 'NONE',  ( 0.4167140344599875590, -1.721376155575082612, -0.4397180493288434522 ) ) ;
#6535=CARTESIAN_POINT ( 'NONE',  ( 0.3402623241359036266, -1.675594047157907163, -0.3998012311158237742 ) ) ;
#6544=CARTESIAN_POINT ( 'NONE',  ( 0.1747054245739551037, -1.734794744728702653, -0.6813247353107599880 ) ) ;
#6551=DIRECTION ( 'NONE',  ( 0.000000000000000000, 0.000000000000000000, -1.000000000000000000 ) ) ;
#6562=CARTESIAN_POINT ( 'NONE',  ( 0.4264202721361134985, -1.467519734074643534, -0.5166151207188711680 ) ) ;
#6563=CARTESIAN_POINT ( 'NONE',  ( 0.3857322640002042169, -1.760817745270522039, -0.4634799128580170957 ) ) ;
#6566=ORIENTED_EDGE ( 'NONE', *, *, #24850, .F. ) ;
#6568=CARTESIAN_POINT ( 'NONE',  ( 0.4724132931814642444, -1.077943426954374395, -0.4216967736820900203 ) ) ;
#6594=CARTESIAN_POINT ( 'NONE',  ( 0.5024525556466100662, -1.651954489456844533, -0.4338784509423143088 ) ) ;
#6596=B_SPLINE_CURVE_WITH_KNOTS ( 'NONE', 3,
 ( #19845, #13664, #4407, #26229 ),
 .UNSPECIFIED., .F., .F.,
 ( 4, 4 ),
 ( 3.127317220692750759E-18, 0.0003263726155883022958 ),
 .UNSPECIFIED. ) ;
#6599=CARTESIAN_POINT ( 'NONE',  ( 0.5122377810313424318, -1.683552081238520293, -0.5849915292415723833 ) ) ;
#6601=CARTESIAN_POINT ( 'NONE',  ( 0.6129759397991038083, -1.613544640311175948, -0.5428363245105037871 ) ) ;
#6605=ORIENTED_EDGE ( 'NONE', *, *, #18805, .T. ) ;
#6610=CARTESIAN_POINT ( 'NONE',  ( 0.6248336632338993279, -1.524278534507916172, -0.6328788536102397666 ) ) ;
#6618=DIRECTION ( 'NONE',  ( 0.8660512985181131329, 0.4999551463232377313, 0.000000000000000000 ) ) ;
#6627=EDGE_CURVE ( 'NONE', #32971, #38598, #6454, .T. ) ;
#6629=B_SPLINE_CURVE_WITH_KNOTS ( 'NONE', 3,
 ( #31788, #6471, #34461, #37531 ),
 .UNSPECIFIED., .F., .F.,
 ( 4, 4 ),
 ( 0.0009402988323797356694, 0.001215464345533929895 ),
 .UNSPECIFIED. ) ;
#6639=ORIENTED_EDGE ( 'NONE', *, *, #27778, .T. ) ;
#6648=EDGE_LOOP ( 'NONE', ( #34442, #32987, #10522, #23931 ) ) ;
#6652=CARTESIAN_POINT ( 'NONE',  ( 0.2190497394446654089, -1.621418830003412692, -0.3569805845145136436 ) ) ;
#6655=CARTESIAN_POINT ( 'NONE',  ( -2.112273405726188513E-14, -1.835409001655643690, -0.3543101909453316156 ) ) ;
#6659=ORIENTED_EDGE ( 'NONE', *, *, #15454, .T. ) ;
#6660=EDGE_CURVE ( 'NONE', #23858, #24493, #23171, .T. ) ;
#6671=CARTESIAN_POINT ( 'NONE',  ( 0.1996203293408511381, -2.065051801937105136, -0.7178016293569640105 ) ) ;
#6675=EDGE_CURVE ( 'NONE', #24795, #7643, #20858, .T. ) ;
#6676=AXIS2_PLACEMENT_3D ( 'NONE', #18944, #31479, #3287 ) ;
#6682=FACE_OUTER_BOUND ( 'NONE', #34141, .T. ) ;
#6683=EDGE_CURVE ( 'NONE', #20307, #8639, #15593, .T. ) ;
#6685=DIRECTION ( 'NONE',  ( 0.8057988841560899118, 0.4797014836779449065, -0.3472385993088597522 ) ) ;
#6697=DIRECTION ( 'NONE',  ( 0.8660512985181135770, 0.4999551463232370652, 0.000000000000000000 ) ) ;
#6700=EDGE_LOOP ( 'NONE', ( #17042, #6605, #14826, #1637, #26228, #39614, #12098, #5502 ) ) ;
#6703=( BOUNDED_SURFACE ( )  B_SPLINE_SURFACE ( 3, 2, ( 
 ( #8152, #38803, #39235 ),
 ( #13716, #32650, #4455 ),
 ( #23427, #1815, #35945 ),
 ( #11057, #7751, #20315 ),
 ( #32836, #4643, #17217 ),
 ( #23615, #29762, #7939 ),
 ( #20514, #4852, #39422 ),
 ( #11243, #23815, #36335 ) ),
 .UNSPECIFIED., .F., .F., .T. ) 
 B_SPLINE_SURFACE_WITH_KNOTS ( ( 4, 2, 2, 4 ),
 ( 3, 3 ),
 ( 0.000000000000000000, 0.0009689511937531078639, 0.001453426790629661850, 0.001937902387506215728 ),
 ( 0.000000000000000000, 1.000000000000000000 ),
 .UNSPECIFIED. ) 
 GEOMETRIC_REPRESENTATION_ITEM ( )  RATIONAL_B_SPLINE_SURFACE ( (
 ( 1.000000000000000000, 0.7071067811865507924, 1.000000000000000000),
 ( 1.000000000000000000, 0.7661883050553089936, 1.000000000000000000),
 ( 1.000000000000000000, 0.8090289802883275927, 1.000000000000000000),
 ( 1.000000000000000000, 0.8549856046166490753, 1.000000000000000000),
 ( 1.000000000000000000, 0.8668418550465033512, 1.000000000000000000),
 ( 1.000000000000000000, 0.8822522463525879211, 1.000000000000000000),
 ( 1.000000000000000000, 0.8856360263997571369, 1.000000000000000000),
 ( 1.000000000000000000, 0.8847557669246132184, 1.000000000000000000) ) ) 
 REPRESENTATION_ITEM ( '' )  SURFACE ( )  );
#6707=DIRECTION ( 'NONE',  ( 1.000000000000000000, 0.000000000000000000, 0.000000000000000000 ) ) ;
#6715=ORIENTED_EDGE ( 'NONE', *, *, #766, .T. ) ;
#6719=CARTESIAN_POINT ( 'NONE',  ( 0.1734973056165642902, -1.209394307038482497, -0.5155029497116575543 ) ) ;
#6722=ORIENTED_EDGE ( 'NONE', *, *, #12462, .T. ) ;
#6730=CARTESIAN_POINT ( 'NONE',  ( 0.4159916692016358830, -1.069406866067976081, -0.5155029497116575543 ) ) ;
#6735=CARTESIAN_POINT ( 'NONE',  ( 0.3827795040295842166, -1.762256314311558603, -0.5556587900919752743 ) ) ;
#6738=CARTESIAN_POINT ( 'NONE',  ( 0.3967399397739009292, -2.017252274505498821, -0.7078152146948345491 ) ) ;
#6756=ORIENTED_EDGE ( 'NONE', *, *, #15580, .T. ) ;
#6759=AXIS2_PLACEMENT_3D ( 'NONE', #10046, #7139, #22828 ) ;
#6761=LINE ( 'NONE', #19544, #20628 ) ;
#6762=ORIENTED_EDGE ( 'NONE', *, *, #18805, .F. ) ;
#6770=CARTESIAN_POINT ( 'NONE',  ( 0.2059273467974226113, -1.283046334493782803, -0.3194715457588298557 ) ) ;
#6773=CARTESIAN_POINT ( 'NONE',  ( 0.009624474380123570691, -1.740256400171903861, -0.3645574449919975479 ) ) ;
#6790=CIRCLE ( 'NONE', #33078, 0.1999999999999999833 ) ;
#6793=CARTESIAN_POINT ( 'NONE',  ( 0.1778100121041887027, -1.872358142960663496, -0.6552623532412349405 ) ) ;
#6797=CARTESIAN_POINT ( 'NONE',  ( 0.3711309917658967561, -1.727276130344147509, -0.6834503960384243904 ) ) ;
#6800=VECTOR ( 'NONE', #3027, 39.37007874015748854 ) ;
#6802=VERTEX_POINT ( 'NONE', #14199 ) ;
#6805=CARTESIAN_POINT ( 'NONE',  ( 0.4463968940846189670, -1.144227781936946409, -0.6446835755021989023 ) ) ;
#6809=CARTESIAN_POINT ( 'NONE',  ( 0.4942350278003149744, -1.646331289742994031, -0.4039250241487104542 ) ) ;
#6811=ORIENTED_EDGE ( 'NONE', *, *, #11100, .F. ) ;
#6814=ORIENTED_EDGE ( 'NONE', *, *, #30517, .F. ) ;
#6816=CARTESIAN_POINT ( 'NONE',  ( 0.3665972292190579074, -1.767090988255677342, -0.5848990675856741150 ) ) ;
#6817=CARTESIAN_POINT ( 'NONE',  ( -2.115421433687637455E-14, -2.107936428766274073, -0.7005084057759867200 ) ) ;
#6824=CIRCLE ( 'NONE', #31802, 0.05000000000000000971 ) ;
#6826=CARTESIAN_POINT ( 'NONE',  ( 0.6505092258671375527, -1.603730573490085964, -0.4546931408925402041 ) ) ;
#6837=CARTESIAN_POINT ( 'NONE',  ( 0.4726289841176697371, -1.127529792599587299, -0.3806505246460042957 ) ) ;
#6843=AXIS2_PLACEMENT_3D ( 'NONE', #5677, #18231, #27905 ) ;
#6855=EDGE_CURVE ( 'NONE', #19345, #19020, #22455, .T. ) ;
#6860=ADVANCED_FACE ( 'NONE', ( #10921 ), #39696, .F. ) ;
#6862=DIRECTION ( 'NONE',  ( 0.4999551463232373427, -0.8660512985181134660, 0.000000000000000000 ) ) ;
#6864=EDGE_CURVE ( 'NONE', #17453, #26250, #40070, .T. ) ;
#6890=AXIS2_PLACEMENT_3D ( 'NONE', #1512, #39140, #36042 ) ;
#6896=CARTESIAN_POINT ( 'NONE',  ( 0.3923243630925510872, -1.966611948492501316, -0.4968729097670202544 ) ) ;
#6902=CARTESIAN_POINT ( 'NONE',  ( 0.3854517798335491685, -1.606485021356798937, -0.4131913823358430160 ) ) ;
#6904=DIRECTION ( 'NONE',  ( 0.4999551463232377313, -0.8660512985181132439, -0.000000000000000000 ) ) ;
#6913=DIRECTION ( 'NONE',  ( 0.4999551463232372317, -0.8660512985181135770, 0.000000000000000000 ) ) ;
#6914=ADVANCED_FACE ( 'NONE', ( #13987 ), #26766, .F. ) ;
#6917=DIRECTION ( 'NONE',  ( 0.8660512985181132439, 0.4999551463232376758, 0.000000000000000000 ) ) ;
#6924=ORIENTED_EDGE ( 'NONE', *, *, #1417, .F. ) ;
#6925=ORIENTED_EDGE ( 'NONE', *, *, #34633, .F. ) ;
#6930=EDGE_LOOP ( 'NONE', ( #24337, #3927, #17011, #4795, #304 ) ) ;
#6935=CARTESIAN_POINT ( 'NONE',  ( 0.3909832130543929307, -1.949124834775286974, -0.5003013863325592725 ) ) ;
#6939=CARTESIAN_POINT ( 'NONE',  ( 0.4334910933930137267, -1.677114403799170317, -0.6121645795958546854 ) ) ;
#6941=CARTESIAN_POINT ( 'NONE',  ( 0.09999999999997892519, -2.097675824466505023, -0.2588528740066098344 ) ) ;
#6946=CARTESIAN_POINT ( 'NONE',  ( 0.1934531163328969683, -1.995776386748306486, -0.7016548334849427304 ) ) ;
#6948=CARTESIAN_POINT ( 'NONE',  ( 0.3604846637226567507, -1.752356493123346182, -0.4785798120827651769 ) ) ;
#6951=CARTESIAN_POINT ( 'NONE',  ( 0.6409176605149490280, -1.402773510675777935, -0.6244726438235953525 ) ) ;
#6957=( BOUNDED_SURFACE ( )  B_SPLINE_SURFACE ( 3, 2, ( 
 ( #29468, #20414, #36236 ),
 ( #4751, #26602, #11349 ),
 ( #39519, #7440, #7656 ),
 ( #20627, #14237, #32545 ) ),
 .UNSPECIFIED., .F., .F., .T. ) 
 B_SPLINE_SURFACE_WITH_KNOTS ( ( 4, 4 ),
 ( 3, 3 ),
 ( -2.862293735361731706E-17, 0.001825051142017924174 ),
 ( 0.000000000000000000, 1.000000000000000000 ),
 .UNSPECIFIED. ) 
 GEOMETRIC_REPRESENTATION_ITEM ( )  RATIONAL_B_SPLINE_SURFACE ( (
 ( 1.000000000000000000, 0.7061763356917307721, 1.000000000000000000),
 ( 1.000000000000000000, 0.7067362331337568859, 1.000000000000000000),
 ( 1.000000000000000000, 0.7071034392571956539, 1.000000000000000000),
 ( 1.000000000000000000, 0.7071067811865460184, 1.000000000000000000) ) ) 
 REPRESENTATION_ITEM ( '' )  SURFACE ( )  );
#6960=CARTESIAN_POINT ( 'NONE',  ( 0.2410612609043008003, -1.582380839801596828, -0.7041768810579421833 ) ) ;
#6964=ORIENTED_EDGE ( 'NONE', *, *, #11506, .F. ) ;
#6966=CARTESIAN_POINT ( 'NONE',  ( 0.3770485601393582797, -1.761594279002118402, -0.5750035625930455252 ) ) ;
#6980=CARTESIAN_POINT ( 'NONE',  ( 0.5403448000457757860, -1.667326427136834432, -0.4959994330086619496 ) ) ;
#6982=CARTESIAN_POINT ( 'NONE',  ( 0.5054609057099638258, -1.017757956463559710, -0.5155029497116575543 ) ) ;
#6985=CARTESIAN_POINT ( 'NONE',  ( 0.03025250162251530775, -1.950833258820844129, -0.3011725134765823597 ) ) ;
#6987=ORIENTED_EDGE ( 'NONE', *, *, #29094, .T. ) ;
#6988=DIRECTION ( 'NONE',  ( 0.000000000000000000, 0.000000000000000000, -1.000000000000000000 ) ) ;
#6997=CARTESIAN_POINT ( 'NONE',  ( 0.1959265899308195724, -1.288818386415671036, -0.7414046965098800568 ) ) ;
#7000=CARTESIAN_POINT ( 'NONE',  ( 0.4409894265177971562, -1.112709430993880755, -0.5155029497116575543 ) ) ;
#7001=EDGE_CURVE ( 'NONE', #19341, #24493, #31029, .T. ) ;
#7007=CARTESIAN_POINT ( 'NONE',  ( 0.1935645654550193218, -1.998378335482414947, -0.6716191072629904557 ) ) ;
#7010=FACE_OUTER_BOUND ( 'NONE', #2241, .T. ) ;
#7012=DIRECTION ( 'NONE',  ( -0.6036887133119795967, -0.3484981542248280495, 0.7170139286803393075 ) ) ;
#7018=EDGE_CURVE ( 'NONE', #32180, #5888, #31628, .T. ) ;
#7021=ORIENTED_EDGE ( 'NONE', *, *, #16097, .T. ) ;
#7036=ORIENTED_EDGE ( 'NONE', *, *, #7706, .T. ) ;
#7037=CARTESIAN_POINT ( 'NONE',  ( 0.6299594025232742034, -1.615593600489037884, -0.5387823541095865254 ) ) ;
#7042=CARTESIAN_POINT ( 'NONE',  ( 0.4955364640417493360, -1.624781976271624462, -0.5908697979789261368 ) ) ;
#7046=CARTESIAN_POINT ( 'NONE',  ( 0.4546139439372508528, -1.086704419948380851, -0.6194763249030063035 ) ) ;
#7051=CARTESIAN_POINT ( 'NONE',  ( 0.4795819664771984736, -1.106247336020415917, -0.4111404562665418871 ) ) ;
#7054=VERTEX_POINT ( 'NONE', #37013 ) ;
#7055=CARTESIAN_POINT ( 'NONE',  ( 0.5489247571685185179, -1.593093418273787254, -0.5155029497116575543 ) ) ;
#7065=ORIENTED_EDGE ( 'NONE', *, *, #2465, .F. ) ;
#7072=CARTESIAN_POINT ( 'NONE',  ( 0.5288925617653345013, -1.600649924176790417, -0.4348607546581709227 ) ) ;
#7076=ADVANCED_FACE ( 'NONE', ( #8836 ), #1709, .T. ) ;
#7078=B_SPLINE_CURVE_WITH_KNOTS ( 'NONE', 3,
 ( #24023, #1602, #24216, #26480 ),
 .UNSPECIFIED., .F., .F.,
 ( 4, 4 ),
 ( 1.063271609842796554E-14, 0.0008871692367504230205 ),
 .UNSPECIFIED. ) ;
#7081=CARTESIAN_POINT ( 'NONE',  ( 0.4741640079579751421, -1.162838329081267830, -0.4122610257295771796 ) ) ;
#7083=CIRCLE ( 'NONE', #25500, 0.1700000000000001510 ) ;
#7094=DIRECTION ( 'NONE',  ( 0.4999551463232385085, -0.8660512985181127998, 0.000000000000000000 ) ) ;
#7095=CARTESIAN_POINT ( 'NONE',  ( 0.4165289612193914248, -1.649214957849692187, -0.4090022746516587815 ) ) ;
#7113=ORIENTED_EDGE ( 'NONE', *, *, #16045, .T. ) ;
#7125=CARTESIAN_POINT ( 'NONE',  ( 0.4768809664655372926, -1.091612543784717282, -0.6129809598074057453 ) ) ;
#7134=CARTESIAN_POINT ( 'NONE',  ( 0.3881547982128820684, -1.813545243782807459, -0.6998239732715378913 ) ) ;
#7135=CYLINDRICAL_SURFACE ( 'NONE', #30605, 0.04330708661417343591 ) ;
#7138=ADVANCED_FACE ( 'NONE', ( #22628 ), #35162, .F. ) ;
#7139=DIRECTION ( 'NONE',  ( 0.4999551463232372872, -0.8660512985181134660, 0.000000000000000000 ) ) ;
#7140=CARTESIAN_POINT ( 'NONE',  ( 0.2059273467974224725, -1.283046334493782137, -0.3824824602286829855 ) ) ;
#7148=FACE_OUTER_BOUND ( 'NONE', #26843, .T. ) ;
#7152=EDGE_CURVE ( 'NONE', #8912, #39763, #9946, .T. ) ;
#7154=ORIENTED_EDGE ( 'NONE', *, *, #39340, .T. ) ;
#7161=CARTESIAN_POINT ( 'NONE',  ( 0.3798092287356915620, -1.663952012720910867, -0.6129662916473187506 ) ) ;
#7170=CARTESIAN_POINT ( 'NONE',  ( -2.097120186386331940E-14, -2.097675824466503691, -0.2907077406111385764 ) ) ;
#7183=FACE_OUTER_BOUND ( 'NONE', #14095, .T. ) ;
#7189=B_SPLINE_CURVE_WITH_KNOTS ( 'NONE', 3,
 ( #23881, #2056, #1470, #11114, #39694, #7613, #36409, #20184 ),
 .UNSPECIFIED., .F., .F.,
 ( 4, 2, 2, 4 ),
 ( -5.999999998886577302E-08, 0.0008460481067746681693, 0.001692156213549325357, 0.003384372427098619133 ),
 .UNSPECIFIED. ) ;
#7190=CARTESIAN_POINT ( 'NONE',  ( 0.2093553890865970102, -1.281067390074186907, -0.7153666112938229515 ) ) ;
#7193=CARTESIAN_POINT ( 'NONE',  ( 0.4189043378923988370, -1.737431724743732753, -0.5872665585884508932 ) ) ;
#7196=EDGE_CURVE ( 'NONE', #33728, #26101, #27098, .T. ) ;
#7204=ORIENTED_EDGE ( 'NONE', *, *, #766, .F. ) ;
#7212=CARTESIAN_POINT ( 'NONE',  ( 0.6099797830822989431, -1.615543353997655585, -0.5095064010331072923 ) ) ;
#7220=CARTESIAN_POINT ( 'NONE',  ( 0.3484951945142048535, -1.627819363848378220, -0.3328913857909800433 ) ) ;
#7226=CARTESIAN_POINT ( 'NONE',  ( 0.4992403769284946558, -1.623239255310001683, -0.5868208237444024755 ) ) ;
#7241=CARTESIAN_POINT ( 'NONE',  ( 0.3999999999999786504, -1.973385418564556293, -0.6834611762463905782 ) ) ;
#7250=ORIENTED_EDGE ( 'NONE', *, *, #14485, .F. ) ;
#7255=CARTESIAN_POINT ( 'NONE',  ( 0.3798059133362846063, -1.714498463400732309, -0.3386984188363488801 ) ) ;
#7257=CARTESIAN_POINT ( 'NONE',  ( 0.2284923717121199460, -1.304659949875474068, -0.5155029497116575543 ) ) ;
#7263=CARTESIAN_POINT ( 'NONE',  ( 0.5092518242376296023, -1.618326942756133979, -0.4583555508459725147 ) ) ;
#7279=CARTESIAN_POINT ( 'NONE',  ( 0.4079890870890051091, -1.708188938037489502, -0.6405138877632798877 ) ) ;
#7283=CARTESIAN_POINT ( 'NONE',  ( 0.5190464946628291498, -1.673342222487466779, -0.5944019783408716062 ) ) ;
#7300=CARTESIAN_POINT ( 'NONE',  ( 0.2914323826288400254, -1.233685883474753497, -0.5166151207188711680 ) ) ;
#7305=CARTESIAN_POINT ( 'NONE',  ( 0.5741821450848180186, -1.541683553717290600, -0.4860598978662519221 ) ) ;
#7306=ORIENTED_EDGE ( 'NONE', *, *, #15369, .T. ) ;
#7310=AXIS2_PLACEMENT_3D ( 'NONE', #3145, #34801, #18983 ) ;
#7315=EDGE_LOOP ( 'NONE', ( #13245, #3189, #33725, #30858 ) ) ;
#7322=CYLINDRICAL_SURFACE ( 'NONE', #34280, 0.04330708661417322775 ) ;
#7324=CARTESIAN_POINT ( 'NONE',  ( 0.4093192649698303431, -1.477391824278450061, -0.5625509170971494388 ) ) ;
#7328=CARTESIAN_POINT ( 'NONE',  ( 0.3896220963715341101, -1.743012515435767407, -0.7180593106334604014 ) ) ;
#7330=DIRECTION ( 'NONE',  ( 0.8660512985181132439, 0.4999551463232376203, 0.000000000000000000 ) ) ;
#7333=CARTESIAN_POINT ( 'NONE',  ( 0.6246939234061054114, -1.524535107703195003, -0.6328271379228022075 ) ) ;
#7342=CARTESIAN_POINT ( 'NONE',  ( 0.5693027582541522191, -1.577552960580653307, -0.4686421343491008473 ) ) ;
#7346=CARTESIAN_POINT ( 'NONE',  ( 0.1993688661005383334, -1.286831035182783634, -0.2901530652563581447 ) ) ;
#7362=ORIENTED_EDGE ( 'NONE', *, *, #31902, .T. ) ;
#7368=CIRCLE ( 'NONE', #29085, 0.1700000000000000400 ) ;
#7369=CARTESIAN_POINT ( 'NONE',  ( 0.01299436802863446032, -1.701590229751596572, -0.3397165561182163285 ) ) ;
#7370=ORIENTED_EDGE ( 'NONE', *, *, #15151, .F. ) ;
#7371=EDGE_CURVE ( 'NONE', #13497, #29847, #26955, .T. ) ;
#7372=FACE_OUTER_BOUND ( 'NONE', #16441, .T. ) ;
#7375=CARTESIAN_POINT ( 'NONE',  ( 0.7009661026058806588, -1.563056106223301045, -0.5155029497116575543 ) ) ;
#7379=CIRCLE ( 'NONE', #30394, 0.03000000000000005440 ) ;
#7391=CARTESIAN_POINT ( 'NONE',  ( 0.1890382415369475377, -1.253790046906361422, -0.3976186731358027915 ) ) ;
#7392=CARTESIAN_POINT ( 'NONE',  ( 0.2332815142676702147, -1.595247443236931462, -0.6698052276397686855 ) ) ;
#7394=CARTESIAN_POINT ( 'NONE',  ( 0.3783141089212034291, -1.720060367475409135, -0.4893959057094034448 ) ) ;
#7408=VECTOR ( 'NONE', #20020, 39.37007874015748143 ) ;
#7413=ORIENTED_EDGE ( 'NONE', *, *, #16964, .T. ) ;
#7415=CARTESIAN_POINT ( 'NONE',  ( 0.5328454728509273153, -1.654335657659062653, -0.4959994330086620051 ) ) ;
#7416=CARTESIAN_POINT ( 'NONE',  ( 0.6297115083997322227, -1.615736705109999782, -0.4933022779381483480 ) ) ;
#7432=DIRECTION ( 'NONE',  ( 0.8660512985181135770, 0.4999551463232370652, 0.000000000000000000 ) ) ;
#7440=CARTESIAN_POINT ( 'NONE',  ( 0.3999999999981719290, -2.080276347128062753, -0.2651857657968351156 ) ) ;
#7446=CARTESIAN_POINT ( 'NONE',  ( 0.4795062484387999646, -1.112529643762525611, -0.4042499308301856220 ) ) ;
#7453=DIRECTION ( 'NONE',  ( 1.000000000000000000, 0.000000000000000000, 0.000000000000000000 ) ) ;
#7469=EDGE_CURVE ( 'NONE', #2400, #29368, #23707, .T. ) ;
#7482=ORIENTED_EDGE ( 'NONE', *, *, #25745, .T. ) ;
#7493=AXIS2_PLACEMENT_3D ( 'NONE', #19820, #29686, #14254 ) ;
#7499=CARTESIAN_POINT ( 'NONE',  ( 0.4186432780919984720, -1.612034538517055360, -0.6668481824684697745 ) ) ;
#7515=DIRECTION ( 'NONE',  ( 0.8013552086938348085, 0.4626073089491885559, 0.3792417529835693801 ) ) ;
#7517=CARTESIAN_POINT ( 'NONE',  ( 0.4227944218364425577, -1.670731094902153213, -0.6342269662369710570 ) ) ;
#7524=CARTESIAN_POINT ( 'NONE',  ( 0.5777362523500105818, -1.534599504986668084, -0.5616871023379128580 ) ) ;
#7529=CIRCLE ( 'NONE', #12127, 0.2000000000000000666 ) ;
#7531=CIRCLE ( 'NONE', #27264, 0.02999999999999999195 ) ;
#7538=ORIENTED_EDGE ( 'NONE', *, *, #16685, .T. ) ;
#7539=CARTESIAN_POINT ( 'NONE',  ( 0.02999999999997886302, -2.183180860297921466, -0.4937760292030871079 ) ) ;
#7542=AXIS2_PLACEMENT_3D ( 'NONE', #2313, #20836, #39941 ) ;
#7556=FACE_OUTER_BOUND ( 'NONE', #39316, .T. ) ;
#7565=CARTESIAN_POINT ( 'NONE',  ( 0.5892429738200350986, -1.562419363825541918, -0.4777725863729586075 ) ) ;
#7573=EDGE_LOOP ( 'NONE', ( #31271, #25668, #9806, #477, #39063, #10346, #12761, #36300, #35977, #17559 ) ) ;
#7588=CARTESIAN_POINT ( 'NONE',  ( 0.07493559420041842611, -1.491955960748385657, -0.3421605232025932142 ) ) ;
#7589=VERTEX_POINT ( 'NONE', #38122 ) ;
#7593=CARTESIAN_POINT ( 'NONE',  ( 0.02333805985610111142, -1.614515438906713118, -0.6389321993329700744 ) ) ;
#7613=CARTESIAN_POINT ( 'NONE',  ( 0.3957164860440396392, -2.010354213676031065, -0.5038375161603109165 ) ) ;
#7618=DIRECTION ( 'NONE',  ( 1.000000000000000000, 0.000000000000000000, 0.000000000000000000 ) ) ;
#7629=AXIS2_PLACEMENT_3D ( 'NONE', #2760, #2971, #9322 ) ;
#7637=CARTESIAN_POINT ( 'NONE',  ( 0.3984114568195522010, -1.599003643269838904, -0.5155029497116575543 ) ) ;
#7639=CARTESIAN_POINT ( 'NONE',  ( 0.6215274601157204648, -1.354888019438377444, -0.6250000000000000000 ) ) ;
#7643=VERTEX_POINT ( 'NONE', #13397 ) ;
#7653=CIRCLE ( 'NONE', #14883, 0.1033070866141734129 ) ;
#7656=CARTESIAN_POINT ( 'NONE',  ( 0.3999999999999798161, -2.143572916703662123, -0.4549832530184109713 ) ) ;
#7662=CARTESIAN_POINT ( 'NONE',  ( 0.5804493474056371394, -1.147657283997232991, -0.5155029497116575543 ) ) ;
#7674=VERTEX_POINT ( 'NONE', #32717 ) ;
#7677=CARTESIAN_POINT ( 'NONE',  ( 0.6472550179972602624, -1.446945511653702443, -0.6249999999999998890 ) ) ;
#7684=CARTESIAN_POINT ( 'NONE',  ( 0.0004587754601000432132, -1.956353996556619457, -0.6605311053939741939 ) ) ;
#7696=DIRECTION ( 'NONE',  ( 0.4999551463232372317, -0.8660512985181135770, 0.000000000000000000 ) ) ;
#7698=VERTEX_POINT ( 'NONE', #17088 ) ;
#7699=CARTESIAN_POINT ( 'NONE',  ( 0.6554021398533210752, -1.532257051837409900, -0.6160679160980194746 ) ) ;
#7704=CARTESIAN_POINT ( 'NONE',  ( 0.3379549838205658796, -1.287644724967739629, -0.5155029497116575543 ) ) ;
#7706=EDGE_CURVE ( 'NONE', #19341, #5039, #3307, .T. ) ;
#7709=CARTESIAN_POINT ( 'NONE',  ( 0.07438451276000504486, -1.494117022116229654, -0.3422791976087487531 ) ) ;
#7710=CARTESIAN_POINT ( 'NONE',  ( 0.5424528042998149058, -1.629943420504956553, -0.5873670775642777508 ) ) ;
#7720=CARTESIAN_POINT ( 'NONE',  ( 0.02999999999990856162, -2.097674344635099608, -0.7286986457865541889 ) ) ;
#7726=CARTESIAN_POINT ( 'NONE',  ( 0.6627999150273293782, -1.460136208901648081, -0.4136584506876441747 ) ) ;
#7733=CARTESIAN_POINT ( 'NONE',  ( 0.5764814451414584928, -1.536917970227292596, -0.4740999583163317821 ) ) ;
#7735=EDGE_CURVE ( 'NONE', #23598, #17175, #34198, .T. ) ;
#7743=VERTEX_POINT ( 'NONE', #1478 ) ;
#7745=FACE_OUTER_BOUND ( 'NONE', #27632, .T. ) ;
#7749=DIRECTION ( 'NONE',  ( 1.060606950627616773E-16, 6.122684696619993730E-17, 1.000000000000000000 ) ) ;
#7751=CARTESIAN_POINT ( 'NONE',  ( 0.3885448048373752461, -1.754957712888778776, -0.4416481762448698500 ) ) ;
#7756=CARTESIAN_POINT ( 'NONE',  ( 0.1424029337235096226, -1.400533250147911746, -0.3244367222852112542 ) ) ;
#7757=DIRECTION ( 'NONE',  ( -0.4999551463232373427, 0.8660512985181134660, -0.000000000000000000 ) ) ;
#7759=CARTESIAN_POINT ( 'NONE',  ( 0.5794003230470022858, -1.608195470634162128, -0.5609915163756674650 ) ) ;
#7762=ADVANCED_FACE ( 'NONE', ( #17503 ), #19732, .F. ) ;
#7765=B_SPLINE_CURVE_WITH_KNOTS ( 'NONE', 3,
 ( #14444, #4990, #20647, #4387, #14052, #10556, #39350, #16747, #10987, #29484 ),
 .UNSPECIFIED., .F., .F.,
 ( 4, 2, 2, 2, 4 ),
 ( 1.734723475976807094E-18, 0.0006437901958235721887, 0.001287580391647142643, 0.001931370587470713097, 0.002575160783294283551 ),
 .UNSPECIFIED. ) ;
#7767=CARTESIAN_POINT ( 'NONE',  ( 0.5858181074991345438, -1.569584648740467214, -0.5056512426634341972 ) ) ;
#7772=ORIENTED_EDGE ( 'NONE', *, *, #26909, .T. ) ;
#7784=DIRECTION ( 'NONE',  ( 0.4999551463232373427, -0.8660512985181134660, 0.000000000000000000 ) ) ;
#7789=CARTESIAN_POINT ( 'NONE',  ( 0.1909286924077255587, -1.257064795538239022, -0.3194715457588295227 ) ) ;
#7791=CARTESIAN_POINT ( 'NONE',  ( 0.7009661026058806588, -1.563056106223301045, -0.5155029497116575543 ) ) ;
#7800=CARTESIAN_POINT ( 'NONE',  ( 0.5467981811930779923, -1.652054351292815637, -0.5405695263049933308 ) ) ;
#7826=CARTESIAN_POINT ( 'NONE',  ( 0.6143533635013058714, -1.612503925854076536, -0.4829043714737934478 ) ) ;
#7836=CARTESIAN_POINT ( 'NONE',  ( 0.5058599984363495450, -1.583313914148366752, -0.4933326546058600659 ) ) ;
#7845=DIRECTION ( 'NONE',  ( 0.4999551463232377313, -0.8660512985181132439, -0.000000000000000000 ) ) ;
#7851=ADVANCED_FACE ( 'NONE', ( #20387 ), #31122, .F. ) ;
#7853=CARTESIAN_POINT ( 'NONE',  ( 0.3866201621456603621, -1.651307175440333008, -0.6361171515213966954 ) ) ;
#7856=DIRECTION ( 'NONE',  ( -0.4999551463232373427, 0.8660512985181134660, -0.000000000000000000 ) ) ;
#7860=EDGE_LOOP ( 'NONE', ( #22294, #38142, #36932, #23149, #21116, #20476, #1631 ) ) ;
#7865=CARTESIAN_POINT ( 'NONE',  ( 0.1102165803549850082, -1.338154550093276773, -0.7053715155666281378 ) ) ;
#7885=CARTESIAN_POINT ( 'NONE',  ( 0.6428829812445570058, -1.575050579808648488, -0.6023022189774835944 ) ) ;
#7890=DIRECTION ( 'NONE',  ( -1.000000000000000000, 0.000000000000000000, 0.000000000000000000 ) ) ;
#7896=AXIS2_PLACEMENT_3D ( 'NONE', #26307, #4669, #13944 ) ;
#7899=CARTESIAN_POINT ( 'NONE',  ( 0.5484265422080265573, -1.662660989552970703, -0.5492187312042384750 ) ) ;
#7913=CARTESIAN_POINT ( 'NONE',  ( 0.6378052450953181074, -1.586953600521664010, -0.4356635440277025206 ) ) ;
#7928=CARTESIAN_POINT ( 'NONE',  ( 0.2180524034168905279, -1.623376798655958630, -0.3571287730820865702 ) ) ;
#7939=CARTESIAN_POINT ( 'NONE',  ( 0.3717319392551187152, -1.764663464368710910, -0.4441500688334885094 ) ) ;
#7946=CARTESIAN_POINT ( 'NONE',  ( 0.1809966328114128720, -1.222385076516254054, -0.5155029497116575543 ) ) ;
#7949=CARTESIAN_POINT ( 'NONE',  ( 0.5916862240641643789, -1.591472326627963119, -0.5949256914164438026 ) ) ;
#7957=CARTESIAN_POINT ( 'NONE',  ( 0.5713982549016157764, -1.545293902939492314, -0.5110934287108533924 ) ) ;
#7958=CARTESIAN_POINT ( 'NONE',  ( 0.4251784823825139337, -1.612149241703929148, -0.6654675560951863744 ) ) ;
#7968=AXIS2_PLACEMENT_3D ( 'NONE', #2978, #28079, #12424 ) ;
#7985=VERTEX_POINT ( 'NONE', #6361 ) ;
#7992=B_SPLINE_CURVE_WITH_KNOTS ( 'NONE', 3,
 ( #20095, #11218, #23784, #36305, #10412, #8127, #32206, #35920, #4021, #22972 ),
 .UNSPECIFIED., .F., .F.,
 ( 4, 2, 2, 2, 4 ),
 ( 0.000000000000000000, 0.0004226723285983043500, 0.0008453446571966087000, 0.001268016985794912996, 0.001690689314393217400 ),
 .UNSPECIFIED. ) ;
#8000=CARTESIAN_POINT ( 'NONE',  ( 0.4159916692016358830, -1.069406866067976081, -0.5155029497116575543 ) ) ;
#8009=ORIENTED_EDGE ( 'NONE', *, *, #32015, .T. ) ;
#8011=CARTESIAN_POINT ( 'NONE',  ( 0.4004245401938955617, -1.732304313445140576, -0.5960862704056979489 ) ) ;
#8017=VERTEX_POINT ( 'NONE', #12959 ) ;
#8026=SHAPE_REPRESENTATION ( 'Lower Pivot Bracket', ( #27819 ), #23225 ) ;
#8030=CARTESIAN_POINT ( 'NONE',  ( 0.4882254327172352304, -1.607754588109558069, -0.3920044576893668697 ) ) ;
#8039=B_SPLINE_SURFACE_WITH_KNOTS ( 'NONE', 3, 1, ( 
 ( #28395, #40534 ),
 ( #19143, #9064 ),
 ( #25321, #37861 ),
 ( #15842, #31290 ) ),
 .UNSPECIFIED., .F., .F., .F.,
 ( 4, 4 ),
 ( 2, 2 ),
 ( 0.000000000000000000, 1.000000000000000000 ),
 ( 0.000000000000000000, 1.000000000000000000 ),
 .UNSPECIFIED. ) ;
#8045=CARTESIAN_POINT ( 'NONE',  ( 0.3980399496921868674, -1.697909729581410954, -0.4245199042543691403 ) ) ;
#8062=B_SPLINE_CURVE_WITH_KNOTS ( 'NONE', 3,
 ( #35925, #16998, #29963, #20707, #20297, #39217, #20101, #5047 ),
 .UNSPECIFIED., .F., .F.,
 ( 4, 2, 2, 4 ),
 ( -2.312373376517052359E-05, 0.002683137465569600168, 0.004036268065236973783, 0.005389398664904348699 ),
 .UNSPECIFIED. ) ;
#8063=CARTESIAN_POINT ( 'NONE',  ( 0.3940698435746058381, -1.648959190003135511, -0.6369338832859893218 ) ) ;
#8064=DIRECTION ( 'NONE',  ( 0.4999551463232372317, -0.8660512985181133550, 0.000000000000000000 ) ) ;
#8067=CARTESIAN_POINT ( 'NONE',  ( 0.1909286924077255032, -1.257064795538239022, -0.7462941026102624109 ) ) ;
#8069=CARTESIAN_POINT ( 'NONE',  ( 0.2130735790700678256, -1.295425452470167604, -0.6217217108911923251 ) ) ;
#8077=CARTESIAN_POINT ( 'NONE',  ( 0.1462602504189297326, -1.332370281534213996, -0.7166700418499228897 ) ) ;
#8084=ORIENTED_EDGE ( 'NONE', *, *, #11441, .T. ) ;
#8085=CARTESIAN_POINT ( 'NONE',  ( 0.1999999999999794720, -2.107936428766273629, -0.2870436526301871627 ) ) ;
#8102=CARTESIAN_POINT ( 'NONE',  ( 0.4223102950200747219, -1.705408558797358864, -0.5055542070596241722 ) ) ;
#8105=CARTESIAN_POINT ( 'NONE',  ( 0.3699999999999787903, -2.097675824466503691, -0.4857926189863390753 ) ) ;
#8107=CARTESIAN_POINT ( 'NONE',  ( 0.1356432309609771070, -1.347689971048232627, -0.3196700151196194550 ) ) ;
#8112=EDGE_CURVE ( 'NONE', #37390, #29909, #34221, .T. ) ;
#8126=AXIS2_PLACEMENT_3D ( 'NONE', #7000, #25535, #19568 ) ;
#8127=CARTESIAN_POINT ( 'NONE',  ( 0.3840482169485068265, -1.614345010373418488, -0.3632487003279359916 ) ) ;
#8129=CARTESIAN_POINT ( 'NONE',  ( 0.1836898292508203356, -1.885732359905404332, -0.3111683550142131383 ) ) ;
#8132=DIRECTION ( 'NONE',  ( 0.4999551463232372872, -0.8660512985181134660, 0.000000000000000000 ) ) ;
#8133=CARTESIAN_POINT ( 'NONE',  ( 0.5846680594243126583, -1.499425989846573382, -0.5926635984244745803 ) ) ;
#8145=DIRECTION ( 'NONE',  ( 0.000000000000000000, 0.000000000000000000, -1.000000000000000000 ) ) ;
#8148=CARTESIAN_POINT ( 'NONE',  ( 0.3470125293659282462, -1.126547217955315539, -0.5155029497116575543 ) ) ;
#8152=CARTESIAN_POINT ( 'NONE',  ( 0.4100456123093288441, -1.725225710419908021, -0.4268450903248970363 ) ) ;
#8160=AXIS2_PLACEMENT_3D ( 'NONE', #28354, #224, #627 ) ;
#8163=CARTESIAN_POINT ( 'NONE',  ( 0.6253849347580197060, -1.612577459345563513, -0.5660843253017027177 ) ) ;
#8170=CARTESIAN_POINT ( 'NONE',  ( 0.5905302434980007620, -1.559944958562061723, -0.4720911378474059727 ) ) ;
#8191=CARTESIAN_POINT ( 'NONE',  ( 0.3616412802241143476, -1.759290408630900693, -0.5212859374495405484 ) ) ;
#8198=CARTESIAN_POINT ( 'NONE',  ( 0.1734515873220548177, -1.267154000006108339, -0.3263956774707204023 ) ) ;
#8201=CARTESIAN_POINT ( 'NONE',  ( 0.1870725001947720623, -1.259290933580937688, -0.7121575810423941277 ) ) ;
#8204=CARTESIAN_POINT ( 'NONE',  ( -2.112273405726188513E-14, -2.097675824466503691, -0.6968677163258658602 ) ) ;
#8207=AXIS2_PLACEMENT_3D ( 'NONE', #36891, #27851, #2551 ) ;
#8212=CARTESIAN_POINT ( 'NONE',  ( 0.5339261027788213543, -1.567111879318243473, -0.5155029497116575543 ) ) ;
#8229=ORIENTED_EDGE ( 'NONE', *, *, #34158, .T. ) ;
#8230=CARTESIAN_POINT ( 'NONE',  ( 0.4259907721281001036, -1.086727892038337417, -0.5155029497116575543 ) ) ;
#8233=ORIENTED_EDGE ( 'NONE', *, *, #20732, .T. ) ;
#8239=CARTESIAN_POINT ( 'NONE',  ( 0.2059273467974228888, -1.283046334493782803, -0.6919850938583151923 ) ) ;
#8241=CARTESIAN_POINT ( 'NONE',  ( 0.4822264149303859826, -1.608418054921360918, -0.3880980494168181361 ) ) ;
#8247=EDGE_LOOP ( 'NONE', ( #23635, #27944, #3244, #5910 ) ) ;
#8251=CIRCLE ( 'NONE', #17448, 0.05330708661417339622 ) ;
#8255=CARTESIAN_POINT ( 'NONE',  ( 0.02999864200428311450, -2.091147118151543083, -0.7263534371344014806 ) ) ;
#8257=DIRECTION ( 'NONE',  ( 0.4999551463232372317, -0.8660512985181135770, 0.000000000000000000 ) ) ;
#8258=CARTESIAN_POINT ( 'NONE',  ( 0.4331046530248302551, -1.588691189085156052, -0.6440782542836179791 ) ) ;
#8267=CARTESIAN_POINT ( 'NONE',  ( 0.6268473112825395654, -1.602176188498357190, -0.4542866955106492077 ) ) ;
#8275=B_SPLINE_CURVE_WITH_KNOTS ( 'NONE', 3,
 ( #28840, #13194, #4134, #6599, #22896, #19179, #22282, #26172, #25978, #34795 ),
 .UNSPECIFIED., .F., .F.,
 ( 4, 2, 2, 2, 4 ),
 ( 0.000000000000000000, 0.0005616480656060959548, 0.001123296131212191910, 0.001684944196818287864, 0.002246592262424383819 ),
 .UNSPECIFIED. ) ;
#8276=CARTESIAN_POINT ( 'NONE',  ( 0.3731218858483254519, -1.618895737510273936, -0.6660657155332145862 ) ) ;
#8280=( BOUNDED_SURFACE ( )  B_SPLINE_SURFACE ( 3, 2, ( 
 ( #7193, #13599, #26161 ),
 ( #38681, #4715, #8011 ),
 ( #1871, #20378, #39483 ),
 ( #16891, #20797, #8421 ),
 ( #29433, #33319, #14591 ),
 ( #20584, #14385, #29628 ),
 ( #20988, #5125, #32906 ),
 ( #1277, #33118, #26764 ),
 ( #39096, #23671, #27161 ),
 ( #4927, #36198, #38875 ) ),
 .UNSPECIFIED., .F., .F., .T. ) 
 B_SPLINE_SURFACE_WITH_KNOTS ( ( 4, 2, 2, 2, 4 ),
 ( 3, 3 ),
 ( 3.523657060577889411E-19, 0.0004886858803072692331, 0.0009773717606145380325, 0.001466057640921806723, 0.001954743521229075631 ),
 ( 0.000000000000000000, 1.000000000000000000 ),
 .UNSPECIFIED. ) 
 GEOMETRIC_REPRESENTATION_ITEM ( )  RATIONAL_B_SPLINE_SURFACE ( (
 ( 1.000000000000000000, 0.7071067811883920973, 1.000000000000000000),
 ( 1.000000000000000000, 0.7381839715666297375, 1.000000000000000000),
 ( 1.000000000000000000, 0.7637209924130993199, 1.000000000000000000),
 ( 1.000000000000000000, 0.8085232108216923175, 1.000000000000000000),
 ( 1.000000000000000000, 0.8280261753706451566, 1.000000000000000000),
 ( 1.000000000000000000, 0.8596601947502618968, 1.000000000000000000),
 ( 1.000000000000000000, 0.8720237471664858964, 1.000000000000000000),
 ( 1.000000000000000000, 0.8878769223232639840, 1.000000000000000000),
 ( 1.000000000000000000, 0.8914915958465460255, 1.000000000000000000),
 ( 1.000000000000000000, 0.8903032814718140342, 1.000000000000000000) ) ) 
 REPRESENTATION_ITEM ( '' )  SURFACE ( )  );
#8282=CARTESIAN_POINT ( 'NONE',  ( 0.09999999999997892519, -2.097675824466505023, -0.7286991843995646034 ) ) ;
#8286=CARTESIAN_POINT ( 'NONE',  ( 0.3901308303885444029, -1.763536657467503321, -0.4831808549932304353 ) ) ;
#8292=CARTESIAN_POINT ( 'NONE',  ( 0.1196427001920667699, -1.324177393134752911, -0.6828421133618256533 ) ) ;
#8298=ORIENTED_EDGE ( 'NONE', *, *, #29094, .F. ) ;
#8309=ORIENTED_EDGE ( 'NONE', *, *, #23502, .F. ) ;
#8315=DIRECTION ( 'NONE',  ( 1.000000000000000000, 0.000000000000000000, 0.000000000000000000 ) ) ;
#8317=CARTESIAN_POINT ( 'NONE',  ( 0.2659700368960441486, -1.559712477108197826, -0.7136488599841258607 ) ) ;
#8324=CARTESIAN_POINT ( 'NONE',  ( 0.3690560719070919427, -2.063130292613079231, -0.5133036944193291040 ) ) ;
#8325=DIRECTION ( 'NONE',  ( 0.4999551463232372317, -0.8660512985181133550, 0.000000000000000000 ) ) ;
#8333=AXIS2_PLACEMENT_3D ( 'NONE', #31078, #31295, #37651 ) ;
#8338=CARTESIAN_POINT ( 'NONE',  ( 0.3741198898060815181, -1.763750014703691082, -0.4380172221794854659 ) ) ;
#8339=CARTESIAN_POINT ( 'NONE',  ( 0.1994740068363786423, -2.042640899752901085, -0.2765909798240093198 ) ) ;
#8348=ORIENTED_EDGE ( 'NONE', *, *, #5114, .T. ) ;
#8354=VERTEX_POINT ( 'NONE', #32676 ) ;
#8356=CARTESIAN_POINT ( 'NONE',  ( 0.3930409166178727154, -1.973603618960653838, -0.2924226959962179517 ) ) ;
#8359=CARTESIAN_POINT ( 'NONE',  ( 0.02999607453758943582, -2.087869005097288788, -0.7252195465745524539 ) ) ;
#8362=CARTESIAN_POINT ( 'NONE',  ( 0.3991297247951158256, -1.748847237429244528, -0.4900819145088913809 ) ) ;
#8367=CARTESIAN_POINT ( 'NONE',  ( 0.5755826762959820320, -1.611988069552146463, -0.4931026870110623017 ) ) ;
#8371=DIRECTION ( 'NONE',  ( -0.8660512985181130219, -0.4999551463232378978, 1.983296656985678775E-15 ) ) ;
#8375=CARTESIAN_POINT ( 'NONE',  ( 0.3808488912321134068, -1.751740863376598067, -0.5696910252506037775 ) ) ;
#8379=ORIENTED_EDGE ( 'NONE', *, *, #34613, .F. ) ;
#8390=CARTESIAN_POINT ( 'NONE',  ( 0.5462802289783860177, -1.167382474216637878, -0.3984834965322623379 ) ) ;
#8401=DIRECTION ( 'NONE',  ( 0.4999551463232372317, -0.8660512985181134660, 0.000000000000000000 ) ) ;
#8405=CARTESIAN_POINT ( 'NONE',  ( 0.5467981811930779923, -1.652054351292815637, -0.5405695263049933308 ) ) ;
#8421=CARTESIAN_POINT ( 'NONE',  ( 0.3901692948650766768, -1.742007056135487453, -0.5885189368440594260 ) ) ;
#8424=DIRECTION ( 'NONE',  ( -0.9780874495037190641, 0.000000000000000000, 0.2081944790894071917 ) ) ;
#8430=B_SPLINE_CURVE_WITH_KNOTS ( 'NONE', 3,
 ( #27404, #24507, #11137, #2299 ),
 .UNSPECIFIED., .F., .F.,
 ( 4, 4 ),
 ( 1.301042606982604936E-18, 0.005310656474785389360 ),
 .UNSPECIFIED. ) ;
#8432=EDGE_LOOP ( 'NONE', ( #37897, #35405, #24155, #27174 ) ) ;
#8453=CARTESIAN_POINT ( 'NONE',  ( 0.3870312468228055414, -1.728124992867544840, -0.4409901392731783165 ) ) ;
#8456=CARTESIAN_POINT ( 'NONE',  ( 0.3794276050540705825, -1.663060803246817709, -0.6235637553391095711 ) ) ;
#8476=EDGE_LOOP ( 'NONE', ( #359, #35280, #19193, #31918 ) ) ;
#8480=CARTESIAN_POINT ( 'NONE',  ( 0.3738311686567912240, -1.761219272650979883, -0.4365117680794876609 ) ) ;
#8481=CARTESIAN_POINT ( 'NONE',  ( 0.3923243630925582481, -1.966611948492517969, -0.4968729097669116745 ) ) ;
#8486=CARTESIAN_POINT ( 'NONE',  ( 0.04054455197037542397, -1.519181945081407248, -0.6711553787198715204 ) ) ;
#8488=CARTESIAN_POINT ( 'NONE',  ( 0.3602315267031791501, -1.757724114542561278, -0.5288427849778383205 ) ) ;
#8501=EDGE_CURVE ( 'NONE', #21610, #2060, #2700, .T. ) ;
#8510=CARTESIAN_POINT ( 'NONE',  ( 0.1554368662221911890, -1.283069701700759513, -0.6964379544131902300 ) ) ;
#8515=CARTESIAN_POINT ( 'NONE',  ( 0.3617574415146475042, -1.960072772299676691, -0.4981249426996302576 ) ) ;
#8516=CARTESIAN_POINT ( 'NONE',  ( 0.3632367524865356967, -1.979769653201874480, -0.4982808577658072724 ) ) ;
#8519=CARTESIAN_POINT ( 'NONE',  ( 0.4484726360943441792, -1.685722521223443904, -0.5155029497116575543 ) ) ;
#8523=CARTESIAN_POINT ( 'NONE',  ( -2.112273405726188513E-14, -2.097675824466503691, -0.4937760292030871079 ) ) ;
#8527=DIRECTION ( 'NONE',  ( 0.4999551463232372317, -0.8660512985181135770, 0.000000000000000000 ) ) ;
#8528=CARTESIAN_POINT ( 'NONE',  ( 0.3264244126186546802, -1.294301107126978767, -0.5166151207188711680 ) ) ;
#8546=CARTESIAN_POINT ( 'NONE',  ( 0.1847441199961494251, -1.719353529619476184, -0.3282637342952985371 ) ) ;
#8559=CARTESIAN_POINT ( 'NONE',  ( 0.6142222766639747755, -1.573946724494656113, -0.5812230652184764423 ) ) ;
#8566=CARTESIAN_POINT ( 'NONE',  ( 0.4081716264380494952, -1.688076292791299782, -0.6123051696410536371 ) ) ;
#8573=B_SPLINE_CURVE_WITH_KNOTS ( 'NONE', 3,
 ( #16009, #35515, #16824, #23205, #19897, #3661, #32038, #19691, #29369, #12925, #10632, #20118 ),
 .UNSPECIFIED., .F., .F.,
 ( 4, 2, 2, 2, 2, 4 ),
 ( 1.291175088092316414E-16, 0.0008557172854888003312, 0.001283575928233135661, 0.001711434570977471425, 0.002567151856466139050, 0.003422869141954806241 ),
 .UNSPECIFIED. ) ;
#8591=VERTEX_POINT ( 'NONE', #11869 ) ;
#8594=EDGE_LOOP ( 'NONE', ( #582, #17002, #39162, #16060 ) ) ;
#8596=LINE ( 'NONE', #37398, #25728 ) ;
#8610=TOROIDAL_SURFACE ( 'NONE', #29657, 0.1333070866141734256, 0.02999999999999999889 ) ;
#8616=DIRECTION ( 'NONE',  ( 0.4999551463232377313, -0.8660512985181132439, -0.000000000000000000 ) ) ;
#8622=DIRECTION ( 'NONE',  ( -0.7038049723615886766, -0.4062933899497684909, 0.5827385710266903551 ) ) ;
#8636=AXIS2_PLACEMENT_3D ( 'NONE', #27587, #5342, #5153 ) ;
#8639=VERTEX_POINT ( 'NONE', #28922 ) ;
#8651=CARTESIAN_POINT ( 'NONE',  ( 0.3724564093243000751, -1.728032324874020143, -0.4192446018103713756 ) ) ;
#8653=CARTESIAN_POINT ( 'NONE',  ( 0.3402959632056909989, -1.632552626064600609, -0.5940485371126208447 ) ) ;
#8679=EDGE_CURVE ( 'NONE', #29543, #19627, #37502, .T. ) ;
#8702=CARTESIAN_POINT ( 'NONE',  ( 0.2914323826288399699, -1.233685883474753497, -0.5166151207188711680 ) ) ;
#8703=TOROIDAL_SURFACE ( 'NONE', #31066, 0.05000000000000000971, 0.1700000000000000400 ) ;
#8706=AXIS2_PLACEMENT_3D ( 'NONE', #19730, #37634, #16051 ) ;
#8713=CARTESIAN_POINT ( 'NONE',  ( 0.4777184729955372133, -1.099464642909131928, -0.4149595035330911896 ) ) ;
#8724=CARTESIAN_POINT ( 'NONE',  ( -2.112273405726188513E-14, -2.104523713476923685, -0.2882857794135356144 ) ) ;
#8735=EDGE_CURVE ( 'NONE', #25046, #40387, #22372, .T. ) ;
#8736=CARTESIAN_POINT ( 'NONE',  ( 0.3633112630502835505, -1.980641880850154468, -0.4944986277467309788 ) ) ;
#8738=FACE_OUTER_BOUND ( 'NONE', #12386, .T. ) ;
#8741=ORIENTED_EDGE ( 'NONE', *, *, #13496, .T. ) ;
#8748=CARTESIAN_POINT ( 'NONE',  ( 0.3324871086615504012, -1.659137217475707304, -0.6399689536651966826 ) ) ;
#8752=ORIENTED_EDGE ( 'NONE', *, *, #28244, .T. ) ;
#8756=FACE_OUTER_BOUND ( 'NONE', #7573, .T. ) ;
#8760=( BOUNDED_SURFACE ( )  B_SPLINE_SURFACE ( 3, 2, ( 
 ( #39270, #1850, #5669 ),
 ( #27685, #15127, #40220 ),
 ( #2589, #5855, #11093 ),
 ( #35982, #31187, #21536 ) ),
 .UNSPECIFIED., .F., .F., .T. ) 
 B_SPLINE_SURFACE_WITH_KNOTS ( ( 4, 4 ),
 ( 3, 3 ),
 ( 0.000000000000000000, 0.001804009323275673022 ),
 ( 0.000000000000000000, 1.000000000000000000 ),
 .UNSPECIFIED. ) 
 GEOMETRIC_REPRESENTATION_ITEM ( )  RATIONAL_B_SPLINE_SURFACE ( (
 ( 1.000000000000000000, 0.7071067811865464625, 1.000000000000000000),
 ( 1.000000000000000000, 0.7071042723947907893, 1.000000000000000000),
 ( 1.000000000000000000, 0.7064338697126849587, 1.000000000000000000),
 ( 1.000000000000000000, 0.7053326528219889813, 1.000000000000000000) ) ) 
 REPRESENTATION_ITEM ( '' )  SURFACE ( )  );
#8768=AXIS2_PLACEMENT_3D ( 'NONE', #3212, #38372, #25023 ) ;
#8772=CARTESIAN_POINT ( 'NONE',  ( 0.6140140453192455272, -1.573459653471211528, -0.4496618410196442928 ) ) ;
#8773=CARTESIAN_POINT ( 'NONE',  ( 0.02999607453758943582, -2.087869005097288788, -0.7252195465745524539 ) ) ;
#8777=CARTESIAN_POINT ( 'NONE',  ( 0.3699999999999786793, -2.097675824466503691, -0.4688691127277797022 ) ) ;
#8781=DIRECTION ( 'NONE',  ( 0.8660512985181134660, 0.4999551463232372317, 0.000000000000000000 ) ) ;
#8782=CARTESIAN_POINT ( 'NONE',  ( 0.4242202903503162759, -1.646166226851143666, -0.6219045950159559633 ) ) ;
#8784=CARTESIAN_POINT ( 'NONE',  ( 0.4511441812504100035, -1.668355241267087674, -0.6190017437410819667 ) ) ;
#8787=CARTESIAN_POINT ( 'NONE',  ( 0.4503105844069756891, -1.094366478625318440, -0.6237232363132070301 ) ) ;
#8792=AXIS2_PLACEMENT_3D ( 'NONE', #22846, #20149, #3880 ) ;
#8802=AXIS2_PLACEMENT_3D ( 'NONE', #20902, #2371, #36713 ) ;
#8813=CARTESIAN_POINT ( 'NONE',  ( 0.1371954450951175242, -1.846940070490806773, -0.3495212765556848233 ) ) ;
#8817=EDGE_CURVE ( 'NONE', #11734, #858, #13081, .T. ) ;
#8825=VECTOR ( 'NONE', #9098, 39.37007874015748854 ) ;
#8826=TOROIDAL_SURFACE ( 'NONE', #6843, 0.08830708661417323302, 0.01499999999999999944 ) ;
#8836=FACE_OUTER_BOUND ( 'NONE', #25672, .T. ) ;
#8842=ORIENTED_EDGE ( 'NONE', *, *, #36776, .T. ) ;
#8863=AXIS2_PLACEMENT_3D ( 'NONE', #25858, #22964, #37981 ) ;
#8871=CARTESIAN_POINT ( 'NONE',  ( 0.3619193181407161508, -1.620069869474523472, -0.6100577121333333741 ) ) ;
#8875=CARTESIAN_POINT ( 'NONE',  ( 0.3539331831703069198, -1.624680115194805152, -0.4258185731538512431 ) ) ;
#8887=CARTESIAN_POINT ( 'NONE',  ( 0.3394335999418694461, -1.659526807576534146, -0.3889335715588135289 ) ) ;
#8901=CARTESIAN_POINT ( 'NONE',  ( 0.3568951684747839748, -1.733180931717886120, -0.5240687084291923981 ) ) ;
#8906=CARTESIAN_POINT ( 'NONE',  ( 0.1757500541653520265, -1.230771478115229245, -0.7462941026102624109 ) ) ;
#8912=VERTEX_POINT ( 'NONE', #16803 ) ;
#8920=CARTESIAN_POINT ( 'NONE',  ( 0.000000000000000000, 0.000000000000000000, 0.000000000000000000 ) ) ;
#8921=EDGE_CURVE ( 'NONE', #26169, #28258, #14531, .T. ) ;
#8930=CARTESIAN_POINT ( 'NONE',  ( 0.3699999999999785127, -2.054734391222357459, -0.6850094247584045393 ) ) ;
#8932=CARTESIAN_POINT ( 'NONE',  ( 0.3923243630925510872, -1.966611948492501316, -0.4968729097670202544 ) ) ;
#8935=CARTESIAN_POINT ( 'NONE',  ( 0.3942702837509829417, -1.601394264692599156, -0.3531866499983610241 ) ) ;
#8938=ORIENTED_EDGE ( 'NONE', *, *, #15151, .T. ) ;
#8943=ORIENTED_EDGE ( 'NONE', *, *, #25631, .F. ) ;
#8949=CARTESIAN_POINT ( 'NONE',  ( 0.3777061319049067056, -1.720453251631598679, -0.5284398357475414976 ) ) ;
#8963=FACE_OUTER_BOUND ( 'NONE', #21569, .T. ) ;
#8966=CARTESIAN_POINT ( 'NONE',  ( 0.1808977814881074231, -1.754363797449167262, -0.3261742699824988767 ) ) ;
#8977=EDGE_CURVE ( 'NONE', #5149, #4721, #886, .T. ) ;
#8983=B_SPLINE_CURVE_WITH_KNOTS ( 'NONE', 3,
 ( #5216, #15301, #27647, #40177, #40394, #40592 ),
 .UNSPECIFIED., .F., .F.,
 ( 4, 2, 4 ),
 ( -5.502486261264484631E-06, 0.0003446809754944347277, 0.0006948644372501340018 ),
 .UNSPECIFIED. ) ;
#8984=CARTESIAN_POINT ( 'NONE',  ( 0.6612567317249036236, -1.491170171073062045, -0.4119998595604874025 ) ) ;
#8989=DIRECTION ( 'NONE',  ( 1.000000000000000000, 0.000000000000000000, 0.000000000000000000 ) ) ;
#8996=CARTESIAN_POINT ( 'NONE',  ( 0.4233792892081513215, -1.670469256985428474, -0.6343475356697100276 ) ) ;
#8999=CARTESIAN_POINT ( 'NONE',  ( 0.4939251185753719686, -1.677760966407569665, -0.6096475700680613619 ) ) ;
#9007=ORIENTED_EDGE ( 'NONE', *, *, #40637, .F. ) ;
#9013=CARTESIAN_POINT ( 'NONE',  ( 0.5612334960093817715, -1.620627794947044897, -0.4868944820179721966 ) ) ;
#9020=CARTESIAN_POINT ( 'NONE',  ( 0.2112514853725389330, -1.519796704070200732, -0.3223733989273451228 ) ) ;
#9022=EDGE_LOOP ( 'NONE', ( #37130, #20720, #3235 ) ) ;
#9026=CARTESIAN_POINT ( 'NONE',  ( 0.1926120471057841121, -1.518195021730778471, -0.3560059264261548062 ) ) ;
#9027=DIRECTION ( 'NONE',  ( -0.4999551463232372317, 0.8660512985181134660, -0.000000000000000000 ) ) ;
#9028=CARTESIAN_POINT ( 'NONE',  ( 0.07950324646436757181, -1.397811199834917417, -0.3670508432710352653 ) ) ;
#9030=CARTESIAN_POINT ( 'NONE',  ( 0.5901238867768096030, -1.488331658671158797, -0.4293751906308629906 ) ) ;
#9032=EDGE_CURVE ( 'NONE', #19986, #37556, #32285, .T. ) ;
#9048=ORIENTED_EDGE ( 'NONE', *, *, #6142, .F. ) ;
#9056=ORIENTED_EDGE ( 'NONE', *, *, #36776, .F. ) ;
#9058=VERTEX_POINT ( 'NONE', #27069 ) ;
#9064=CARTESIAN_POINT ( 'NONE',  ( -0.002218965743620939825, -1.368565310413371705, -0.3828039145932563558 ) ) ;
#9067=CARTESIAN_POINT ( 'NONE',  ( 0.3842289435304718226, -1.843891179545533943, -0.4840290186776841086 ) ) ;
#9072=CARTESIAN_POINT ( 'NONE',  ( 0.5308991137012172290, -1.672779244431372492, -0.4688114127372004503 ) ) ;
#9086=CARTESIAN_POINT ( 'NONE',  ( 0.3646274796662056228, -1.706748141935739094, -0.4511273082355062303 ) ) ;
#9088=CARTESIAN_POINT ( 'NONE',  ( 0.3591498995103406533, -1.737620376665804933, -0.5147966178037263196 ) ) ;
#9091=DIRECTION ( 'NONE',  ( 0.8660512985181133550, 0.4999551463232371207, 0.000000000000000000 ) ) ;
#9096=CARTESIAN_POINT ( 'NONE',  ( 0.1959265899308190728, -1.288818386415671036, -0.7414046965098798347 ) ) ;
#9098=DIRECTION ( 'NONE',  ( 0.4999551463232372317, -0.8660512985181133550, 0.000000000000000000 ) ) ;
#9100=CARTESIAN_POINT ( 'NONE',  ( 0.4159916692016358830, -1.069406866067976081, -0.5155029497116575543 ) ) ;
#9105=CARTESIAN_POINT ( 'NONE',  ( 0.3520636416031024951, -1.608800853759478677, -0.6368828113034350480 ) ) ;
#9106=DIRECTION ( 'NONE',  ( 0.000000000000000000, 0.000000000000000000, -1.000000000000000000 ) ) ;
#9111=CARTESIAN_POINT ( 'NONE',  ( 0.5079445638232780169, -1.582110533707940192, -0.5155029497116575543 ) ) ;
#9116=CARTESIAN_POINT ( 'NONE',  ( 0.003465668518863261691, -1.839186521745578284, -0.6434132171392461519 ) ) ;
#9120=CARTESIAN_POINT ( 'NONE',  ( 0.3624061103390691096, -1.968824918581854932, -0.4968426515055719972 ) ) ;
#9121=CARTESIAN_POINT ( 'NONE',  ( 0.3898146559560766722, -1.698689370364980133, -0.4973142990484694104 ) ) ;
#9131=ORIENTED_EDGE ( 'NONE', *, *, #2894, .F. ) ;
#9136=CARTESIAN_POINT ( 'NONE',  ( 0.4840267074530639757, -1.682517813888804392, -0.4333519947141560857 ) ) ;
#9138=CARTESIAN_POINT ( 'NONE',  ( 0.1836296472909090260, -1.744742035088381327, -0.3568621931777658518 ) ) ;
#9146=ADVANCED_FACE ( 'NONE', ( #9962 ), #35291, .T. ) ;
#9154=DIRECTION ( 'NONE',  ( -0.2204180896037088722, -0.8274293670542908208, 0.5165041222600136317 ) ) ;
#9156=CARTESIAN_POINT ( 'NONE',  ( 0.3916117103943055899, -1.785355738137090809, -0.5264918531311321148 ) ) ;
#9170=CARTESIAN_POINT ( 'NONE',  ( 0.4887921365776448090, -1.679766821171225999, -0.4193976862638449377 ) ) ;
#9171=CARTESIAN_POINT ( 'NONE',  ( 0.6058310743872277193, -1.588085125911432804, -0.4741143205363104740 ) ) ;
#9172=CARTESIAN_POINT ( 'NONE',  ( 0.3957193873654859528, -2.010249311248437198, -0.4875152547671333658 ) ) ;
#9178=CARTESIAN_POINT ( 'NONE',  ( 0.4045767908288230297, -1.721983033185328527, -0.6022994628584866783 ) ) ;
#9184=CARTESIAN_POINT ( 'NONE',  ( 0.5005869906397938385, -1.690277863677645875, -0.6089672282429000605 ) ) ;
#9188=ADVANCED_FACE ( 'NONE', ( #35270 ), #8610, .F. ) ;
#9191=CARTESIAN_POINT ( 'NONE',  ( 0.5395555926592416895, -1.597940071789080374, -0.5747445381412426002 ) ) ;
#9197=EDGE_LOOP ( 'NONE', ( #21428, #18053, #23644, #6762 ) ) ;
#9202=DIRECTION ( 'NONE',  ( -0.4999551463232373427, 0.8660512985181134660, -0.000000000000000000 ) ) ;
#9209=CARTESIAN_POINT ( 'NONE',  ( 0.2060189241777137525, -2.057789047793026516, -0.3052958066308563145 ) ) ;
#9211=AXIS2_PLACEMENT_3D ( 'NONE', #40409, #16143, #12235 ) ;
#9213=CARTESIAN_POINT ( 'NONE',  ( 0.001230546430223489760, -1.915437084753079722, -0.3396229129526682211 ) ) ;
#9216=CARTESIAN_POINT ( 'NONE',  ( 0.3999999999999783729, -2.086934379033410725, -0.5179790689110178592 ) ) ;
#9224=CARTESIAN_POINT ( 'NONE',  ( 0.5873347430034532302, -1.537871679492680110, -0.6182658308370784228 ) ) ;
#9232=( BOUNDED_SURFACE ( )  B_SPLINE_SURFACE ( 3, 2, ( 
 ( #18134, #14628, #8653 ),
 ( #5353, #27414, #30690 ),
 ( #31446, #23705, #14419 ),
 ( #17714, #8456, #20624 ),
 ( #30479, #21448, #37048 ),
 ( #28351, #4964, #17531 ),
 ( #30079, #23917, #8871 ),
 ( #2309, #40126, #14849 ) ),
 .UNSPECIFIED., .F., .F., .F. ) 
 B_SPLINE_SURFACE_WITH_KNOTS ( ( 4, 2, 2, 4 ),
 ( 3, 3 ),
 ( 0.001132904267245888079, 0.001446982864295271072, 0.001761061461344653849, 0.002389218655443419402 ),
 ( 0.000000000000000000, 1.000000000000000000 ),
 .UNSPECIFIED. ) 
 GEOMETRIC_REPRESENTATION_ITEM ( )  RATIONAL_B_SPLINE_SURFACE ( (
 ( 1.000000000000000000, 0.4483291926235775660, 1.000000000000000000),
 ( 1.000000000000000000, 0.4613307591293988597, 1.000000000000000000),
 ( 1.000000000000000000, 0.4741491466902303942, 1.000000000000000000),
 ( 1.000000000000000000, 0.4983216539137984014, 1.000000000000000000),
 ( 1.000000000000000000, 0.5096972859111215115, 1.000000000000000000),
 ( 1.000000000000000000, 0.5380540011986519877, 1.000000000000000000),
 ( 1.000000000000000000, 0.5496804717520560324, 1.000000000000000000),
 ( 1.000000000000000000, 0.5504785946861833201, 1.000000000000000000) ) ) 
 REPRESENTATION_ITEM ( '' )  SURFACE ( )  );
#9241=EDGE_LOOP ( 'NONE', ( #28041, #24827, #417, #6119, #16340, #24458 ) ) ;
#9245=CARTESIAN_POINT ( 'NONE',  ( 0.4959102259190470430, -1.676612535457929098, -0.4224503755058100496 ) ) ;
#9253=CARTESIAN_POINT ( 'NONE',  ( 0.4705465871830276092, -1.070011441572239930, -0.4234330131081484594 ) ) ;
#9269=CARTESIAN_POINT ( 'NONE',  ( 0.3701597793959978122, -1.743707579621869286, -0.4236181223213599245 ) ) ;
#9283=CARTESIAN_POINT ( 'NONE',  ( 0.4705313329396505484, -1.155124162917906538, -0.6196578200117470736 ) ) ;
#9288=CARTESIAN_POINT ( 'NONE',  ( 0.3699999999999786793, -2.183180860297921466, -0.4937760292030871079 ) ) ;
#9292=ORIENTED_EDGE ( 'NONE', *, *, #19196, .F. ) ;
#9299=CIRCLE ( 'NONE', #38202, 0.1033070866141734268 ) ;
#9303=FACE_OUTER_BOUND ( 'NONE', #37025, .T. ) ;
#9307=ORIENTED_EDGE ( 'NONE', *, *, #7735, .T. ) ;
#9322=DIRECTION ( 'NONE',  ( 0.8660512985181135770, 0.4999551463232370652, 0.000000000000000000 ) ) ;
#9336=CARTESIAN_POINT ( 'NONE',  ( 0.5462348416196848300, -1.594646255991501560, -0.4868944820179722521 ) ) ;
#9339=CARTESIAN_POINT ( 'NONE',  ( 0.3666495184304034427, -1.755770389311256396, -0.5282448765462863793 ) ) ;
#9343=CARTESIAN_POINT ( 'NONE',  ( 0.1757500541653520265, -1.230771478115229245, -0.5931747813493342125 ) ) ;
#9347=ORIENTED_EDGE ( 'NONE', *, *, #24878, .F. ) ;
#9350=DIRECTION ( 'NONE',  ( -0.8660512985181131329, -0.4999551463232376758, 0.000000000000000000 ) ) ;
#9353=CARTESIAN_POINT ( 'NONE',  ( 0.3327035037690653230, -1.656108012777571359, -0.6420915705233924964 ) ) ;
#9355=CARTESIAN_POINT ( 'NONE',  ( 0.3465130674089420548, -1.628963608593047230, -0.3702441142993493362 ) ) ;
#9359=CARTESIAN_POINT ( 'NONE',  ( 0.3982344888468541955, -1.728315610757950260, -0.3049413784164444197 ) ) ;
#9375=CARTESIAN_POINT ( 'NONE',  ( 0.4685571881589434273, -1.131435060437132156, -0.3725158680014900026 ) ) ;
#9380=CIRCLE ( 'NONE', #10686, 0.02999999999999999542 ) ;
#9385=CIRCLE ( 'NONE', #32377, 0.2200000000000000566 ) ;
#9387=CARTESIAN_POINT ( 'NONE',  ( 0.1834964085430285941, -1.226715333008844055, -0.5155029497116575543 ) ) ;
#9388=CARTESIAN_POINT ( 'NONE',  ( 0.3679573697808270483, -2.043903617469527312, -0.4804103685335425200 ) ) ;
#9390=CARTESIAN_POINT ( 'NONE',  ( 0.3969700875656382300, -1.750093955434189663, -0.5306525527942058673 ) ) ;
#9400=ORIENTED_EDGE ( 'NONE', *, *, #34137, .F. ) ;
#9403=VERTEX_POINT ( 'NONE', #9911 ) ;
#9408=CARTESIAN_POINT ( 'NONE',  ( 0.3397077535880359545, -1.654685348432989089, -0.3858274525146626055 ) ) ;
#9418=CARTESIAN_POINT ( 'NONE',  ( 0.6123118846157344919, -1.441347382273072908, -0.6250000000000000000 ) ) ;
#9419=AXIS2_PLACEMENT_3D ( 'NONE', #40036, #18041, #8989 ) ;
#9421=CARTESIAN_POINT ( 'NONE',  ( 0.3784118722789395206, -1.581834032482531738, -0.2869361388274794256 ) ) ;
#9427=AXIS2_PLACEMENT_3D ( 'NONE', #27416, #5577, #40129 ) ;
#9428=CARTESIAN_POINT ( 'NONE',  ( 0.1161415672770640256, -1.518500864528294914, -0.6476785841699168600 ) ) ;
#9429=CARTESIAN_POINT ( 'NONE',  ( 0.3459163166870670159, -1.704669448431704648, -0.4228134667771305533 ) ) ;
#9436=CARTESIAN_POINT ( 'NONE',  ( 0.5925625413354431714, -1.513297660314260940, -0.6339996871210799023 ) ) ;
#9441=ORIENTED_EDGE ( 'NONE', *, *, #25225, .F. ) ;
#9447=ORIENTED_EDGE ( 'NONE', *, *, #38540, .T. ) ;
#9454=ORIENTED_EDGE ( 'NONE', *, *, #22847, .F. ) ;
#9459=CARTESIAN_POINT ( 'NONE',  ( 0.5185821078642816051, -1.679889620532657224, -0.4521106403573806887 ) ) ;
#9464=CARTESIAN_POINT ( 'NONE',  ( 0.4140578086700125171, -1.707491598636114327, -0.4205192078341298267 ) ) ;
#9466=EDGE_LOOP ( 'NONE', ( #12316, #20967, #35966, #31777 ) ) ;
#9467=CARTESIAN_POINT ( 'NONE',  ( 0.4525225916027839634, -1.089042801799552374, -0.4103247334897814347 ) ) ;
#9472=CARTESIAN_POINT ( 'NONE',  ( 0.5368241747238033934, -1.669358818002142364, -0.4818844110413548210 ) ) ;
#9477=EDGE_CURVE ( 'NONE', #14915, #19986, #33604, .T. ) ;
#9496=CARTESIAN_POINT ( 'NONE',  ( 0.3436318669657925096, -1.639703809451618088, -0.4374757763236017394 ) ) ;
#9500=EDGE_CURVE ( 'NONE', #28258, #28471, #23124, .T. ) ;
#9511=AXIS2_PLACEMENT_3D ( 'NONE', #11739, #14216, #36019 ) ;
#9514=CARTESIAN_POINT ( 'NONE',  ( 0.6343156381093978391, -1.595758837318228540, -0.5875140676452393906 ) ) ;
#9517=ORIENTED_EDGE ( 'NONE', *, *, #13262, .T. ) ;
#9522=CARTESIAN_POINT ( 'NONE',  ( 0.5788902524971968333, -1.608766677709437598, -0.5587703673255073333 ) ) ;
#9527=DIRECTION ( 'NONE',  ( 0.4999551463232373427, -0.8660512985181134660, 0.000000000000000000 ) ) ;
#9531=CIRCLE ( 'NONE', #32514, 0.05000000000000000971 ) ;
#9535=CARTESIAN_POINT ( 'NONE',  ( 0.07293838214825623667, -1.413098248535316070, -0.6555667331668242337 ) ) ;
#9536=ADVANCED_FACE ( 'NONE', ( #16309 ), #37282, .T. ) ;
#9541=DIRECTION ( 'NONE',  ( -0.4999551463232372317, 0.8660512985181135770, -0.000000000000000000 ) ) ;
#9543=VERTEX_POINT ( 'NONE', #20205 ) ;
#9552=ORIENTED_EDGE ( 'NONE', *, *, #5147, .T. ) ;
#9559=CARTESIAN_POINT ( 'NONE',  ( 0.3646343803856678112, -1.994732639415563558, -0.3188592562828334587 ) ) ;
#9562=CARTESIAN_POINT ( 'NONE',  ( -2.112273405726188513E-14, -1.837418632672298768, -0.6339733133327630776 ) ) ;
#9564=CARTESIAN_POINT ( 'NONE',  ( 0.3462147144707520829, -1.728761431451053321, -0.5787996928876401048 ) ) ;
#9571=CARTESIAN_POINT ( 'NONE',  ( 0.4732169041981261759, -1.632014213049435281, -0.4230577161329019953 ) ) ;
#9577=B_SPLINE_CURVE_WITH_KNOTS ( 'NONE', 3,
 ( #33300, #30209, #1658, #5107, #17662, #35575, #26330, #4693 ),
 .UNSPECIFIED., .F., .F.,
 ( 4, 2, 2, 4 ),
 ( -6.000000000156461008E-08, 0.0008322485881172374776, 0.001664557176234476550, 0.003329174352468955780 ),
 .UNSPECIFIED. ) ;
#9589=CARTESIAN_POINT ( 'NONE',  ( 0.6025502600592794744, -1.571821872759174621, -0.4181649500142127773 ) ) ;
#9594=CARTESIAN_POINT ( 'NONE',  ( 0.1893026375364066649, -1.254248048989826225, -0.6328096728701395612 ) ) ;
#9597=CARTESIAN_POINT ( 'NONE',  ( 0.3599725030089058753, -1.738129011639496291, -0.5054791832264183826 ) ) ;
#9598=CARTESIAN_POINT ( 'NONE',  ( 0.3779900952041616025, -1.610792511722474840, -0.4148273735560925601 ) ) ;
#9600=CARTESIAN_POINT ( 'NONE',  ( 0.5358573072157438721, -1.635276992059453427, -0.4933326546058601769 ) ) ;
#9603=ORIENTED_EDGE ( 'NONE', *, *, #34902, .F. ) ;
#9604=CARTESIAN_POINT ( 'NONE',  ( 0.3740544490715725923, -1.618991780640511635, -0.6658790255296196392 ) ) ;
#9615=CARTESIAN_POINT ( 'NONE',  ( 0.4123503261003252374, -1.705581556875543914, -0.3887263060331934139 ) ) ;
#9622=CARTESIAN_POINT ( 'NONE',  ( 0.1929960976912158399, -1.971902824862748593, -0.3252172897420532727 ) ) ;
#9625=TOROIDAL_SURFACE ( 'NONE', #33924, 0.1333070866141734256, 0.02999999999999999889 ) ;
#9637=CIRCLE ( 'NONE', #33296, 0.1033070866141734129 ) ;
#9639=CARTESIAN_POINT ( 'NONE',  ( 0.3999999999999783729, -2.097675824466503691, -0.5196396315034579327 ) ) ;
#9641=EDGE_CURVE ( 'NONE', #29368, #13497, #16910, .T. ) ;
#9642=CARTESIAN_POINT ( 'NONE',  ( 0.07652314640228294329, -2.107936428766273629, -0.7005084057759866090 ) ) ;
#9653=VECTOR ( 'NONE', #35856, 39.37007874015748143 ) ;
#9654=DIRECTION ( 'NONE',  ( 0.000000000000000000, 0.9437421848352475218, -0.3306821564015722803 ) ) ;
#9665=ADVANCED_FACE ( 'NONE', ( #13804 ), #35419, .T. ) ;
#9673=CARTESIAN_POINT ( 'NONE',  ( 0.3925301276612754298, -1.756377271995033684, -0.4843757382520948451 ) ) ;
#9680=ORIENTED_EDGE ( 'NONE', *, *, #23081, .F. ) ;
#9684=CARTESIAN_POINT ( 'NONE',  ( 0.1999999999999786393, -2.081198020765314460, -0.7227018020631825745 ) ) ;
#9693=DIRECTION ( 'NONE',  ( 4.503376743791639448E-15, 0.9613939893712163398, -0.2751755752258865373 ) ) ;
#9697=CARTESIAN_POINT ( 'NONE',  ( 0.1857471242690073021, -1.941376881060412174, -0.6624637124125288823 ) ) ;
#9701=ORIENTED_EDGE ( 'NONE', *, *, #20550, .F. ) ;
#9703=ORIENTED_EDGE ( 'NONE', *, *, #38815, .F. ) ;
#9704=CARTESIAN_POINT ( 'NONE',  ( 0.4450935511747624584, -1.144980177316206049, -0.3864693716766450793 ) ) ;
#9710=ORIENTED_EDGE ( 'NONE', *, *, #12462, .F. ) ;
#9711=CARTESIAN_POINT ( 'NONE',  ( 0.2484857473122377980, -1.339293634572156000, -0.5155029497116575543 ) ) ;
#9714=CARTESIAN_POINT ( 'NONE',  ( 0.6315454840034280259, -1.614677985444239239, -0.5441907603584862363 ) ) ;
#9718=EDGE_LOOP ( 'NONE', ( #21043, #25155, #22730, #36158, #20915, #14977, #14939, #36765 ) ) ;
#9740=DIRECTION ( 'NONE',  ( 0.8660512985181135770, 0.4999551463232371207, 1.024644699336566956E-15 ) ) ;
#9748=FACE_OUTER_BOUND ( 'NONE', #7315, .T. ) ;
#9758=CARTESIAN_POINT ( 'NONE',  ( 0.4170115945640069932, -1.702980413955156758, -0.6123808887097255127 ) ) ;
#9760=VERTEX_POINT ( 'NONE', #11553 ) ;
#9773=CARTESIAN_POINT ( 'NONE',  ( 0.4271757566612302548, -1.700307850918723274, -0.5150901720920313398 ) ) ;
#9787=DIRECTION ( 'NONE',  ( 0.000000000000000000, 0.9396926207858876667, -0.3420201433257257229 ) ) ;
#9794=CARTESIAN_POINT ( 'NONE',  ( 0.5584481223773475334, -1.622235738823061491, -0.4750859664929777404 ) ) ;
#9797=DIRECTION ( 'NONE',  ( 0.000000000000000000, 0.2751755752258863708, 0.9613939893712163398 ) ) ;
#9806=ORIENTED_EDGE ( 'NONE', *, *, #37813, .T. ) ;
#9810=VERTEX_POINT ( 'NONE', #30676 ) ;
#9813=CYLINDRICAL_SURFACE ( 'NONE', #24215, 0.1033070866141734129 ) ;
#9814=CARTESIAN_POINT ( 'NONE',  ( 0.3404871394918290717, -1.648910532809566787, -0.3823052341430687728 ) ) ;
#9830=CARTESIAN_POINT ( 'NONE',  ( 0.3961214603528522837, -2.010890533879527098, -0.7066937474304769706 ) ) ;
#9835=EDGE_CURVE ( 'NONE', #13144, #23421, #35589, .T. ) ;
#9841=( BOUNDED_SURFACE ( )  B_SPLINE_SURFACE ( 3, 2, ( 
 ( #3477, #28581, #32063 ),
 ( #1044, #16422, #28963 ),
 ( #829, #13550, #454 ),
 ( #35355, #26121, #34543 ),
 ( #18923, #12950, #9843 ),
 ( #22412, #34943, #14543 ),
 ( #32454, #36147, #30186 ),
 ( #26718, #1233, #11262 ),
 ( #1625, #29995, #17038 ),
 ( #14147, #8170, #13731 ),
 ( #7342, #7565, #26505 ),
 ( #19919, #4279, #2016 ),
 ( #5079, #35538, #23832 ),
 ( #35958, #7767, #16847 ),
 ( #20333, #4872, #7957 ),
 ( #1828, #26907, #32855 ),
 ( #29387, #32666, #27108 ),
 ( #23443, #39247, #20750 ),
 ( #14344, #38823, #4658 ),
 ( #33065, #10451, #39439 ),
 ( #26298, #35751, #33273 ),
 ( #36353, #23018, #10655 ),
 ( #17639, #23227, #20139 ),
 ( #4470, #13934, #29577 ),
 ( #17233, #17443, #1419 ),
 ( #39037, #10870, #20531 ),
 ( #11068, #29784, #23630 ),
 ( #18251, #15155, #2818 ) ),
 .UNSPECIFIED., .F., .F., .T. ) 
 B_SPLINE_SURFACE_WITH_KNOTS ( ( 4, 2, 2, 2, 2, 2, 2, 2, 2, 2, 2, 2, 2, 4 ),
 ( 3, 3 ),
 ( 0.008694144295605974598, 0.009671288477786803284, 0.01015986056887721936, 0.01064843265996763370, 0.01113700475105804805, 0.01162557684214846412, 0.01211414893323887847, 0.01260272102432929281, 0.01309129311541970715, 0.01357986520651012149, 0.01406843729760053757, 0.01455700938869095191, 0.01553415357087178233, 0.01651129775305261102 ),
 ( 0.000000000000000000, 1.000000000000000000 ),
 .UNSPECIFIED. ) 
 GEOMETRIC_REPRESENTATION_ITEM ( )  RATIONAL_B_SPLINE_SURFACE ( (
 ( 1.000000000000000000, 0.6470169433091488287, 1.000000000000000000),
 ( 1.000000000000000000, 0.6654672097952949450, 1.000000000000000000),
 ( 1.000000000000000000, 0.6852032907093373870, 1.000000000000000000),
 ( 1.000000000000000000, 0.7106118140251836968, 1.000000000000000000),
 ( 1.000000000000000000, 0.7184497985660520669, 1.000000000000000000),
 ( 1.000000000000000000, 0.7321196217632601755, 1.000000000000000000),
 ( 1.000000000000000000, 0.7378276987527578878, 1.000000000000000000),
 ( 1.000000000000000000, 0.7460113087339939053, 1.000000000000000000),
 ( 1.000000000000000000, 0.7485381724456307007, 1.000000000000000000),
 ( 1.000000000000000000, 0.7496653861197896118, 1.000000000000000000),
 ( 1.000000000000000000, 0.7481474087358157554, 1.000000000000000000),
 ( 1.000000000000000000, 0.7416790020604431266, 1.000000000000000000),
 ( 1.000000000000000000, 0.7366135046999445768, 1.000000000000000000),
 ( 1.000000000000000000, 0.7274392094783487250, 1.000000000000000000),
 ( 1.000000000000000000, 0.7238593899674543586, 1.000000000000000000),
 ( 1.000000000000000000, 0.7238140619247546148, 1.000000000000000000),
 ( 1.000000000000000000, 0.7273137035903693981, 1.000000000000000000),
 ( 1.000000000000000000, 0.7363604236068268527, 1.000000000000000000),
 ( 1.000000000000000000, 0.7415226458536995358, 1.000000000000000000),
 ( 1.000000000000000000, 0.7480748423670980918, 1.000000000000000000),
 ( 1.000000000000000000, 0.7496261409616462590, 1.000000000000000000),
 ( 1.000000000000000000, 0.7486302821632393467, 1.000000000000000000),
 ( 1.000000000000000000, 0.7461034829534261004, 1.000000000000000000),
 ( 1.000000000000000000, 0.7338444141171208690, 1.000000000000000000),
 ( 1.000000000000000000, 0.7192226083161986638, 1.000000000000000000),
 ( 1.000000000000000000, 0.6852364196241883532, 1.000000000000000000),
 ( 1.000000000000000000, 0.6655055671846430432, 1.000000000000000000),
 ( 1.000000000000000000, 0.6469660273759296754, 1.000000000000000000) ) ) 
 REPRESENTATION_ITEM ( '' )  SURFACE ( )  );
#9843=CARTESIAN_POINT ( 'NONE',  ( 0.5825939818895130573, -1.511660705017517037, -0.4462983586487643817 ) ) ;
#9844=CARTESIAN_POINT ( 'NONE',  ( 0.4268980379306122064, -1.643599345667950962, -0.4092648393969009479 ) ) ;
#9855=EDGE_LOOP ( 'NONE', ( #22381, #13529, #8233 ) ) ;
#9859=AXIS2_PLACEMENT_3D ( 'NONE', #39295, #26561, #36005 ) ;
#9862=CARTESIAN_POINT ( 'NONE',  ( 0.1984280195443378358, -1.270055564915130608, -0.3194734774171836822 ) ) ;
#9868=CARTESIAN_POINT ( 'NONE',  ( 0.3897459579033060728, -1.931687273480471312, -0.4920516470159677080 ) ) ;
#9876=FACE_OUTER_BOUND ( 'NONE', #3146, .T. ) ;
#9877=FACE_OUTER_BOUND ( 'NONE', #4486, .T. ) ;
#9885=CARTESIAN_POINT ( 'NONE',  ( 0.1988350626189778203, -1.655126656547283082, -0.6577951576610993056 ) ) ;
#9886=ADVANCED_FACE ( 'NONE', ( #11335 ), #8039, .T. ) ;
#9889=CARTESIAN_POINT ( 'NONE',  ( 0.3716760655518760448, -1.720866715815103420, -0.6853003695678743235 ) ) ;
#9890=AXIS2_PLACEMENT_3D ( 'NONE', #3550, #34412, #31521 ) ;
#9895=ORIENTED_EDGE ( 'NONE', *, *, #33780, .F. ) ;
#9898=CARTESIAN_POINT ( 'NONE',  ( 0.4555369797039701685, -1.145095616941093297, -0.3997359831693639842 ) ) ;
#9904=ORIENTED_EDGE ( 'NONE', *, *, #3338, .T. ) ;
#9908=EDGE_CURVE ( 'NONE', #37075, #9543, #31655, .T. ) ;
#9911=CARTESIAN_POINT ( 'NONE',  ( 0.5455881031540378290, -1.595019605959082654, -0.5473203437262895710 ) ) ;
#9921=ORIENTED_EDGE ( 'NONE', *, *, #33885, .T. ) ;
#9946=CIRCLE ( 'NONE', #27610, 0.02999999999999999195 ) ;
#9958=EDGE_CURVE ( 'NONE', #33739, #23391, #21415, .T. ) ;
#9962=FACE_OUTER_BOUND ( 'NONE', #9855, .T. ) ;
#9966=ORIENTED_EDGE ( 'NONE', *, *, #26247, .T. ) ;
#9978=CARTESIAN_POINT ( 'NONE',  ( 0.4409062655693435917, -1.690090444797295532, -0.4991292961807995421 ) ) ;
#9986=EDGE_CURVE ( 'NONE', #20774, #16986, #20499, .T. ) ;
#9995=CARTESIAN_POINT ( 'NONE',  ( 0.1759300380180282841, -1.231083256582695906, -0.6184399470714002645 ) ) ;
#9998=CARTESIAN_POINT ( 'NONE',  ( 0.3879614285305876820, -1.650392248945780960, -0.3945637954816432202 ) ) ;
#10002=ORIENTED_EDGE ( 'NONE', *, *, #1714, .F. ) ;
#10006=ADVANCED_FACE ( 'NONE', ( #26529 ), #12988, .T. ) ;
#10009=ADVANCED_FACE ( 'NONE', ( #20560, #33093 ), #28103, .T. ) ;
#10016=EDGE_CURVE ( 'NONE', #19872, #357, #24614, .T. ) ;
#10019=ORIENTED_EDGE ( 'NONE', *, *, #15014, .T. ) ;
#10020=ADVANCED_FACE ( 'NONE', ( #1653 ), #17260, .T. ) ;
#10030=CARTESIAN_POINT ( 'NONE',  ( 0.3868395167223153130, -1.896608414150803501, -0.5100822255063985899 ) ) ;
#10036=CARTESIAN_POINT ( 'NONE',  ( 0.02746053214171286644, -1.399542977676857758, -0.3784122419456570907 ) ) ;
#10037=CARTESIAN_POINT ( 'NONE',  ( 0.3757471142192216340, -1.766731021160330206, -0.5680748514784758063 ) ) ;
#10045=ADVANCED_FACE ( 'NONE', ( #8963 ), #8760, .F. ) ;
#10046=CARTESIAN_POINT ( 'NONE',  ( 0.4159916692016358830, -1.069406866067976081, -0.5155029497116575543 ) ) ;
#10055=CARTESIAN_POINT ( 'NONE',  ( 0.4231587444657393116, -1.645334281830443945, -0.4089428064156527820 ) ) ;
#10056=CARTESIAN_POINT ( 'NONE',  ( 0.2764337282391428618, -1.207704344519209938, -0.5166151207188711680 ) ) ;
#10060=EDGE_LOOP ( 'NONE', ( #16963, #31671, #36326, #11503, #35872, #33283 ) ) ;
#10068=DIRECTION ( 'NONE',  ( -0.9903960388894593736, -0.05258684961124808488, -0.1278683283695876416 ) ) ;
#10070=EDGE_LOOP ( 'NONE', ( #15833, #19893, #9400, #39559 ) ) ;
#10077=CARTESIAN_POINT ( 'NONE',  ( 0.04088380661261944299, -1.519926711703535327, -0.3733014666261871839 ) ) ;
#10091=( BOUNDED_SURFACE ( )  B_SPLINE_SURFACE ( 3, 2, ( 
 ( #39861, #11680, #39646 ),
 ( #8787, #36574, #17837 ),
 ( #27521, #1634, #14349 ),
 ( #39444, #30398, #23838 ),
 ( #2230, #24435, #21363 ),
 ( #5700, #14768, #27331 ) ),
 .UNSPECIFIED., .F., .F., .F. ) 
 B_SPLINE_SURFACE_WITH_KNOTS ( ( 4, 2, 4 ),
 ( 3, 3 ),
 ( 6.179952383167375274E-18, 0.0007344380730649742277, 0.001468876146129942384 ),
 ( 0.000000000000000000, 1.000000000000000000 ),
 .UNSPECIFIED. ) 
 GEOMETRIC_REPRESENTATION_ITEM ( )  RATIONAL_B_SPLINE_SURFACE ( (
 ( 1.000000000000000000, 0.8219793159978235897, 1.000000000000000000),
 ( 1.000000000000000000, 0.8695169202949041276, 1.000000000000000000),
 ( 1.000000000000000000, 0.9157158777252236703, 1.000000000000000000),
 ( 1.000000000000000000, 0.9814457743411639790, 1.000000000000000000),
 ( 1.000000000000000000, 1.000262163779328528, 1.000000000000000000),
 ( 1.000000000000000000, 1.000000000000000000, 1.000000000000000000) ) ) 
 REPRESENTATION_ITEM ( '' )  SURFACE ( )  );
#10100=CIRCLE ( 'NONE', #6150, 0.01000000000000002970 ) ;
#10103=CARTESIAN_POINT ( 'NONE',  ( 0.3777603768608356338, -1.691903399793905027, -0.6926901660271995720 ) ) ;
#10120=CARTESIAN_POINT ( 'NONE',  ( 0.6379677522609080720, -1.610970530618076380, -0.5598555352862202295 ) ) ;
#10129=CARTESIAN_POINT ( 'NONE',  ( 0.6273212425429852690, -1.617116560689232152, -0.5218031926553677868 ) ) ;
#10133=EDGE_CURVE ( 'NONE', #24018, #38684, #18526, .T. ) ;
#10137=AXIS2_PLACEMENT_3D ( 'NONE', #30994, #27924, #8781 ) ;
#10138=CARTESIAN_POINT ( 'NONE',  ( 0.4631642984387073780, -1.593038035242256401, -0.6007335213492860371 ) ) ;
#10140=TOROIDAL_SURFACE ( 'NONE', #23961, 0.08830708661417323302, 0.01499999999999999944 ) ;
#10143=CARTESIAN_POINT ( 'NONE',  ( 0.4528109813659910721, -1.108023691146801548, -0.3699862881067115250 ) ) ;
#10155=AXIS2_PLACEMENT_3D ( 'NONE', #17696, #30463, #1697 ) ;
#10161=EDGE_LOOP ( 'NONE', ( #36264, #10185, #9904, #37774 ) ) ;
#10165=ORIENTED_EDGE ( 'NONE', *, *, #19009, .T. ) ;
#10170=CARTESIAN_POINT ( 'NONE',  ( 0.3595150996541451871, -1.929818105082974800, -0.5025626374741613001 ) ) ;
#10171=CARTESIAN_POINT ( 'NONE',  ( 0.2817715218429098223, -1.549959437726055933, -0.3415684628476097218 ) ) ;
#10185=ORIENTED_EDGE ( 'NONE', *, *, #5475, .T. ) ;
#10192=CIRCLE ( 'NONE', #11513, 0.09088067974298034979 ) ;
#10206=CARTESIAN_POINT ( 'NONE',  ( 0.5313741818379943416, -1.669536910112647377, -0.5811632390357616140 ) ) ;
#10218=ORIENTED_EDGE ( 'NONE', *, *, #17180, .F. ) ;
#10223=DIRECTION ( 'NONE',  ( 0.8660512985181133550, 0.4999551463232373982, 0.000000000000000000 ) ) ;
#10231=DIRECTION ( 'NONE',  ( -0.8153658488301590568, -0.4895179469056346044, -0.3091127823606886760 ) ) ;
#10236=CARTESIAN_POINT ( 'NONE',  ( 0.3409152363046567547, -1.516880185093696154, -0.5318766032426672785 ) ) ;
#10237=CARTESIAN_POINT ( 'NONE',  ( 0.1845478187330835684, -1.892088228647428094, -0.3405287551785696754 ) ) ;
#10240=VERTEX_POINT ( 'NONE', #32539 ) ;
#10246=FACE_OUTER_BOUND ( 'NONE', #21201, .T. ) ;
#10247=CARTESIAN_POINT ( 'NONE',  ( 0.4119477494091341452, -1.689530741032903238, -0.6036133972602488740 ) ) ;
#10250=CARTESIAN_POINT ( 'NONE',  ( 0.1999999999999788058, -2.097675824466502803, -0.2588528740066096678 ) ) ;
#10252=AXIS2_PLACEMENT_3D ( 'NONE', #26683, #30154, #39404 ) ;
#10253=CIRCLE ( 'NONE', #18139, 0.1033070866141732325 ) ;
#10255=CARTESIAN_POINT ( 'NONE',  ( 0.1750363347825162064, -1.731740520214466450, -0.6813996879367362203 ) ) ;
#10264=DIRECTION ( 'NONE',  ( 0.4999551463232373427, -0.8660512985181134660, 0.000000000000000000 ) ) ;
#10274=CARTESIAN_POINT ( 'NONE',  ( 0.5137193753217319525, -1.640798741474252420, -0.6166062277181030282 ) ) ;
#10275=DIRECTION ( 'NONE',  ( 0.8660512985181134660, 0.4999551463232372317, 0.000000000000000000 ) ) ;
#10287=CARTESIAN_POINT ( 'NONE',  ( 0.3491199008570403661, -1.710663813406571254, -0.5475265892256320210 ) ) ;
#10290=EDGE_LOOP ( 'NONE', ( #18306, #33123, #3377, #35046, #21256, #33479, #39705, #16452, #35869, #5049, #24108, #16945, #21167, #31076, #7250, #24284 ) ) ;
#10297=CARTESIAN_POINT ( 'NONE',  ( 0.1106902893256054288, -1.391740630825941905, -0.3302364130144593291 ) ) ;
#10299=ADVANCED_FACE ( 'NONE', ( #16918 ), #16716, .T. ) ;
#10317=CARTESIAN_POINT ( 'NONE',  ( 0.1976446668592635181, -2.032347859264719059, -0.6786056056212084187 ) ) ;
#10320=CARTESIAN_POINT ( 'NONE',  ( 0.3707960435722095216, -1.730448033722604251, -0.6824770964179540655 ) ) ;
#10331=VERTEX_POINT ( 'NONE', #20214 ) ;
#10334=DIRECTION ( 'NONE',  ( 0.8660512985181133550, 0.4999551463232373427, 9.313118160219073865E-16 ) ) ;
#10335=CARTESIAN_POINT ( 'NONE',  ( 0.6293241097234876236, -1.615960343088709505, -0.5667764449061211129 ) ) ;
#10337=EDGE_CURVE ( 'NONE', #23348, #6307, #28233, .T. ) ;
#10342=APPLICATION_CONTEXT ( 'configuration controlled 3d designs of mechanical parts and assemblies' ) ;
#10344=( BOUNDED_SURFACE ( )  B_SPLINE_SURFACE ( 3, 2, ( 
 ( #32064, #3872, #26506 ),
 ( #10453, #35959, #25914 ),
 ( #20140, #26719, #39248 ),
 ( #19531, #23019, #32456 ) ),
 .UNSPECIFIED., .F., .F., .T. ) 
 B_SPLINE_SURFACE_WITH_KNOTS ( ( 4, 4 ),
 ( 3, 3 ),
 ( 0.000000000000000000, 0.0002767335164478071353 ),
 ( 0.000000000000000000, 1.000000000000000000 ),
 .UNSPECIFIED. ) 
 GEOMETRIC_REPRESENTATION_ITEM ( )  RATIONAL_B_SPLINE_SURFACE ( (
 ( 1.000000000000000000, 0.7071328584466077816, 1.000000000000000000),
 ( 1.000000000000000000, 0.7071158410878489731, 1.000000000000000000),
 ( 1.000000000000000000, 0.7071067847848822030, 1.000000000000000000),
 ( 1.000000000000000000, 0.7071067811865467956, 1.000000000000000000) ) ) 
 REPRESENTATION_ITEM ( '' )  SURFACE ( )  );
#10346=ORIENTED_EDGE ( 'NONE', *, *, #19973, .F. ) ;
#10351=CARTESIAN_POINT ( 'NONE',  ( 0.3316968599837757381, -1.522201780612220112, -0.7090643400862902679 ) ) ;
#10352=CARTESIAN_POINT ( 'NONE',  ( 0.5156646344045052732, -1.614467889434319625, -0.5600385693181707536 ) ) ;
#10356=CARTESIAN_POINT ( 'NONE',  ( 0.4795819664771984736, -1.106247336020415917, -0.4111404562665418871 ) ) ;
#10364=CARTESIAN_POINT ( 'NONE',  ( 0.1424029337235096226, -1.400533250147911746, -0.3552704771134632677 ) ) ;
#10375=CARTESIAN_POINT ( 'NONE',  ( 0.2901625129748762189, -1.544549902221894255, -0.3389314648480827308 ) ) ;
#10382=FACE_OUTER_BOUND ( 'NONE', #8594, .T. ) ;
#10386=CARTESIAN_POINT ( 'NONE',  ( 0.6343156381093978391, -1.595758837318228318, -0.5875140676452393906 ) ) ;
#10396=CARTESIAN_POINT ( 'NONE',  ( 0.5454085514665598655, -1.664197832243224262, -0.5577771241037264849 ) ) ;
#10401=ADVANCED_FACE ( 'NONE', ( #29873 ), #4778, .T. ) ;
#10410=ORIENTED_EDGE ( 'NONE', *, *, #26256, .T. ) ;
#10412=CARTESIAN_POINT ( 'NONE',  ( 0.3946348076106268588, -1.611793502148812340, -0.3621938603178055383 ) ) ;
#10413=DIRECTION ( 'NONE',  ( 0.000000000000000000, 0.7095423125567595912, -0.7046628319214841563 ) ) ;
#10414=CARTESIAN_POINT ( 'NONE',  ( 0.1909286924077258640, -1.257064795538239244, -0.7462941026102620778 ) ) ;
#10416=FACE_OUTER_BOUND ( 'NONE', #24481, .T. ) ;
#10418=CARTESIAN_POINT ( 'NONE',  ( 0.5768838759879602041, -1.536724830852129520, -0.5579058299699864998 ) ) ;
#10435=CARTESIAN_POINT ( 'NONE',  ( 0.1045181657808564313, -1.266534658925821732, -0.5155029497116575543 ) ) ;
#10441=CARTESIAN_POINT ( 'NONE',  ( 0.3927073942151048658, -1.776709627579699413, -0.7060183551223596643 ) ) ;
#10451=CARTESIAN_POINT ( 'NONE',  ( 0.5895895133292542445, -1.562273338605467021, -0.5541701122963066384 ) ) ;
#10453=CARTESIAN_POINT ( 'NONE',  ( -2.125292368820994835E-14, -2.101103427206035601, -0.2895067271637098982 ) ) ;
#10467=CARTESIAN_POINT ( 'NONE',  ( 0.3553775023099885466, -1.749316302220775832, -0.5487481164399209410 ) ) ;
#10470=ORIENTED_EDGE ( 'NONE', *, *, #20567, .F. ) ;
#10476=CARTESIAN_POINT ( 'NONE',  ( 0.005127655334880022210, -1.809120478639261176, -0.3273012655191571696 ) ) ;
#10483=DIRECTION ( 'NONE',  ( 0.4999551463232373427, -0.8660512985181134660, 0.000000000000000000 ) ) ;
#10492=B_SPLINE_CURVE_WITH_KNOTS ( 'NONE', 3,
 ( #8777, #15149, #12079, #2814 ),
 .UNSPECIFIED., .F., .F.,
 ( 4, 4 ),
 ( 0.000000000000000000, 0.001825717054875163579 ),
 .UNSPECIFIED. ) ;
#10494=CARTESIAN_POINT ( 'NONE',  ( 0.1759300380180284507, -1.231083256582695684, -0.4125659523519146221 ) ) ;
#10498=CARTESIAN_POINT ( 'NONE',  ( 0.2002642730199227783, -1.651659577068177676, -0.6582679755329989835 ) ) ;
#10501=CARTESIAN_POINT ( 'NONE',  ( 0.1761268469877938225, -1.381065068506146298, -0.3150366247064029235 ) ) ;
#10514=ORIENTED_EDGE ( 'NONE', *, *, #37719, .F. ) ;
#10522=ORIENTED_EDGE ( 'NONE', *, *, #10982, .T. ) ;
#10530=CARTESIAN_POINT ( 'NONE',  ( 0.4935456730871101150, -1.587903313234494629, -0.4610633267758252329 ) ) ;
#10534=CARTESIAN_POINT ( 'NONE',  ( 0.3332516724025844645, -1.614750829017314926, -0.6926149471072686747 ) ) ;
#10551=CARTESIAN_POINT ( 'NONE',  ( 0.2059273467974224725, -1.283046334493782137, -0.3824824602286829855 ) ) ;
#10553=TOROIDAL_SURFACE ( 'NONE', #3969, 0.05330708661417323663, 0.01000000000000000021 ) ;
#10554=CARTESIAN_POINT ( 'NONE',  ( 0.6473787150721044270, -1.455279521797666176, -0.6250000000000000000 ) ) ;
#10556=CARTESIAN_POINT ( 'NONE',  ( 0.5318889985472864401, -1.659866604704374637, -0.4542321257220686137 ) ) ;
#10558=ORIENTED_EDGE ( 'NONE', *, *, #38815, .T. ) ;
#10563=CARTESIAN_POINT ( 'NONE',  ( 0.3587246564956185768, -1.771947280444475137, -0.5205743448439883458 ) ) ;
#10564=CARTESIAN_POINT ( 'NONE',  ( 0.3819720823480106109, -1.699928762836120377, -0.3361580370732986101 ) ) ;
#10575=EDGE_LOOP ( 'NONE', ( #9603, #8229, #40192, #15636 ) ) ;
#10611=TOROIDAL_SURFACE ( 'NONE', #33598, 0.2200000000000000011, 0.02999999999999999889 ) ;
#10623=CARTESIAN_POINT ( 'NONE',  ( 0.2402595592073158148, -1.589192177423347285, -0.3527948934348379972 ) ) ;
#10632=CARTESIAN_POINT ( 'NONE',  ( 0.5586419605352853646, -1.622123839695630787, -0.4759077358386838985 ) ) ;
#10639=ADVANCED_FACE ( 'NONE', ( #12363 ), #15849, .F. ) ;
#10650=AXIS2_PLACEMENT_3D ( 'NONE', #32140, #29262, #29462 ) ;
#10655=CARTESIAN_POINT ( 'NONE',  ( 0.5781467389326836459, -1.533504052124724293, -0.5635290765616033370 ) ) ;
#10662=DIRECTION ( 'NONE',  ( 0.000000000000000000, 0.000000000000000000, -1.000000000000000000 ) ) ;
#10671=ORIENTED_EDGE ( 'NONE', *, *, #28489, .T. ) ;
#10678=CARTESIAN_POINT ( 'NONE',  ( 0.04075052232006950298, -1.520844532399347804, -0.3463593800647417065 ) ) ;
#10686=AXIS2_PLACEMENT_3D ( 'NONE', #13780, #33502, #26343 ) ;
#10693=EDGE_CURVE ( 'NONE', #35263, #23421, #30130, .T. ) ;
#10694=CARTESIAN_POINT ( 'NONE',  ( 0.1999999999999789724, -2.183180860297921466, -0.4937760292030871079 ) ) ;
#10702=CARTESIAN_POINT ( 'NONE',  ( 0.4259907721281001036, -1.086727892038337417, -0.5155029497116575543 ) ) ;
#10704=EDGE_CURVE ( 'NONE', #1646, #32089, #37998, .T. ) ;
#10707=CIRCLE ( 'NONE', #13985, 0.1033070866141732880 ) ;
#10720=CIRCLE ( 'NONE', #21246, 0.2000000000000000111 ) ;
#10728=CARTESIAN_POINT ( 'NONE',  ( 0.3595715536228106801, -1.625401886829162423, -0.3696110269036073093 ) ) ;
#10743=CARTESIAN_POINT ( 'NONE',  ( 0.3995269031511867741, -1.597602329235723095, -0.3111376553386354105 ) ) ;
#10753=DIRECTION ( 'NONE',  ( 0.8660512985181130219, 0.4999551463232378978, -1.983296656985678775E-15 ) ) ;
#10771=ORIENTED_EDGE ( 'NONE', *, *, #5874, .T. ) ;
#10774=ORIENTED_EDGE ( 'NONE', *, *, #33119, .F. ) ;
#10776=CARTESIAN_POINT ( 'NONE',  ( -1.310828011476809540E-05, -2.055032695347356331, -0.7138301564589908388 ) ) ;
#10778=VERTEX_POINT ( 'NONE', #13919 ) ;
#10792=DIRECTION ( 'NONE',  ( 0.8660512985181132439, 0.4999551463232374537, 0.000000000000000000 ) ) ;
#10803=CIRCLE ( 'NONE', #21333, 0.1033070866141734129 ) ;
#10804=DIRECTION ( 'NONE',  ( 0.8660512985181130219, 0.4999551463232377868, 0.000000000000000000 ) ) ;
#10812=CARTESIAN_POINT ( 'NONE',  ( 0.4807327490442517282, -1.659256856822121540, -0.6108297979790577870 ) ) ;
#10822=CARTESIAN_POINT ( 'NONE',  ( 0.3650945375302141471, -1.739603212589635461, -0.4849876925477283884 ) ) ;
#10834=CARTESIAN_POINT ( 'NONE',  ( 0.5795887036850762009, -1.527265703570089617, -0.4600246038137717486 ) ) ;
#10837=CARTESIAN_POINT ( 'NONE',  ( 0.5046384106032315575, -1.676392394905552585, -0.5155029497116575543 ) ) ;
#10840=CARTESIAN_POINT ( 'NONE',  ( 0.3925301276612754298, -1.756377271995033684, -0.4843757382520948451 ) ) ;
#10844=CARTESIAN_POINT ( 'NONE',  ( 0.4679018147548930084, -1.094320404139347058, -0.6313355493825374420 ) ) ;
#10851=AXIS2_PLACEMENT_3D ( 'NONE', #28111, #27500, #5681 ) ;
#10862=CARTESIAN_POINT ( 'NONE',  ( 0.6186972872989504602, -1.565036408902899634, -0.5905337336510069202 ) ) ;
#10866=CARTESIAN_POINT ( 'NONE',  ( 0.4262438152663738933, -1.592651821845863402, -0.6151431148613257793 ) ) ;
#10870=CARTESIAN_POINT ( 'NONE',  ( 0.6116753299763959539, -1.502912699639540550, -0.6106436555062486615 ) ) ;
#10879=CARTESIAN_POINT ( 'NONE',  ( 0.4428400309745523233, -1.146281092196613338, -0.3830631589809550541 ) ) ;
#10880=CARTESIAN_POINT ( 'NONE',  ( 0.3743765113291571689, -1.762474601098698024, -0.5779735398402915392 ) ) ;
#10883=CARTESIAN_POINT ( 'NONE',  ( 0.3445219659096331322, -1.630113034086819290, -0.4330379103484555681 ) ) ;
#10886=ORIENTED_EDGE ( 'NONE', *, *, #39431, .F. ) ;
#10889=EDGE_LOOP ( 'NONE', ( #40314, #984, #27024, #13140 ) ) ;
#10895=CARTESIAN_POINT ( 'NONE',  ( 0.003504163894631640280, -1.844708889207917313, -0.3218820310881243540 ) ) ;
#10899=CARTESIAN_POINT ( 'NONE',  ( 9.222166083094558481E-05, -2.006822057499934697, -0.6711564558286039484 ) ) ;
#10906=CARTESIAN_POINT ( 'NONE',  ( 0.5306085078623116180, -1.660610003246502986, -0.5787814785457732203 ) ) ;
#10921=FACE_OUTER_BOUND ( 'NONE', #39060, .T. ) ;
#10922=EDGE_CURVE ( 'NONE', #31364, #16583, #17892, .T. ) ;
#10937=AXIS2_PLACEMENT_3D ( 'NONE', #6173, #15040, #60 ) ;
#10940=( BOUNDED_SURFACE ( )  B_SPLINE_SURFACE ( 3, 2, ( 
 ( #24720, #18947, #40537 ),
 ( #18522, #25109, #40327 ),
 ( #37650, #34152, #9467 ),
 ( #6568, #22247, #22441 ),
 ( #9253, #2899, #12359 ),
 ( #18741, #21630, #31482 ) ),
 .UNSPECIFIED., .F., .F., .F. ) 
 B_SPLINE_SURFACE_WITH_KNOTS ( ( 4, 2, 4 ),
 ( 3, 3 ),
 ( -3.523657060577889411E-18, 0.0007344380730649657709, 0.001468876146129935011 ),
 ( 0.000000000000000000, 1.000000000000000000 ),
 .UNSPECIFIED. ) 
 GEOMETRIC_REPRESENTATION_ITEM ( )  RATIONAL_B_SPLINE_SURFACE ( (
 ( 1.000000000000000000, 0.8219793159978276975, 1.000000000000000000),
 ( 1.000000000000000000, 0.8695169202949302178, 1.000000000000000000),
 ( 1.000000000000000000, 0.9157158777251862558, 1.000000000000000000),
 ( 1.000000000000000000, 0.9814457743412016155, 1.000000000000000000),
 ( 1.000000000000000000, 1.000262163779300995, 1.000000000000000000),
 ( 1.000000000000000000, 1.000000000000000000, 1.000000000000000000) ) ) 
 REPRESENTATION_ITEM ( '' )  SURFACE ( )  );
#10943=CARTESIAN_POINT ( 'NONE',  ( 0.4835349102845575842, -1.678212234975946293, -0.3866364743305659157 ) ) ;
#10945=CARTESIAN_POINT ( 'NONE',  ( 0.4409062655693438137, -1.690090444797295977, -0.7462941026102624109 ) ) ;
#10956=CARTESIAN_POINT ( 'NONE',  ( 0.4341912152387207291, -1.592006445115355273, -0.4177668494440743285 ) ) ;
#10958=CARTESIAN_POINT ( 'NONE',  ( 0.4104061326339791815, -1.719843444618068595, -0.4250636112545012613 ) ) ;
#10959=CARTESIAN_POINT ( 'NONE',  ( 0.3722076170955361252, -1.592376083966843714, -0.7090645075809880460 ) ) ;
#10967=LENGTH_MEASURE_WITH_UNIT ( LENGTH_MEASURE( 0.02539999999999999897 ), #38919 );
#10976=DIRECTION ( 'NONE',  ( 0.000000000000000000, 1.000000000000000000, -1.224646799147353207E-16 ) ) ;
#10978=EDGE_CURVE ( 'NONE', #31057, #37937, #22537, .T. ) ;
#10979=ORIENTED_EDGE ( 'NONE', *, *, #12200, .F. ) ;
#10980=CARTESIAN_POINT ( 'NONE',  ( 0.3408288395586620556, -1.672135129142385379, -0.5725068027761680556 ) ) ;
#10982=EDGE_CURVE ( 'NONE', #8354, #34456, #5119, .T. ) ;
#10984=CARTESIAN_POINT ( 'NONE',  ( 0.3844041218437064811, -1.810736139791024435, -0.4824699277892320337 ) ) ;
#10987=CARTESIAN_POINT ( 'NONE',  ( 0.5457082879296111244, -1.652683526200752206, -0.4845594716743291119 ) ) ;
#10992=CARTESIAN_POINT ( 'NONE',  ( 0.1141769515801121238, -1.332194933707445017, -0.6802792144121206919 ) ) ;
#10998=DIRECTION ( 'NONE',  ( 0.8660512985181136880, 0.4999551463232368431, 0.000000000000000000 ) ) ;
#11006=ORIENTED_EDGE ( 'NONE', *, *, #21937, .T. ) ;
#11012=DIRECTION ( 'NONE',  ( -0.8400989100995858161, 0.000000000000000000, 0.5424332412836514461 ) ) ;
#11033=CARTESIAN_POINT ( 'NONE',  ( 0.3703394740834939913, -1.759797141953248323, -0.4296865123946668197 ) ) ;
#11036=CARTESIAN_POINT ( 'NONE',  ( 0.1999999999999789724, -2.183180860297921466, -0.4937760292030871079 ) ) ;
#11038=CARTESIAN_POINT ( 'NONE',  ( 0.5816799176160351026, -1.521122139812363550, -0.5782616316121675926 ) ) ;
#11040=B_SPLINE_CURVE_WITH_KNOTS ( 'NONE', 3,
 ( #3901, #38057, #34578, #13583 ),
 .UNSPECIFIED., .F., .F.,
 ( 4, 4 ),
 ( 0.000000000000000000, 0.0002767576745124534663 ),
 .UNSPECIFIED. ) ;
#11041=CARTESIAN_POINT ( 'NONE',  ( 0.1759300380180284507, -1.231083256582695684, -0.4125659523519146221 ) ) ;
#11042=ORIENTED_EDGE ( 'NONE', *, *, #6180, .F. ) ;
#11047=CARTESIAN_POINT ( 'NONE',  ( 0.5338352526116463270, -1.174566725300919989, -0.4248180574663139586 ) ) ;
#11057=CARTESIAN_POINT ( 'NONE',  ( 0.3848779947554198944, -1.747748222921210903, -0.4374302019815166642 ) ) ;
#11059=CARTESIAN_POINT ( 'NONE',  ( 0.3925301276612723211, -1.756377271995031020, -0.4843757382520817445 ) ) ;
#11063=CARTESIAN_POINT ( 'NONE',  ( 0.5747947170275361506, -1.612684560496418174, -0.5055484516149173491 ) ) ;
#11068=CARTESIAN_POINT ( 'NONE',  ( 0.5945517648669413902, -1.497934605890146154, -0.6409792228890591748 ) ) ;
#11080=CARTESIAN_POINT ( 'NONE',  ( 0.6229690016365089233, -1.526593058827372174, -0.3991335894808961116 ) ) ;
#11087=DIRECTION ( 'NONE',  ( 0.000000000000000000, 0.000000000000000000, -1.000000000000000000 ) ) ;
#11093=CARTESIAN_POINT ( 'NONE',  ( 0.3699999999999783462, -2.120664306612686012, -0.5256090310107919272 ) ) ;
#11099=CARTESIAN_POINT ( 'NONE',  ( 0.09537675404226049480, -1.364128109777166475, -0.3613912495262363023 ) ) ;
#11100=EDGE_CURVE ( 'NONE', #5197, #12681, #36026, .T. ) ;
#11114=CARTESIAN_POINT ( 'NONE',  ( 0.3986312341787107694, -2.053945766513980864, -0.5118724213368843756 ) ) ;
#11121=CARTESIAN_POINT ( 'NONE',  ( 0.4670757733960571034, -1.683842906665585337, -0.4131506686299025732 ) ) ;
#11123=ORIENTED_EDGE ( 'NONE', *, *, #5874, .F. ) ;
#11126=EDGE_LOOP ( 'NONE', ( #28397, #2615, #34707, #23424 ) ) ;
#11134=CARTESIAN_POINT ( 'NONE',  ( 0.2009282062366657129, -1.274386533297698909, -0.7137155460508515237 ) ) ;
#11136=ORIENTED_EDGE ( 'NONE', *, *, #32611, .T. ) ;
#11137=CARTESIAN_POINT ( 'NONE',  ( 0.2120815815383247649, -1.521234644788605150, -0.3529678530972831796 ) ) ;
#11143=CARTESIAN_POINT ( 'NONE',  ( 0.1994740068363786423, -2.042640899752901085, -0.2765909798240093198 ) ) ;
#11146=EDGE_CURVE ( 'NONE', #34108, #13144, #21842, .T. ) ;
#11153=ADVANCED_FACE ( 'NONE', ( #33111 ), #8703, .F. ) ;
#11155=EDGE_CURVE ( 'NONE', #28743, #21660, #2175, .T. ) ;
#11165=CARTESIAN_POINT ( 'NONE',  ( 0.3487950145890576503, -1.709514507286181262, -0.5484001082352915057 ) ) ;
#11169=CARTESIAN_POINT ( 'NONE',  ( 0.3853448888748426393, -1.884999421977940015, -0.5123789408289101122 ) ) ;
#11175=CARTESIAN_POINT ( 'NONE',  ( 0.003157895387556955251, -1.847058397352856485, -0.6456400114880085361 ) ) ;
#11182=CARTESIAN_POINT ( 'NONE',  ( 0.3572222731481287661, -1.622781385286526934, -0.3671481750039431446 ) ) ;
#11196=CARTESIAN_POINT ( 'NONE',  ( 0.4584717390208091770, -1.703043547193807017, -0.5155029497116575543 ) ) ;
#11198=DIRECTION ( 'NONE',  ( -1.000000000000000000, -0.000000000000000000, -0.000000000000000000 ) ) ;
#11199=CARTESIAN_POINT ( 'NONE',  ( 0.3948319565448157875, -1.761998452218138445, -0.7106721340409676291 ) ) ;
#11200=EDGE_CURVE ( 'NONE', #25557, #23099, #9380, .T. ) ;
#11210=EDGE_CURVE ( 'NONE', #17083, #33728, #33019, .T. ) ;
#11218=CARTESIAN_POINT ( 'NONE',  ( 0.4165782488800118810, -1.609873178559232176, -0.3634132145561362326 ) ) ;
#11227=ORIENTED_EDGE ( 'NONE', *, *, #33623, .T. ) ;
#11239=DIRECTION ( 'NONE',  ( 0.8660512985181135770, 0.4999551463232371207, 0.000000000000000000 ) ) ;
#11243=CARTESIAN_POINT ( 'NONE',  ( 0.3693472207122593387, -1.758516063299185195, -0.4275751132368607599 ) ) ;
#11244=CIRCLE ( 'NONE', #3335, 0.04330708661417322775 ) ;
#11246=CIRCLE ( 'NONE', #15863, 0.05000000000000000971 ) ;
#11249=CARTESIAN_POINT ( 'NONE',  ( 0.3933751395322767075, -1.752169251404669836, -0.4834917239368273223 ) ) ;
#11251=CARTESIAN_POINT ( 'NONE',  ( 0.3627000673212703030, -1.755081015781649656, -0.5954581570135634161 ) ) ;
#11254=CARTESIAN_POINT ( 'NONE',  ( 0.6226077036546983079, -1.616690395946017489, -0.5571391715294409241 ) ) ;
#11262=CARTESIAN_POINT ( 'NONE',  ( 0.5786394055816501680, -1.530760785047180272, -0.4642196941395432264 ) ) ;
#11264=CARTESIAN_POINT ( 'NONE',  ( 0.2617674847955998030, -1.607303447862003631, -0.3199733892743805708 ) ) ;
#11265=AXIS2_PLACEMENT_3D ( 'NONE', #16062, #12975, #38054 ) ;
#11268=ADVANCED_FACE ( 'NONE', ( #23484 ), #36194, .F. ) ;
#11277=EDGE_LOOP ( 'NONE', ( #23490, #19581, #15490, #32458, #39385, #7204, #14400 ) ) ;
#11279=CARTESIAN_POINT ( 'NONE',  ( 0.003604657698724842135, -1.841449275801259056, -0.3518445214664046028 ) ) ;
#11290=CARTESIAN_POINT ( 'NONE',  ( 3.007606603700621411E-05, -2.025203935284336065, -0.6754650421693230156 ) ) ;
#11298=ADVANCED_BREP_SHAPE_REPRESENTATION ( '', ( #4903, #27819 ), #23225 ) ;
#11307=CIRCLE ( 'NONE', #25119, 0.05330708661417327826 ) ;
#11315=EDGE_LOOP ( 'NONE', ( #13394, #3272, #14839, #22386 ) ) ;
#11316=ORIENTED_EDGE ( 'NONE', *, *, #5489, .F. ) ;
#11324=ORIENTED_EDGE ( 'NONE', *, *, #25393, .T. ) ;
#11331=CARTESIAN_POINT ( 'NONE',  ( 0.5406636675755426280, -1.597291370477161410, -0.4587226045079861314 ) ) ;
#11335=FACE_OUTER_BOUND ( 'NONE', #21918, .T. ) ;
#11337=EDGE_LOOP ( 'NONE', ( #12211, #37687, #23352, #40094, #27980, #12138, #12738, #31279, #21265 ) ) ;
#11338=DIRECTION ( 'NONE',  ( 0.000000000000000000, 1.000000000000000000, -1.224646799147353207E-16 ) ) ;
#11345=CARTESIAN_POINT ( 'NONE',  ( 0.4054385157837457898, -1.690091043903728663, -0.4198998561151282005 ) ) ;
#11346=CARTESIAN_POINT ( 'NONE',  ( 0.3795613398208534384, -1.760143698493221942, -0.5723197561600823491 ) ) ;
#11349=CARTESIAN_POINT ( 'NONE',  ( 0.3999999999999788169, -2.120743408781763595, -0.4622665795123166999 ) ) ;
#11355=CARTESIAN_POINT ( 'NONE',  ( 0.2026016520682514532, -1.284966195589533067, -0.7446434123579800390 ) ) ;
#11361=CIRCLE ( 'NONE', #4119, 0.04330708661417340122 ) ;
#11362=CIRCLE ( 'NONE', #18589, 0.03000000000000003358 ) ;
#11365=AXIS2_PLACEMENT_3D ( 'NONE', #7324, #1024, #38412 ) ;
#11366=ORIENTED_EDGE ( 'NONE', *, *, #36357, .T. ) ;
#11377=CARTESIAN_POINT ( 'NONE',  ( 0.004836683785373215722, -1.808528659688425577, -0.6707443805300201678 ) ) ;
#11378=CARTESIAN_POINT ( 'NONE',  ( 0.5227242486541291422, -1.180980899171317322, -0.4111404562665418871 ) ) ;
#11383=ORIENTED_EDGE ( 'NONE', *, *, #12837, .F. ) ;
#11384=CARTESIAN_POINT ( 'NONE',  ( 0.1998159314661579755, -2.070111469871240395, -0.2999320603925721973 ) ) ;
#11399=( GEOMETRIC_REPRESENTATION_CONTEXT ( 3 ) GLOBAL_UNCERTAINTY_ASSIGNED_CONTEXT ( ( #15737 ) ) GLOBAL_UNIT_ASSIGNED_CONTEXT ( ( #1126, #26195, #23112 ) ) REPRESENTATION_CONTEXT ( 'NONE', 'WORKASPACE' ) );
#11400=EDGE_CURVE ( 'NONE', #4182, #3488, #26722, .T. ) ;
#11405=CARTESIAN_POINT ( 'NONE',  ( 0.3937935369999097657, -1.750528853568169341, -0.7155743560682789051 ) ) ;
#11409=( BOUNDED_SURFACE ( )  B_SPLINE_SURFACE ( 3, 2, ( 
 ( #34146, #2683, #12148 ),
 ( #27992, #37433, #9245 ),
 ( #15641, #21822, #28388 ),
 ( #28188, #53, #37640 ),
 ( #9459, #257, #12755 ),
 ( #22647, #16654, #32083 ),
 ( #32475, #13755, #32267 ),
 ( #471, #29203, #29408 ),
 ( #12968, #35177, #16444 ),
 ( #6980, #26321, #22433 ) ),
 .UNSPECIFIED., .F., .F., .F. ) 
 B_SPLINE_SURFACE_WITH_KNOTS ( ( 4, 2, 2, 2, 4 ),
 ( 3, 3 ),
 ( 1.517883041479706208E-18, 0.0005537231258318653241, 0.001107446251663729130, 0.001661169377495592828, 0.002214892503327456526 ),
 ( 0.000000000000000000, 1.000000000000000000 ),
 .UNSPECIFIED. ) 
 GEOMETRIC_REPRESENTATION_ITEM ( )  RATIONAL_B_SPLINE_SURFACE ( (
 ( 1.000000000000000000, 0.7071067811865474617, 1.000000000000000000),
 ( 1.000000000000000000, 0.7265894298401162077, 1.000000000000000000),
 ( 1.000000000000000000, 0.7434232128335919176, 1.000000000000000000),
 ( 1.000000000000000000, 0.7721148371329119575, 1.000000000000000000),
 ( 1.000000000000000000, 0.7840904396559796874, 1.000000000000000000),
 ( 1.000000000000000000, 0.8021033243800309576, 1.000000000000000000),
 ( 1.000000000000000000, 0.8082547127764595496, 1.000000000000000000),
 ( 1.000000000000000000, 0.8155145129532223036, 1.000000000000000000),
 ( 1.000000000000000000, 0.8165278830576885305, 1.000000000000000000),
 ( 1.000000000000000000, 0.8164965809277219266, 1.000000000000000000) ) ) 
 REPRESENTATION_ITEM ( '' )  SURFACE ( )  );
#11411=CARTESIAN_POINT ( 'NONE',  ( 0.09022811215523972306, -1.443092559558259991, -0.3376645326784880052 ) ) ;
#11412=CARTESIAN_POINT ( 'NONE',  ( 0.1986386779382385004, -2.044490618953881178, -0.6815266969527320473 ) ) ;
#11423=CIRCLE ( 'NONE', #39669, 0.04330708661417327632 ) ;
#11432=CARTESIAN_POINT ( 'NONE',  ( 0.1870594047279228178, -1.705895718177093290, -0.3287721483933107591 ) ) ;
#11437=ADVANCED_FACE ( 'NONE', ( #27562 ), #40083, .F. ) ;
#11439=ORIENTED_EDGE ( 'NONE', *, *, #35638, .T. ) ;
#11441=EDGE_CURVE ( 'NONE', #19986, #33249, #21796, .T. ) ;
#11444=DIRECTION ( 'NONE',  ( 0.4999551463232373427, -0.8660512985181134660, 0.000000000000000000 ) ) ;
#11451=CARTESIAN_POINT ( 'NONE',  ( 0.02999778723028691946, -2.087755359801442445, -0.2623954751430958021 ) ) ;
#11463=CARTESIAN_POINT ( 'NONE',  ( 0.3969982963057271386, -1.750077671058422712, -0.4821875037442190370 ) ) ;
#11464=TOROIDAL_SURFACE ( 'NONE', #40379, 0.1333070866141734256, 0.02999999999999999889 ) ;
#11469=CARTESIAN_POINT ( 'NONE',  ( 0.6191930749538706591, -1.620849352080218742, -0.5429756578775681852 ) ) ;
#11475=CARTESIAN_POINT ( 'NONE',  ( 0.3648248434763127768, -1.736370150272759316, -0.6021910921396982364 ) ) ;
#11482=DIRECTION ( 'NONE',  ( 0.8660512985181130219, 0.4999551463232377868, 0.000000000000000000 ) ) ;
#11491=ORIENTED_EDGE ( 'NONE', *, *, #2894, .T. ) ;
#11495=VECTOR ( 'NONE', #14333, 39.37007874015748143 ) ;
#11502=CARTESIAN_POINT ( 'NONE',  ( 0.5639234115582156814, -1.619074957229330369, -0.5155029497116575543 ) ) ;
#11503=ORIENTED_EDGE ( 'NONE', *, *, #30467, .T. ) ;
#11504=CARTESIAN_POINT ( 'NONE',  ( 0.1757436668871035501, -1.266759027082864586, -0.7075046458427431961 ) ) ;
#11506=EDGE_CURVE ( 'NONE', #19020, #6462, #27166, .T. ) ;
#11509=CARTESIAN_POINT ( 'NONE',  ( -2.112273405726188513E-14, -2.101105564483095822, -0.6980540538755429791 ) ) ;
#11513=AXIS2_PLACEMENT_3D ( 'NONE', #28245, #9527, #6618 ) ;
#11514=AXIS2_PLACEMENT_3D ( 'NONE', #37504, #24587, #39993 ) ;
#11534=CARTESIAN_POINT ( 'NONE',  ( 0.4570572541747411344, -1.685982556225596118, -0.4119774522368083169 ) ) ;
#11541=AXIS2_PLACEMENT_3D ( 'NONE', #24632, #15564, #34262 ) ;
#11544=EDGE_LOOP ( 'NONE', ( #26124, #34406, #9552, #16695, #28697, #3656 ) ) ;
#11548=DIRECTION ( 'NONE',  ( 0.2549153265716599392, 0.000000000000000000, 0.9669633789750592401 ) ) ;
#11553=CARTESIAN_POINT ( 'NONE',  ( 0.5934892211655993233, -1.486388914344519696, -0.3866566986715374021 ) ) ;
#11580=CIRCLE ( 'NONE', #31929, 0.03000000000000002318 ) ;
#11582=CARTESIAN_POINT ( 'NONE',  ( 0.3575561407676253745, -1.730055797317831434, -0.4930369608202382348 ) ) ;
#11586=ADVANCED_FACE ( 'NONE', ( #3264, #16030 ), #25910, .F. ) ;
#11588=CARTESIAN_POINT ( 'NONE',  ( 0.3722032372398466626, -1.759169682601392948, -0.4326628031163745614 ) ) ;
#11594=CARTESIAN_POINT ( 'NONE',  ( 0.1583587972720514880, -1.279555781728052288, -0.7002456816688629182 ) ) ;
#11595=CARTESIAN_POINT ( 'NONE',  ( 0.3616412802241140145, -1.759290408630901803, -0.5212859374495408815 ) ) ;
#11613=AXIS2_PLACEMENT_3D ( 'NONE', #32795, #30328, #23768 ) ;
#11616=( CONVERSION_BASED_UNIT ( 'INCH', #39785 ) LENGTH_UNIT ( ) NAMED_UNIT ( #26255 ) );
#11619=CARTESIAN_POINT ( 'NONE',  ( 0.3909325643991080068, -1.787092977304432173, -0.7036838712262254436 ) ) ;
#11628=CARTESIAN_POINT ( 'NONE',  ( 0.1909286924077255310, -1.257064795538239022, -0.3824824602286830411 ) ) ;
#11639=CARTESIAN_POINT ( 'NONE',  ( 0.2164472520689793289, -1.620189540922670313, -0.3270271536848740057 ) ) ;
#11641=CARTESIAN_POINT ( 'NONE',  ( 0.7009661026058806588, -1.563056106223300823, -0.5155029497116575543 ) ) ;
#11642=CARTESIAN_POINT ( 'NONE',  ( 0.2059273467974225835, -1.283046334493782359, -0.4400554600884078460 ) ) ;
#11653=CARTESIAN_POINT ( 'NONE',  ( 0.3905003066036929482, -1.793686422149088688, -0.5256265208041123183 ) ) ;
#11666=DIRECTION ( 'NONE',  ( -0.8660512985181132439, -0.4999551463232375648, 0.000000000000000000 ) ) ;
#11668=CARTESIAN_POINT ( 'NONE',  ( 0.6033773671567600472, -1.592159661714941832, -0.4857557934844767833 ) ) ;
#11672=CARTESIAN_POINT ( 'NONE',  ( 0.3755263365652165009, -1.754697207561586980, -0.4344311325575616611 ) ) ;
#11675=CARTESIAN_POINT ( 'NONE',  ( 0.4052584708005012026, -1.689779467654166201, -0.6110500361598382169 ) ) ;
#11680=CARTESIAN_POINT ( 'NONE',  ( 0.4679018147548930084, -1.094320404139347058, -0.6313355493825376641 ) ) ;
#11691=CARTESIAN_POINT ( 'NONE',  ( 0.07195434016001761579, -1.416717534487766272, -0.3655371694413775963 ) ) ;
#11698=DIRECTION ( 'NONE',  ( -0.8660512985181130219, -0.4999551463232378978, 0.000000000000000000 ) ) ;
#11725=ORIENTED_EDGE ( 'NONE', *, *, #12014, .T. ) ;
#11730=CARTESIAN_POINT ( 'NONE',  ( 0.4256128369825924462, -1.668893475541606053, -0.3965718019701741093 ) ) ;
#11734=VERTEX_POINT ( 'NONE', #4061 ) ;
#11739=CARTESIAN_POINT ( 'NONE',  ( 0.1834964085430285941, -1.226715333008844055, -0.5155029497116575543 ) ) ;
#11750=CARTESIAN_POINT ( 'NONE',  ( -2.128280327564064936E-14, -2.101101183304413311, -0.6980525384215444662 ) ) ;
#11752=CARTESIAN_POINT ( 'NONE',  ( 0.4144479545766268647, -1.706837603466250686, -0.4202405736507541789 ) ) ;
#11753=CARTESIAN_POINT ( 'NONE',  ( 0.3938619850121877763, -1.751888204654250325, -0.5728934638734284324 ) ) ;
#11769=CARTESIAN_POINT ( 'NONE',  ( 0.3500164589514257463, -1.719894267657803733, -0.4370873290842924308 ) ) ;
#11776=CARTESIAN_POINT ( 'NONE',  ( 0.3695052819757338458, -1.758428263776098621, -0.4278193900811942396 ) ) ;
#11777=CARTESIAN_POINT ( 'NONE',  ( 0.3923243630925575820, -1.966611948492509088, -0.4968729097669151162 ) ) ;
#11783=CARTESIAN_POINT ( 'NONE',  ( 0.1809287994913508502, -1.262837545876213108, -0.7414037396183945638 ) ) ;
#11784=CARTESIAN_POINT ( 'NONE',  ( 0.4356662251172991329, -1.610775558009423847, -0.3686272921855576756 ) ) ;
#11809=CARTESIAN_POINT ( 'NONE',  ( 0.4030327056921976792, -1.680968334469209680, -0.4031266960524464982 ) ) ;
#11822=AXIS2_PLACEMENT_3D ( 'NONE', #32909, #7618, #32712 ) ;
#11825=CARTESIAN_POINT ( 'NONE',  ( 0.3686706805007330390, -2.055989704601955292, -0.4776676948433997705 ) ) ;
#11830=CARTESIAN_POINT ( 'NONE',  ( 0.1999999999999789724, -2.166079853131637645, -0.4467913981637917087 ) ) ;
#11840=EDGE_LOOP ( 'NONE', ( #20435, #40056, #34076, #16751 ) ) ;
#11843=CARTESIAN_POINT ( 'NONE',  ( 0.1913042973830217097, -1.953999136512327039, -0.2983785852701217323 ) ) ;
#11856=B_SPLINE_CURVE_WITH_KNOTS ( 'NONE', 3,
 ( #27799, #2904, #9472, #9072, #5968, #15850, #40333, #15457, #37657, #12164 ),
 .UNSPECIFIED., .F., .F.,
 ( 4, 2, 2, 2, 4 ),
 ( 0.000000000000000000, 0.0005579115002213586028, 0.001115823000442717206, 0.001673734500664075808, 0.002231646000885434411 ),
 .UNSPECIFIED. ) ;
#11857=CARTESIAN_POINT ( 'NONE',  ( 0.6253075507800407440, -1.612178444674642108, -0.4646957544917997840 ) ) ;
#11860=CARTESIAN_POINT ( 'NONE',  ( 0.4071174156400276245, -1.728162493485833284, -0.4292401697313079079 ) ) ;
#11863=CARTESIAN_POINT ( 'NONE',  ( 0.3649706973906967633, -1.747755802024545835, -0.5186209711426437163 ) ) ;
#11865=CARTESIAN_POINT ( 'NONE',  ( 0.4624855077751916510, -1.656167738812893475, -0.6359952755422354498 ) ) ;
#11866=ORIENTED_EDGE ( 'NONE', *, *, #30467, .F. ) ;
#11867=CARTESIAN_POINT ( 'NONE',  ( 0.4209912206648682154, -1.078067379053157193, -0.5155029497116575543 ) ) ;
#11869=CARTESIAN_POINT ( 'NONE',  ( 0.02999999999997886302, -2.183180860297921466, -0.7437760292030870524 ) ) ;
#11870=DIRECTION ( 'NONE',  ( 0.4999551463232372317, -0.8660512985181135770, 0.000000000000000000 ) ) ;
#11874=CARTESIAN_POINT ( 'NONE',  ( 0.4646886455416142647, -1.611488784964096643, -0.6527336024875409759 ) ) ;
#11879=DIRECTION ( 'NONE',  ( 0.4999551463232373427, -0.8660512985181134660, 0.000000000000000000 ) ) ;
#11887=CYLINDRICAL_SURFACE ( 'NONE', #20154, 0.2200000000000000289 ) ;
#11889=AXIS2_PLACEMENT_3D ( 'NONE', #36884, #2136, #18169 ) ;
#11903=EDGE_CURVE ( 'NONE', #27374, #20774, #10492, .T. ) ;
#11904=FACE_OUTER_BOUND ( 'NONE', #36523, .T. ) ;
#11907=PRODUCT_DEFINITION ( 'UNKNOWN', '', #17475, #23273 ) ;
#11912=DIRECTION ( 'NONE',  ( 0.4999551463232372317, -0.8660512985181134660, 0.000000000000000000 ) ) ;
#11928=AXIS2_PLACEMENT_3D ( 'NONE', #40384, #31135, #9106 ) ;
#11938=EDGE_CURVE ( 'NONE', #7698, #33903, #38306, .T. ) ;
#11949=AXIS2_PLACEMENT_3D ( 'NONE', #38756, #26659, #19855 ) ;
#11950=CARTESIAN_POINT ( 'NONE',  ( 0.02999999999997876934, -2.097675824466503691, -0.7286991843995640483 ) ) ;
#11959=EDGE_CURVE ( 'NONE', #39658, #22474, #20589, .T. ) ;
#11960=CARTESIAN_POINT ( 'NONE',  ( 0.3595715536228113463, -1.625401886829162201, -0.3696110269036072538 ) ) ;
#11987=CARTESIAN_POINT ( 'NONE',  ( 0.3699999999999786793, -2.183180860297921466, -0.4937760292030871079 ) ) ;
#12007=AXIS2_PLACEMENT_3D ( 'NONE', #8519, #21084, #33610 ) ;
#12014=EDGE_CURVE ( 'NONE', #19186, #5500, #6113, .T. ) ;
#12022=TOROIDAL_SURFACE ( 'NONE', #17274, 0.2200000000000000566, 0.02999999999999999889 ) ;
#12023=CARTESIAN_POINT ( 'NONE',  ( 0.1894590026941424810, -1.967797451371194439, -0.6662202007303367202 ) ) ;
#12026=CARTESIAN_POINT ( 'NONE',  ( 0.2189426737742418139, -1.305592238685004736, -0.4125659523519144001 ) ) ;
#12040=CARTESIAN_POINT ( 'NONE',  ( 0.2327253210492125635, -1.594686327790063363, -0.3238482666460236192 ) ) ;
#12055=CARTESIAN_POINT ( 'NONE',  ( 0.1960722456818422554, -1.288731303253011440, -0.2917126172454974076 ) ) ;
#12058=CARTESIAN_POINT ( 'NONE',  ( 0.4999668580349169722, -1.586321472701693214, -0.5587740707772209658 ) ) ;
#12059=CARTESIAN_POINT ( 'NONE',  ( 0.3965441076082558691, -2.011587606276659557, -0.2840872118775558675 ) ) ;
#12074=CARTESIAN_POINT ( 'NONE',  ( 0.6222686170074345213, -1.528537841564955757, -0.3994016981617310447 ) ) ;
#12075=CARTESIAN_POINT ( 'NONE',  ( 0.1685455824392826929, -1.307862364081260775, -0.7280104148493009575 ) ) ;
#12078=AXIS2_PLACEMENT_3D ( 'NONE', #25636, #22357, #6487 ) ;
#12079=CARTESIAN_POINT ( 'NONE',  ( 0.3699999999999786793, -2.143549940236731732, -0.4549916158381474007 ) ) ;
#12080=CIRCLE ( 'NONE', #4196, 0.2500000000000000555 ) ;
#12082=CARTESIAN_POINT ( 'NONE',  ( 0.3634393234136681916, -1.759352117114970859, -0.5002830012641544810 ) ) ;
#12083=CARTESIAN_POINT ( 'NONE',  ( 0.3828601130222601956, -1.724001686837443481, -0.5877931644812478540 ) ) ;
#12085=CARTESIAN_POINT ( 'NONE',  ( 0.5264113014007612001, -1.640729993778266893, -0.5166151207188711680 ) ) ;
#12093=CARTESIAN_POINT ( 'NONE',  ( 0.5189221204507463714, -1.603650243462305003, -0.6104946154672951097 ) ) ;
#12097=CARTESIAN_POINT ( 'NONE',  ( 0.1909286924077255032, -1.257064795538239022, -0.3194753470178354759 ) ) ;
#12098=ORIENTED_EDGE ( 'NONE', *, *, #13191, .T. ) ;
#12102=AXIS2_PLACEMENT_3D ( 'NONE', #19340, #31879, #32467 ) ;
#12104=CARTESIAN_POINT ( 'NONE',  ( -2.112273405726188513E-14, -2.183180860297921466, -0.4937760292030871079 ) ) ;
#12106=DIRECTION ( 'NONE',  ( 0.8660512985181134660, 0.4999551463232372317, 0.000000000000000000 ) ) ;
#12117=FACE_OUTER_BOUND ( 'NONE', #31237, .T. ) ;
#12120=CARTESIAN_POINT ( 'NONE',  ( 0.2398702836577433772, -1.946110816799010879, -0.6651903542983218509 ) ) ;
#12127=AXIS2_PLACEMENT_3D ( 'NONE', #39681, #4708, #29424 ) ;
#12132=CARTESIAN_POINT ( 'NONE',  ( 0.1977815345931705215, -1.253108778471563767, -0.3161890406021737876 ) ) ;
#12138=ORIENTED_EDGE ( 'NONE', *, *, #15426, .F. ) ;
#12140=DIRECTION ( 'NONE',  ( 0.000000000000000000, 0.000000000000000000, -1.000000000000000000 ) ) ;
#12148=CARTESIAN_POINT ( 'NONE',  ( 0.4887921365776452531, -1.679766821171225999, -0.4193976862638447711 ) ) ;
#12154=ORIENTED_EDGE ( 'NONE', *, *, #29775, .T. ) ;
#12164=CARTESIAN_POINT ( 'NONE',  ( 0.4915260346479126685, -1.695508583366576616, -0.4333519947141560857 ) ) ;
#12166=CIRCLE ( 'NONE', #7542, 0.08830708661417338567 ) ;
#12167=CARTESIAN_POINT ( 'NONE',  ( 0.4554213719789483861, -1.084118224209758452, -0.4129387436622604657 ) ) ;
#12170=CARTESIAN_POINT ( 'NONE',  ( 0.1784968570797965948, -1.218054820023663831, -0.5155029497116575543 ) ) ;
#12176=EDGE_CURVE ( 'NONE', #10240, #37075, #22314, .T. ) ;
#12181=EDGE_CURVE ( 'NONE', #14515, #31373, #34408, .T. ) ;
#12194=VECTOR ( 'NONE', #14802, 39.37007874015748143 ) ;
#12197=ORIENTED_EDGE ( 'NONE', *, *, #22498, .F. ) ;
#12199=CARTESIAN_POINT ( 'NONE',  ( 0.3395539693250317348, -1.657457255472329027, -0.5807180344419580198 ) ) ;
#12200=EDGE_CURVE ( 'NONE', #30753, #23563, #33727, .T. ) ;
#12204=EDGE_LOOP ( 'NONE', ( #1927, #30422, #1808, #27668 ) ) ;
#12211=ORIENTED_EDGE ( 'NONE', *, *, #14177, .T. ) ;
#12212=PLANE ( 'NONE',  #14093 ) ;
#12215=AXIS2_PLACEMENT_3D ( 'NONE', #29325, #4413, #7890 ) ;
#12217=CARTESIAN_POINT ( 'NONE',  ( 0.3699999999999786793, -2.080230235891529667, -0.5026132101038165434 ) ) ;
#12220=PLANE ( 'NONE',  #1090 ) ;
#12221=CARTESIAN_POINT ( 'NONE',  ( 0.04074269369199766400, -1.520498175474628511, -0.6410478022143386578 ) ) ;
#12227=CARTESIAN_POINT ( 'NONE',  ( 0.4722565137939111479, -1.077278095797315149, -0.4218496756560511374 ) ) ;
#12229=CARTESIAN_POINT ( 'NONE',  ( 0.3810179107970706469, -1.714231790258144317, -0.4910716250263590377 ) ) ;
#12234=CARTESIAN_POINT ( 'NONE',  ( 0.4310167615618634707, -1.587237252056899584, -0.3866364743305638618 ) ) ;
#12235=DIRECTION ( 'NONE',  ( 0.000000000000000000, -3.725247264087630335E-15, -1.000000000000000000 ) ) ;
#12241=ORIENTED_EDGE ( 'NONE', *, *, #39340, .F. ) ;
#12242=ORIENTED_EDGE ( 'NONE', *, *, #15432, .F. ) ;
#12248=CARTESIAN_POINT ( 'NONE',  ( 0.3573642944564824342, -1.883588035281504647, -0.5128792341014730694 ) ) ;
#12249=CARTESIAN_POINT ( 'NONE',  ( 0.3885612764051886714, -1.758570040784675159, -0.5425266244860569298 ) ) ;
#12265=CARTESIAN_POINT ( 'NONE',  ( 0.3999999999999789280, -2.087081592863325952, -0.4706838381558562379 ) ) ;
#12273=DIRECTION ( 'NONE',  ( -1.000000000000000000, 0.000000000000000000, 0.000000000000000000 ) ) ;
#12280=CARTESIAN_POINT ( 'NONE',  ( 0.6560555959785092650, -1.525593284718363973, -0.4139158794185884838 ) ) ;
#12281=CARTESIAN_POINT ( 'NONE',  ( 0.03724056042341840345, -1.737240332959331779, -0.6683582582716187659 ) ) ;
#12285=CARTESIAN_POINT ( 'NONE',  ( 0.1909286924077255587, -1.257064795538239022, -0.3404777180881179421 ) ) ;
#12289=CARTESIAN_POINT ( 'NONE',  ( 0.3825425089729009298, -1.696932111950381294, -0.6182103527988705993 ) ) ;
#12292=ORIENTED_EDGE ( 'NONE', *, *, #36822, .F. ) ;
#12293=CARTESIAN_POINT ( 'NONE',  ( 0.5471103864378531467, -1.663420781200640519, -0.5477774273223376955 ) ) ;
#12300=CARTESIAN_POINT ( 'NONE',  ( 0.4382015218937659884, -1.612541052972227940, -0.6615483979663951963 ) ) ;
#12314=VERTEX_POINT ( 'NONE', #8932 ) ;
#12316=ORIENTED_EDGE ( 'NONE', *, *, #1417, .T. ) ;
#12320=CARTESIAN_POINT ( 'NONE',  ( 0.2670249539660715654, -1.533299212170818215, -0.3445188814933614063 ) ) ;
#12322=CARTESIAN_POINT ( 'NONE',  ( 0.5997830302434702388, -1.482755616589708447, -0.4037571860997516415 ) ) ;
#12336=CARTESIAN_POINT ( 'NONE',  ( 0.1727937833756465480, -1.757125623733488018, -0.6809623346501596508 ) ) ;
#12337=CARTESIAN_POINT ( 'NONE',  ( 0.1810766014996238460, -1.262752222553217729, -0.2917159793182513838 ) ) ;
#12338=VERTEX_POINT ( 'NONE', #24371 ) ;
#12346=ORIENTED_EDGE ( 'NONE', *, *, #27835, .F. ) ;
#12359=CARTESIAN_POINT ( 'NONE',  ( 0.4645951959325665404, -1.068949338851189257, -0.4209103011858858490 ) ) ;
#12360=CARTESIAN_POINT ( 'NONE',  ( 0.3886765788477002381, -1.754881642227921645, -0.4506904437265726870 ) ) ;
#12363=FACE_OUTER_BOUND ( 'NONE', #31548, .T. ) ;
#12378=DIRECTION ( 'NONE',  ( 0.4999551463232372317, -0.8660512985181135770, 0.000000000000000000 ) ) ;
#12386=EDGE_LOOP ( 'NONE', ( #16820, #22233, #20510, #15120 ) ) ;
#12390=CARTESIAN_POINT ( 'NONE',  ( 0.1736278472308480370, -1.267052248471710829, -0.7067244366091492980 ) ) ;
#12391=CARTESIAN_POINT ( 'NONE',  ( 0.3646755385473242073, -1.685449887736102603, -0.5938584186312408919 ) ) ;
#12424=DIRECTION ( 'NONE',  ( 0.000000000000000000, 0.000000000000000000, -1.000000000000000000 ) ) ;
#12433=CARTESIAN_POINT ( 'NONE',  ( 0.2215211694921853935, -1.611350768318245974, -0.3261362320128111669 ) ) ;
#12434=CARTESIAN_POINT ( 'NONE',  ( 0.3625960434667531151, -1.762758894398492204, -0.5926935080085831142 ) ) ;
#12450=CARTESIAN_POINT ( 'NONE',  ( 0.3999999999999783729, -2.120664306612643824, -0.5256090310107810470 ) ) ;
#12462=EDGE_CURVE ( 'NONE', #37622, #10331, #10100, .T. ) ;
#12465=CARTESIAN_POINT ( 'NONE',  ( 0.3939451924134707017, -1.988462716268693864, -0.4923357761437431313 ) ) ;
#12466=DIRECTION ( 'NONE',  ( 0.000000000000000000, 0.3420201433257253898, 0.9396926207858877778 ) ) ;
#12472=CARTESIAN_POINT ( 'NONE',  ( 0.3623460565293080693, -1.967939423356526829, -0.4915828919187142931 ) ) ;
#12473=CYLINDRICAL_SURFACE ( 'NONE', #38867, 0.1033070866141734129 ) ;
#12485=EDGE_LOOP ( 'NONE', ( #34503, #28051, #16894, #6639 ) ) ;
#12496=ORIENTED_EDGE ( 'NONE', *, *, #25745, .F. ) ;
#12506=CARTESIAN_POINT ( 'NONE',  ( 0.1487712572053581650, -1.705599614157317534, -0.3615038741254806287 ) ) ;
#12509=CARTESIAN_POINT ( 'NONE',  ( 0.02317555983421318300, -1.616538932131220241, -0.3753236664589540972 ) ) ;
#12511=CARTESIAN_POINT ( 'NONE',  ( 0.3999999999999786504, -1.971318270955308982, -0.3048432623593835822 ) ) ;
#12516=CARTESIAN_POINT ( 'NONE',  ( 0.3520925652409914175, -1.512544934550680287, -0.7187326247832951376 ) ) ;
#12521=EDGE_CURVE ( 'NONE', #30458, #394, #39749, .T. ) ;
#12525=CARTESIAN_POINT ( 'NONE',  ( 0.5616682974235900350, -1.585511599874633193, -0.5166151207188732775 ) ) ;
#12534=ORIENTED_EDGE ( 'NONE', *, *, #8679, .T. ) ;
#12545=DIRECTION ( 'NONE',  ( 0.8660512985181134660, 0.4999551463232371762, 0.000000000000000000 ) ) ;
#12546=CARTESIAN_POINT ( 'NONE',  ( 0.3945306638533003230, -1.754969121428254342, -0.4915120835733784999 ) ) ;
#12548=CARTESIAN_POINT ( 'NONE',  ( 0.4103187208584767043, -1.720663819739514100, -0.4253394185160298546 ) ) ;
#12561=VECTOR ( 'NONE', #32413, 39.37007874015748854 ) ;
#12563=DIRECTION ( 'NONE',  ( -0.4999551463232377313, 0.8660512985181132439, -0.000000000000000000 ) ) ;
#12566=CIRCLE ( 'NONE', #35551, 0.08830708661417320526 ) ;
#12580=CIRCLE ( 'NONE', #4025, 0.1700000000000000400 ) ;
#12590=CARTESIAN_POINT ( 'NONE',  ( 0.3601834888757650122, -1.721134795303484788, -0.5614851183221652997 ) ) ;
#12591=CARTESIAN_POINT ( 'NONE',  ( 0.6104845410980109799, -1.615235805367044808, -0.5028569573147162464 ) ) ;
#12597=B_SPLINE_CURVE_WITH_KNOTS ( 'NONE', 3,
 ( #31806, #13080, #25445, #38168, #9375, #34881 ),
 .UNSPECIFIED., .F., .F.,
 ( 4, 2, 4 ),
 ( 0.000000000000000000, 0.0007264914290232497678, 0.001452982858046499536 ),
 .UNSPECIFIED. ) ;
#12600=CARTESIAN_POINT ( 'NONE',  ( 0.3926032618789407347, -1.756026311479913948, -0.5284552501753293496 ) ) ;
#12630=CARTESIAN_POINT ( 'NONE',  ( 0.3699999999999789568, -2.050772785069567838, -0.3050017341552425654 ) ) ;
#12642=CARTESIAN_POINT ( 'NONE',  ( 0.4346145078518607874, -1.592046523758374077, -0.4178586084682519575 ) ) ;
#12647=AXIS2_PLACEMENT_3D ( 'NONE', #19937, #35772, #4298 ) ;
#12660=AXIS2_PLACEMENT_3D ( 'NONE', #16020, #32049, #23213 ) ;
#12661=CARTESIAN_POINT ( 'NONE',  ( 0.6299088991424890427, -1.603889269770004233, -0.4524234554939136621 ) ) ;
#12667=EDGE_CURVE ( 'NONE', #23137, #26169, #22765, .T. ) ;
#12672=CARTESIAN_POINT ( 'NONE',  ( 0.3988135775770819680, -1.610682515506242751, -0.3616878989671591382 ) ) ;
#12673=CIRCLE ( 'NONE', #159, 0.03000000000000003358 ) ;
#12676=CARTESIAN_POINT ( 'NONE',  ( 0.5375949106523618681, -1.667153108916268334, -0.4581832398558707831 ) ) ;
#12681=VERTEX_POINT ( 'NONE', #35358 ) ;
#12682=CARTESIAN_POINT ( 'NONE',  ( 0.3590659390023258624, -1.625695363421262973, -0.6613478498294523833 ) ) ;
#12696=ADVANCED_FACE ( 'NONE', ( #7148 ), #19967, .T. ) ;
#12721=CARTESIAN_POINT ( 'NONE',  ( 0.2414668910093294429, -2.107936428766274073, -0.7005084057759867200 ) ) ;
#12738=ORIENTED_EDGE ( 'NONE', *, *, #1723, .T. ) ;
#12755=CARTESIAN_POINT ( 'NONE',  ( 0.5213450412171337645, -1.664948425110202246, -0.4412658265323602946 ) ) ;
#12760=DIRECTION ( 'NONE',  ( 0.8660512985181133550, 0.4999551463232371207, 0.000000000000000000 ) ) ;
#12761=ORIENTED_EDGE ( 'NONE', *, *, #30064, .F. ) ;
#12762=ORIENTED_EDGE ( 'NONE', *, *, #2607, .F. ) ;
#12764=FACE_OUTER_BOUND ( 'NONE', #35364, .T. ) ;
#12784=CARTESIAN_POINT ( 'NONE',  ( 0.2829942045735191480, -1.550042413449979062, -0.6886752251949420645 ) ) ;
#12805=ORIENTED_EDGE ( 'NONE', *, *, #37119, .T. ) ;
#12806=TOROIDAL_SURFACE ( 'NONE', #9511, 0.1333070866141734256, 0.02999999999999999889 ) ;
#12808=CARTESIAN_POINT ( 'NONE',  ( 0.6358220093450094312, -1.612209227696623115, -0.5779622822862300335 ) ) ;
#12813=B_SPLINE_CURVE_WITH_KNOTS ( 'NONE', 3,
 ( #22125, #2370, #8935, #40408 ),
 .UNSPECIFIED., .F., .F.,
 ( 4, 4 ),
 ( 0.000000000000000000, 0.001713671539103278673 ),
 .UNSPECIFIED. ) ;
#12831=CARTESIAN_POINT ( 'NONE',  ( 0.4686710939017081357, -1.131369304810952325, -0.3726880373738259977 ) ) ;
#12837=EDGE_CURVE ( 'NONE', #31681, #23240, #4813, .T. ) ;
#12842=CARTESIAN_POINT ( 'NONE',  ( 0.4200748011392089198, -1.654004974025707897, -0.7462941026102624109 ) ) ;
#12852=CARTESIAN_POINT ( 'NONE',  ( 0.4218037824360915677, -1.666477969087174493, -0.5029009060039884016 ) ) ;
#12863=EDGE_LOOP ( 'NONE', ( #30292, #17610, #37070, #28176 ) ) ;
#12865=PLANE ( 'NONE',  #26615 ) ;
#12873=EDGE_CURVE ( 'NONE', #20339, #27374, #19327, .T. ) ;
#12874=FACE_OUTER_BOUND ( 'NONE', #29843, .T. ) ;
#12885=B_SPLINE_CURVE_WITH_KNOTS ( 'NONE', 3,
 ( #26207, #23342, #38730, #14441, #39156, #8069, #20644, #35656 ),
 .UNSPECIFIED., .F., .F.,
 ( 4, 2, 2, 4 ),
 ( 3.469446951953614189E-18, 0.0002979885802634740506, 0.0005959771605269446318, 0.001191954321053884710 ),
 .UNSPECIFIED. ) ;
#12890=CARTESIAN_POINT ( 'NONE',  ( 0.1809966328114128720, -1.222385076516254054, -0.5155029497116575543 ) ) ;
#12895=CARTESIAN_POINT ( 'NONE',  ( 0.3638636590137022120, -1.622755819691197754, -0.3680121727053636826 ) ) ;
#12896=CARTESIAN_POINT ( 'NONE',  ( 0.3675394818443805112, -2.037853795900605114, -0.4718837028662131172 ) ) ;
#12901=DIRECTION ( 'NONE',  ( 4.503376743791639448E-15, 0.9613939893712163398, -0.2751755752258865373 ) ) ;
#12921=ADVANCED_FACE ( 'NONE', ( #31416 ), #21142, .T. ) ;
#12925=CARTESIAN_POINT ( 'NONE',  ( 0.5546656019160204343, -1.624250834075737560, -0.4654251787435473298 ) ) ;
#12926=CARTESIAN_POINT ( 'NONE',  ( 0.1981231351721541856, -1.245830158587560410, -0.3144976166544465324 ) ) ;
#12930=CARTESIAN_POINT ( 'NONE',  ( 0.3702591405535748947, -1.654865263428320077, -0.7284099060135055259 ) ) ;
#12931=ORIENTED_EDGE ( 'NONE', *, *, #22847, .T. ) ;
#12932=ADVANCED_FACE ( 'NONE', ( #21359 ), #21410, .F. ) ;
#12938=CARTESIAN_POINT ( 'NONE',  ( 0.3997069619151109032, -2.078179102625506314, -0.5163588566289569748 ) ) ;
#12941=CARTESIAN_POINT ( 'NONE',  ( 0.1909286924077254199, -1.257064795538238577, -0.7137147910238503812 ) ) ;
#12950=CARTESIAN_POINT ( 'NONE',  ( 0.6040377325928559804, -1.527126331885624522, -0.4341809412190014705 ) ) ;
#12951=CARTESIAN_POINT ( 'NONE',  ( 0.2079683456743255388, -1.627305492656140551, -0.6921328867639651161 ) ) ;
#12952=AXIS2_PLACEMENT_3D ( 'NONE', #3411, #15967, #28119 ) ;
#12956=EDGE_LOOP ( 'NONE', ( #29507, #30118, #9347, #35411 ) ) ;
#12959=CARTESIAN_POINT ( 'NONE',  ( 0.3593346688482154661, -1.735925422213635549, -0.5010936962835144115 ) ) ;
#12963=ORIENTED_EDGE ( 'NONE', *, *, #5739, .T. ) ;
#12968=CARTESIAN_POINT ( 'NONE',  ( 0.5389700850957479528, -1.668120024254199141, -0.4887752422164399757 ) ) ;
#12971=CARTESIAN_POINT ( 'NONE',  ( 0.3946727801157763893, -1.754662960969486818, -0.5213263030586290370 ) ) ;
#12975=DIRECTION ( 'NONE',  ( 0.4999551463232373427, -0.8660512985181134660, 0.000000000000000000 ) ) ;
#12988=( BOUNDED_SURFACE ( )  B_SPLINE_SURFACE ( 3, 2, ( 
 ( #13151, #39070, #7170 ),
 ( #19944, #38247, #13365 ),
 ( #16264, #38657, #26142 ),
 ( #6985, #20164, #16657 ),
 ( #25715, #28991, #38462 ),
 ( #32271, #10895, #22651 ),
 ( #29411, #10476, #1447 ),
 ( #23468, #13759, #6773 ),
 ( #19352, #7369, #35568 ),
 ( #29206, #35183, #19557 ),
 ( #32479, #32087, #13960 ),
 ( #31890, #10678, #10077 ),
 ( #7588, #22861, #3894 ),
 ( #16450, #4304, #1257 ),
 ( #35380, #856, #26325 ),
 ( #10297, #16870, #38849 ),
 ( #23253, #3709, #35778 ),
 ( #32691, #4089, #28801 ),
 ( #1067, #4496, #17059 ),
 ( #29604, #18224, #4689 ),
 ( #20358, #3005, #33294 ),
 ( #26741, #18631, #2794 ),
 ( #39462, #34056, #8198 ),
 ( #12055, #15342, #7789 ) ),
 .UNSPECIFIED., .F., .F., .T. ) 
 B_SPLINE_SURFACE_WITH_KNOTS ( ( 4, 2, 2, 2, 2, 2, 2, 2, 2, 2, 2, 4 ),
 ( 3, 3 ),
 ( 0.005360940551000458604, 0.008137707959848014538, 0.01091447536869557221, 0.01369124277754312988, 0.01646801018639068581, 0.01924477759523824175, 0.02202154500408579768, 0.02340992870850957391, 0.02479831241293335362, 0.02549250426514524520, 0.02618669611735713332, 0.02757507982178090955 ),
 ( 0.000000000000000000, 1.000000000000000000 ),
 .UNSPECIFIED. ) 
 GEOMETRIC_REPRESENTATION_ITEM ( )  RATIONAL_B_SPLINE_SURFACE ( (
 ( 1.000000000000000000, 0.7071328584466060052, 1.000000000000000000),
 ( 1.000000000000000000, 0.7072620464649821415, 1.000000000000000000),
 ( 1.000000000000000000, 0.7085185872330661550, 1.000000000000000000),
 ( 1.000000000000000000, 0.7116993494293128997, 1.000000000000000000),
 ( 1.000000000000000000, 0.7136510046383820471, 1.000000000000000000),
 ( 1.000000000000000000, 0.7179400475017202465, 1.000000000000000000),
 ( 1.000000000000000000, 0.7202921658712200248, 1.000000000000000000),
 ( 1.000000000000000000, 0.7253987115934981134, 1.000000000000000000),
 ( 1.000000000000000000, 0.7281595695102663912, 1.000000000000000000),
 ( 1.000000000000000000, 0.7341325496256051464, 1.000000000000000000),
 ( 1.000000000000000000, 0.7373714411113219125, 1.000000000000000000),
 ( 1.000000000000000000, 0.7439769103193287769, 1.000000000000000000),
 ( 1.000000000000000000, 0.7474422512830740661, 1.000000000000000000),
 ( 1.000000000000000000, 0.7514310957412383418, 1.000000000000000000),
 ( 1.000000000000000000, 0.7525427382793115072, 1.000000000000000000),
 ( 1.000000000000000000, 0.7534397546842908078, 1.000000000000000000),
 ( 1.000000000000000000, 0.7532682500171895557, 1.000000000000000000),
 ( 1.000000000000000000, 0.7505746427157311551, 1.000000000000000000),
 ( 1.000000000000000000, 0.7492519672572479639, 1.000000000000000000),
 ( 1.000000000000000000, 0.7453945544990168148, 1.000000000000000000),
 ( 1.000000000000000000, 0.7428563216680332815, 1.000000000000000000),
 ( 1.000000000000000000, 0.7326522287684954504, 1.000000000000000000),
 ( 1.000000000000000000, 0.7220899002612864992, 1.000000000000000000),
 ( 1.000000000000000000, 0.7071496063340624305, 1.000000000000000000) ) ) 
 REPRESENTATION_ITEM ( '' )  SURFACE ( )  );
#12990=CARTESIAN_POINT ( 'NONE',  ( 0.3968784764610951976, -1.684996356591544231, -0.4053910425699968068 ) ) ;
#12997=CARTESIAN_POINT ( 'NONE',  ( 0.3718881020994557751, -1.717634997487592630, -0.6861734131539279913 ) ) ;
#12999=B_SPLINE_CURVE_WITH_KNOTS ( 'NONE', 3,
 ( #5697, #11264, #40248, #29996 ),
 .UNSPECIFIED., .F., .F.,
 ( 4, 4 ),
 ( 0.000000000000000000, 0.002406601043976852941 ),
 .UNSPECIFIED. ) ;
#13000=ORIENTED_EDGE ( 'NONE', *, *, #29019, .T. ) ;
#13006=CARTESIAN_POINT ( 'NONE',  ( 0.5089656749515859557, -1.649654440091849139, -0.4396827738775478944 ) ) ;
#13011=VERTEX_POINT ( 'NONE', #3218 ) ;
#13012=CARTESIAN_POINT ( 'NONE',  ( 0.6147040457557710891, -1.612300127778828251, -0.5493327930725481201 ) ) ;
#13024=ORIENTED_EDGE ( 'NONE', *, *, #29537, .T. ) ;
#13026=CARTESIAN_POINT ( 'NONE',  ( 0.2209260011871197471, -1.309027873449325918, -0.6184399470714002645 ) ) ;
#13028=ORIENTED_EDGE ( 'NONE', *, *, #9641, .T. ) ;
#13029=CARTESIAN_POINT ( 'NONE',  ( 0.4455220531189463262, -1.593574230686272131, -0.6096253356284021541 ) ) ;
#13061=VERTEX_POINT ( 'NONE', #39206 ) ;
#13065=CARTESIAN_POINT ( 'NONE',  ( 0.5164231089728142932, -1.603420859054122349, -0.4174082106076965060 ) ) ;
#13066=CARTESIAN_POINT ( 'NONE',  ( 0.5747203984579013492, -1.612743926285909346, -0.5166151207188712791 ) ) ;
#13069=CARTESIAN_POINT ( 'NONE',  ( 0.4000000000017098767, -2.081908495022728900, -0.7229603458646237657 ) ) ;
#13080=CARTESIAN_POINT ( 'NONE',  ( 0.4795034887773614307, -1.112758664428941557, -0.4039987388423294523 ) ) ;
#13081=B_SPLINE_CURVE_WITH_KNOTS ( 'NONE', 3,
 ( #20907, #35921, #39212, #8338, #23998, #17191, #11033, #17604 ),
 .UNSPECIFIED., .F., .F.,
 ( 4, 2, 2, 4 ),
 ( 1.734723475976807094E-18, 0.0003750355950782678746, 0.0005625533926174032485, 0.0007500711901565386766 ),
 .UNSPECIFIED. ) ;
#13083=CARTESIAN_POINT ( 'NONE',  ( 0.4264202721361137760, -1.467519734074644200, -0.5166151207188711680 ) ) ;
#13085=ORIENTED_EDGE ( 'NONE', *, *, #31848, .F. ) ;
#13087=CARTESIAN_POINT ( 'NONE',  ( 0.3706793757908085074, -1.615012852715396408, -0.4172838525897037409 ) ) ;
#13088=CARTESIAN_POINT ( 'NONE',  ( 0.1909286924077254199, -1.257064795538238577, -0.7137147910238503812 ) ) ;
#13094=CARTESIAN_POINT ( 'NONE',  ( 0.4003286060160837767, -1.748155145820723622, -0.5147095092263663796 ) ) ;
#13113=CARTESIAN_POINT ( 'NONE',  ( -2.112273405726188513E-14, -2.183180860297921466, -0.4937760292030871079 ) ) ;
#13118=DIRECTION ( 'NONE',  ( -0.8339988114203499281, 0.000000000000000000, -0.5517662390446189669 ) ) ;
#13120=CARTESIAN_POINT ( 'NONE',  ( 0.1989976604547391836, -2.047409678865565574, -0.7132172901365276818 ) ) ;
#13122=CARTESIAN_POINT ( 'NONE',  ( 0.1977770146402836882, -1.253111387755460271, -0.7170389573829240026 ) ) ;
#13137=CARTESIAN_POINT ( 'NONE',  ( 0.3584357512826374936, -1.733078788867854936, -0.4965168443801308285 ) ) ;
#13140=ORIENTED_EDGE ( 'NONE', *, *, #23407, .F. ) ;
#13142=ORIENTED_EDGE ( 'NONE', *, *, #4625, .F. ) ;
#13143=LINE ( 'NONE', #16439, #3470 ) ;
#13144=VERTEX_POINT ( 'NONE', #23177 ) ;
#13151=CARTESIAN_POINT ( 'NONE',  ( 0.02999778723028687782, -2.087755359801442445, -0.2623954751430960242 ) ) ;
#13153=ORIENTED_EDGE ( 'NONE', *, *, #25631, .T. ) ;
#13174=CARTESIAN_POINT ( 'NONE',  ( 0.2280783781436956370, -1.602091971434898232, -0.6679261136964330658 ) ) ;
#13179=B_SPLINE_CURVE_WITH_KNOTS ( 'NONE', 3,
 ( #30955, #13196, #12249, #40205 ),
 .UNSPECIFIED., .F., .F.,
 ( 4, 4 ),
 ( 0.000000000000000000, 0.001130163152920550789 ),
 .UNSPECIFIED. ) ;
#13191=EDGE_CURVE ( 'NONE', #19020, #17902, #36519, .T. ) ;
#13193=ORIENTED_EDGE ( 'NONE', *, *, #16097, .F. ) ;
#13194=CARTESIAN_POINT ( 'NONE',  ( 0.4957543717786337956, -1.693067643768066288, -0.5958955378105396106 ) ) ;
#13196=CARTESIAN_POINT ( 'NONE',  ( 0.3827312705878086474, -1.762287005346949709, -0.5557439487639747044 ) ) ;
#13200=VERTEX_POINT ( 'NONE', #26864 ) ;
#13208=CARTESIAN_POINT ( 'NONE',  ( 0.6470677939190155881, -1.605717247508275713, -0.4588775121292724690 ) ) ;
#13209=EDGE_CURVE ( 'NONE', #7985, #37937, #23779, .T. ) ;
#13217=CARTESIAN_POINT ( 'NONE',  ( 0.4382015218937535539, -1.612541052972219502, -0.6615483979664104064 ) ) ;
#13230=ADVANCED_FACE ( 'NONE', ( #17599 ), #1972, .F. ) ;
#13232=ORIENTED_EDGE ( 'NONE', *, *, #32577, .T. ) ;
#13244=ORIENTED_EDGE ( 'NONE', *, *, #31776, .F. ) ;
#13245=ORIENTED_EDGE ( 'NONE', *, *, #6363, .F. ) ;
#13252=ORIENTED_EDGE ( 'NONE', *, *, #20219, .F. ) ;
#13257=CARTESIAN_POINT ( 'NONE',  ( 0.4268980379306124284, -1.643599345667950518, -0.4092648393969006704 ) ) ;
#13262=EDGE_CURVE ( 'NONE', #32636, #8912, #30747, .T. ) ;
#13264=CIRCLE ( 'NONE', #19173, 0.03000000000000006134 ) ;
#13267=EDGE_CURVE ( 'NONE', #25189, #38684, #971, .T. ) ;
#13268=CARTESIAN_POINT ( 'NONE',  ( 0.4032708983214592924, -1.733579849462775657, -0.3059104399065430968 ) ) ;
#13282=DIRECTION ( 'NONE',  ( 0.8660512985181134660, 0.4999551463232371762, 0.000000000000000000 ) ) ;
#13284=ORIENTED_EDGE ( 'NONE', *, *, #11959, .F. ) ;
#13285=FACE_OUTER_BOUND ( 'NONE', #24377, .T. ) ;
#13287=CIRCLE ( 'NONE', #25105, 0.01499999999999999424 ) ;
#13310=CARTESIAN_POINT ( 'NONE',  ( 0.3397077535880359545, -1.654685348432989089, -0.3858274525146626055 ) ) ;
#13312=ADVANCED_FACE ( 'NONE', ( #6038 ), #14057, .F. ) ;
#13316=CARTESIAN_POINT ( 'NONE',  ( 0.3923243630925510872, -1.966611948492501316, -0.4968729097670202544 ) ) ;
#13322=CARTESIAN_POINT ( 'NONE',  ( -0.002218965743620939825, -1.368565310413371705, -0.3828039145932563558 ) ) ;
#13324=DIRECTION ( 'NONE',  ( 0.4999551463232373427, -0.8660512985181134660, 0.000000000000000000 ) ) ;
#13326=CARTESIAN_POINT ( 'NONE',  ( 0.3860871553693445701, -1.736163695054018241, -0.7193333307755221950 ) ) ;
#13332=CARTESIAN_POINT ( 'NONE',  ( 0.6492251849256891472, -1.449833129731838977, -0.6190067879899118219 ) ) ;
#13340=CARTESIAN_POINT ( 'NONE',  ( 0.4173053972040562387, -1.590420842066649465, -0.4142378684116532761 ) ) ;
#13348=CARTESIAN_POINT ( 'NONE',  ( 0.5838497309001715596, -1.602250078375488274, -0.4543158100596352833 ) ) ;
#13352=ORIENTED_EDGE ( 'NONE', *, *, #21530, .F. ) ;
#13354=CARTESIAN_POINT ( 'NONE',  ( 0.3536427585406661245, -1.745782643693225777, -0.5548824076054205134 ) ) ;
#13365=CARTESIAN_POINT ( 'NONE',  ( -2.097120186386331940E-14, -2.063349513125158463, -0.3027437064113706056 ) ) ;
#13366=ORIENTED_EDGE ( 'NONE', *, *, #31776, .T. ) ;
#13367=DIRECTION ( 'NONE',  ( 1.000000000000000000, 0.000000000000000000, 0.000000000000000000 ) ) ;
#13390=B_SPLINE_CURVE_WITH_KNOTS ( 'NONE', 3,
 ( #16395, #37803, #38401, #19294, #28750, #9622, #612, #10237, #35934, #26694, #26275, #20110, #26087, #35722, #38791, #1204, #1390, #7928, #38606, #13707, #10623, #29973 ),
 .UNSPECIFIED., .F., .F.,
 ( 4, 2, 2, 2, 2, 2, 2, 2, 2, 2, 4 ),
 ( 0.000000000000000000, 0.0007781589143522405546, 0.001556317828704481109, 0.003112635657408943570, 0.006225271314817849844, 0.007781589143522303631, 0.008559748057874530525, 0.009337906972226757418, 0.01089422480093120947, 0.01167238371528343463, 0.01245054262963566152 ),
 .UNSPECIFIED. ) ;
#13391=DIRECTION ( 'NONE',  ( 0.4999551463232372317, -0.8660512985181135770, 0.000000000000000000 ) ) ;
#13393=CIRCLE ( 'NONE', #8126, 0.1333070866141732591 ) ;
#13394=ORIENTED_EDGE ( 'NONE', *, *, #15935, .T. ) ;
#13397=CARTESIAN_POINT ( 'NONE',  ( 0.6511295279640838540, -1.603372484741562243, -0.5770581850489380216 ) ) ;
#13402=EDGE_LOOP ( 'NONE', ( #19333, #10019, #9441, #37393, #20649, #1833, #9 ) ) ;
#13405=CARTESIAN_POINT ( 'NONE',  ( 0.3264244126186546802, -1.294301107126978767, -0.5166151207188711680 ) ) ;
#13410=EDGE_LOOP ( 'NONE', ( #554, #37270, #29022, #3060, #28144, #12805 ) ) ;
#13413=CARTESIAN_POINT ( 'NONE',  ( 0.4241308954920427476, -1.602590692387141136, -0.3549062565033732630 ) ) ;
#13423=CARTESIAN_POINT ( 'NONE',  ( 0.3766087435943047956, -1.648707884900325604, -0.6331061992164871421 ) ) ;
#13424=EDGE_CURVE ( 'NONE', #13497, #8912, #171, .T. ) ;
#13426=CARTESIAN_POINT ( 'NONE',  ( 0.5158078970339151637, -1.604330220985429767, -0.6142783388584680537 ) ) ;
#13434=CARTESIAN_POINT ( 'NONE',  ( 0.4620959648888870452, -1.073996026857335417, -0.6125958513722957743 ) ) ;
#13453=EDGE_LOOP ( 'NONE', ( #15322, #13232, #16258, #14449, #26415, #10671, #1280, #2494 ) ) ;
#13460=( BOUNDED_SURFACE ( )  B_SPLINE_SURFACE ( 3, 2, ( 
 ( #10037, #16613, #6530 ),
 ( #6735, #34928, #625 ),
 ( #3856, #16408, #1026 ),
 ( #35524, #4265, #19903 ) ),
 .UNSPECIFIED., .F., .F., .F. ) 
 B_SPLINE_SURFACE_WITH_KNOTS ( ( 4, 4 ),
 ( 3, 3 ),
 ( 6.938893903907228378E-18, 0.001175067160604088314 ),
 ( 0.000000000000000000, 1.000000000000000000 ),
 .UNSPECIFIED. ) 
 GEOMETRIC_REPRESENTATION_ITEM ( )  RATIONAL_B_SPLINE_SURFACE ( (
 ( 1.000000000000000000, 0.9000550641257055728, 1.000000000000000000),
 ( 1.000000000000000000, 0.9100375230753980915, 1.000000000000000000),
 ( 1.000000000000000000, 0.9182507546028528811, 1.000000000000000000),
 ( 1.000000000000000000, 0.9231872052445992960, 1.000000000000000000) ) ) 
 REPRESENTATION_ITEM ( '' )  SURFACE ( )  );
#13465=VERTEX_POINT ( 'NONE', #20429 ) ;
#13470=CARTESIAN_POINT ( 'NONE',  ( 0.4996517707920770102, -1.622836357335520230, -0.4447391335572282167 ) ) ;
#13480=EDGE_CURVE ( 'NONE', #29455, #19345, #12885, .T. ) ;
#13492=CARTESIAN_POINT ( 'NONE',  ( 0.4751758298663426583, -1.652426242819087010, -0.6334442537810192064 ) ) ;
#13496=EDGE_CURVE ( 'NONE', #24117, #652, #31525, .T. ) ;
#13497=VERTEX_POINT ( 'NONE', #1743 ) ;
#13500=EDGE_CURVE ( 'NONE', #17083, #25706, #25256, .T. ) ;
#13502=CARTESIAN_POINT ( 'NONE',  ( 0.02999607453758943582, -2.087869005097288788, -0.7252195465745524539 ) ) ;
#13504=CIRCLE ( 'NONE', #11541, 0.1033070866141734129 ) ;
#13511=CARTESIAN_POINT ( 'NONE',  ( 0.1992677735555647978, -1.286890397454214963, -0.7430133923425328302 ) ) ;
#13516=EDGE_LOOP ( 'NONE', ( #28589, #16148, #39606, #9056 ) ) ;
#13519=DIRECTION ( 'NONE',  ( 0.4999551463232372317, -0.8660512985181133550, 0.000000000000000000 ) ) ;
#13521=VERTEX_POINT ( 'NONE', #38536 ) ;
#13529=ORIENTED_EDGE ( 'NONE', *, *, #2482, .T. ) ;
#13531=CARTESIAN_POINT ( 'NONE',  ( 0.007992636382689974339, -1.702839484628106081, -0.3714452569209771848 ) ) ;
#13537=AXIS2_PLACEMENT_3D ( 'NONE', #969, #18858, #3203 ) ;
#13539=CARTESIAN_POINT ( 'NONE',  ( 0.3929588477770515342, -1.748770905532780473, -0.7163146028298593704 ) ) ;
#13540=DIRECTION ( 'NONE',  ( 0.8660512985181126888, 0.4999551463232385085, 0.000000000000000000 ) ) ;
#13544=CARTESIAN_POINT ( 'NONE',  ( 0.6378390993400826492, -1.514931934295542293, -0.6154632752815170083 ) ) ;
#13550=CARTESIAN_POINT ( 'NONE',  ( 0.6107159011204299492, -1.503447172704659884, -0.4209194897869562579 ) ) ;
#13553=CARTESIAN_POINT ( 'NONE',  ( 0.5578464603247045295, -1.622583067024152115, -0.5578993484895078403 ) ) ;
#13554=DIRECTION ( 'NONE',  ( 0.4999551463232372317, -0.8660512985181134660, 0.000000000000000000 ) ) ;
#13562=CARTESIAN_POINT ( 'NONE',  ( 0.5960491110230784484, -1.583590495288289102, -0.4275273839149444366 ) ) ;
#13567=CARTESIAN_POINT ( 'NONE',  ( 0.3837205613235070145, -1.661390420354927899, -0.6156094881597907742 ) ) ;
#13569=AXIS2_PLACEMENT_3D ( 'NONE', #21015, #17312, #30472 ) ;
#13570=CARTESIAN_POINT ( 'NONE',  ( 0.2499757726471207031, -1.165244724628914375, -0.5155029497116575543 ) ) ;
#13583=CARTESIAN_POINT ( 'NONE',  ( -2.128333683970191216E-14, -2.097675824466503691, -0.2907100122647986451 ) ) ;
#13586=ADVANCED_FACE ( 'NONE', ( #13640 ), #22955, .F. ) ;
#13588=DIRECTION ( 'NONE',  ( 0.4999551463232377313, -0.8660512985181132439, -0.000000000000000000 ) ) ;
#13589=DIRECTION ( 'NONE',  ( 0.8660512985181134660, 0.4999551463232373427, 0.000000000000000000 ) ) ;
#13596=CARTESIAN_POINT ( 'NONE',  ( 0.2059273467974227778, -1.283046334493782359, -0.7137159211901564770 ) ) ;
#13599=CARTESIAN_POINT ( 'NONE',  ( 0.4113341154505090747, -1.741801871956848657, -0.5994564538100538575 ) ) ;
#13606=CARTESIAN_POINT ( 'NONE',  ( 0.4879569794952549056, -1.656586030313209168, -0.4238502451869202159 ) ) ;
#13611=ORIENTED_EDGE ( 'NONE', *, *, #40315, .T. ) ;
#13614=CARTESIAN_POINT ( 'NONE',  ( 0.3999999999999787059, -2.097675824466503691, -0.7286991843995640483 ) ) ;
#13618=CARTESIAN_POINT ( 'NONE',  ( 0.3637049059787201832, -1.760756476090657330, -0.5110479723366356808 ) ) ;
#13621=CARTESIAN_POINT ( 'NONE',  ( 0.4573071940129567747, -1.592216967606236544, -0.4275647618858054999 ) ) ;
#13624=CARTESIAN_POINT ( 'NONE',  ( 0.3511758406044659386, -1.510956930971388834, -0.7187326247832951376 ) ) ;
#13625=CARTESIAN_POINT ( 'NONE',  ( 0.5001189568028716614, -1.586255355638424236, -0.5583759577945262009 ) ) ;
#13631=CARTESIAN_POINT ( 'NONE',  ( 0.4484878740865431146, -1.108380718066777959, -0.3648515278348753443 ) ) ;
#13640=FACE_OUTER_BOUND ( 'NONE', #31374, .T. ) ;
#13641=ORIENTED_EDGE ( 'NONE', *, *, #33119, .T. ) ;
#13650=CARTESIAN_POINT ( 'NONE',  ( 0.3993510570514907099, -1.686034264335497301, -0.5196087884962241610 ) ) ;
#13660=CARTESIAN_POINT ( 'NONE',  ( 0.3511758406044653280, -1.510956930971387724, -0.7187326247832955817 ) ) ;
#13664=CARTESIAN_POINT ( 'NONE',  ( 0.2127800765133925076, -1.279090382353622601, -0.3161890964247149327 ) ) ;
#13671=DIRECTION ( 'NONE',  ( 0.000000000000000000, -2.294752314677981182E-14, -1.000000000000000000 ) ) ;
#13678=CARTESIAN_POINT ( 'NONE',  ( 0.5195269094232773943, -1.645577264492883884, -0.5790482453853514899 ) ) ;
#13685=ORIENTED_EDGE ( 'NONE', *, *, #26303, .F. ) ;
#13691=EDGE_CURVE ( 'NONE', #26169, #17298, #7529, .T. ) ;
#13694=CARTESIAN_POINT ( 'NONE',  ( 0.3991299184228387920, -1.748847125651597390, -0.4900826320043861206 ) ) ;
#13699=CARTESIAN_POINT ( 'NONE',  ( 0.5788429232882181807, -1.529988839563255709, -0.4632948810236542370 ) ) ;
#13700=VERTEX_POINT ( 'NONE', #17276 ) ;
#13707=CARTESIAN_POINT ( 'NONE',  ( 0.2341860847041785376, -1.597289339054992263, -0.3541232024024360547 ) ) ;
#13713=CARTESIAN_POINT ( 'NONE',  ( 0.3852571783543742301, -1.799609661962979112, -0.5248174630631543547 ) ) ;
#13716=CARTESIAN_POINT ( 'NONE',  ( 0.4032069153717364740, -1.732084460174936780, -0.4324387111440983200 ) ) ;
#13725=CARTESIAN_POINT ( 'NONE',  ( 0.4159916692016358830, -1.069406866067976081, -0.5155029497116575543 ) ) ;
#13731=CARTESIAN_POINT ( 'NONE',  ( 0.5758566523281927196, -1.538448204759498283, -0.4771555642015232190 ) ) ;
#13740=CARTESIAN_POINT ( 'NONE',  ( 0.3686476870012108109, -1.763285233157189769, -0.5845549610680257357 ) ) ;
#13752=DIRECTION ( 'NONE',  ( -0.1858595909941318236, -0.1072932506077262926, 0.9767007580674449407 ) ) ;
#13755=CARTESIAN_POINT ( 'NONE',  ( 0.5388754901600865121, -1.668174632133634816, -0.4628410262239764372 ) ) ;
#13759=CARTESIAN_POINT ( 'NONE',  ( 0.009883767140662630749, -1.737539166105977362, -0.3362136773710249216 ) ) ;
#13763=CARTESIAN_POINT ( 'NONE',  ( 0.1241546671216074288, -1.317368862021473186, -0.6849612450614390724 ) ) ;
#13774=CARTESIAN_POINT ( 'NONE',  ( 0.3999999999999787059, -2.183180860297921466, -0.4937760292030871079 ) ) ;
#13780=CARTESIAN_POINT ( 'NONE',  ( 0.5762321503990789351, -1.646609333902588235, -0.4868944820179721966 ) ) ;
#13789=EDGE_CURVE ( 'NONE', #33249, #7589, #16106, .T. ) ;
#13795=ORIENTED_EDGE ( 'NONE', *, *, #9986, .T. ) ;
#13804=FACE_OUTER_BOUND ( 'NONE', #18513, .T. ) ;
#13806=EDGE_LOOP ( 'NONE', ( #9703, #1016, #13085 ) ) ;
#13811=CARTESIAN_POINT ( 'NONE',  ( 0.5007472363511182856, -1.585864761131932532, -0.4741568162196909131 ) ) ;
#13813=CARTESIAN_POINT ( 'NONE',  ( 0.02999999999997886302, -2.183180860297921466, -0.4937760292030871079 ) ) ;
#13823=LINE ( 'NONE', #4756, #7408 ) ;
#13828=CARTESIAN_POINT ( 'NONE',  ( 0.3699999999999786793, -2.120797187169804143, -0.5256435360466946705 ) ) ;
#13831=CARTESIAN_POINT ( 'NONE',  ( -0.004088490883478934287, -1.369644552158580053, -0.6494983983435047570 ) ) ;
#13833=AXIS2_PLACEMENT_3D ( 'NONE', #34842, #3790, #28882 ) ;
#13840=CARTESIAN_POINT ( 'NONE',  ( -4.849418284861270240E-05, -2.028079589045944875, -0.6757198890148005122 ) ) ;
#13842=CARTESIAN_POINT ( 'NONE',  ( 0.3616412802241143476, -1.759290408630900693, -0.5212859374495405484 ) ) ;
#13843=CIRCLE ( 'NONE', #30941, 0.1033070866141734129 ) ;
#13855=EDGE_LOOP ( 'NONE', ( #27615, #31717, #15117, #19507, #26633 ) ) ;
#13856=CARTESIAN_POINT ( 'NONE',  ( 0.6613703362948644138, -1.499461042372710162, -0.6190604815614721979 ) ) ;
#13859=DIRECTION ( 'NONE',  ( 0.000000000000000000, 0.000000000000000000, -1.000000000000000000 ) ) ;
#13866=AXIS2_PLACEMENT_3D ( 'NONE', #10056, #13554, #10275 ) ;
#13871=DIRECTION ( 'NONE',  ( 0.8660512985181131329, 0.4999551463232375648, 0.000000000000000000 ) ) ;
#13876=CARTESIAN_POINT ( 'NONE',  ( 0.02999999999997891853, -2.097675824466501915, -0.7286991843995629381 ) ) ;
#13884=CARTESIAN_POINT ( 'NONE',  ( 0.6625354623209831484, -1.473466724634002523, -0.4125543668030850486 ) ) ;
#13892=CARTESIAN_POINT ( 'NONE',  ( 0.5731004126284177103, -1.543550752164076112, -0.5377031886939181993 ) ) ;
#13896=AXIS2_PLACEMENT_3D ( 'NONE', #18736, #21626, #12760 ) ;
#13897=AXIS2_PLACEMENT_3D ( 'NONE', #14590, #33117, #30222 ) ;
#13900=CARTESIAN_POINT ( 'NONE',  ( 0.4500146950278320346, -1.107499313017888065, -0.6660426939124520773 ) ) ;
#13902=ORIENTED_EDGE ( 'NONE', *, *, #20270, .T. ) ;
#13906=ORIENTED_EDGE ( 'NONE', *, *, #2221, .T. ) ;
#13912=CARTESIAN_POINT ( 'NONE',  ( 0.1424029337235096226, -1.400533250147911746, -0.6250000000000000000 ) ) ;
#13919=CARTESIAN_POINT ( 'NONE',  ( 0.4781934768423676818, -1.682642038360962600, -0.6151431148613257793 ) ) ;
#13925=DIRECTION ( 'NONE',  ( 0.8660512985181134660, 0.4999551463232372872, 0.000000000000000000 ) ) ;
#13929=CARTESIAN_POINT ( 'NONE',  ( 0.4212779473123670071, -1.592273152480388365, -0.6162687442765694135 ) ) ;
#13934=CARTESIAN_POINT ( 'NONE',  ( 0.6010818854071131589, -1.537619199427677552, -0.5899312111515385704 ) ) ;
#13936=CARTESIAN_POINT ( 'NONE',  ( 0.4165289612192157875, -1.649214957849792995, -0.4090022746517852359 ) ) ;
#13944=DIRECTION ( 'NONE',  ( -0.8660512985181133550, -0.4999551463232373982, 0.000000000000000000 ) ) ;
#13947=CARTESIAN_POINT ( 'NONE',  ( 0.3512419370235244087, -1.705526293757532397, -0.4723484404679085258 ) ) ;
#13952=CARTESIAN_POINT ( 'NONE',  ( -2.112274968902149179E-14, -2.062017255485956824, -0.3032107891533308286 ) ) ;
#13960=CARTESIAN_POINT ( 'NONE',  ( 0.02666506398941732164, -1.593264902264835081, -0.3735695336613014117 ) ) ;
#13965=AXIS2_PLACEMENT_3D ( 'NONE', #4925, #23670, #29624 ) ;
#13971=DIRECTION ( 'NONE',  ( -0.8660512985181135770, -0.4999551463232370652, 0.000000000000000000 ) ) ;
#13977=ADVANCED_FACE ( 'NONE', ( #31601 ), #32673, .F. ) ;
#13982=ORIENTED_EDGE ( 'NONE', *, *, #4525, .F. ) ;
#13983=DIRECTION ( 'NONE',  ( 1.000000000000000000, 0.000000000000000000, 0.000000000000000000 ) ) ;
#13985=AXIS2_PLACEMENT_3D ( 'NONE', #31853, #13324, #3858 ) ;
#13987=FACE_OUTER_BOUND ( 'NONE', #13402, .T. ) ;
#13995=CARTESIAN_POINT ( 'NONE',  ( 0.4207172239728091956, -1.680578273617128859, -0.4138233700378491364 ) ) ;
#14006=CARTESIAN_POINT ( 'NONE',  ( 0.1977814221236954828, -1.253108843398078820, -0.3161890964247148217 ) ) ;
#14008=CARTESIAN_POINT ( 'NONE',  ( 0.7879355633825926297, -1.507076940126293341, -0.5155029497116575543 ) ) ;
#14018=CARTESIAN_POINT ( 'NONE',  ( 0.4846270837680086707, -1.589735006747021506, -0.4491141958821768809 ) ) ;
#14040=CARTESIAN_POINT ( 'NONE',  ( 0.1999999999999789724, -2.183180860297921466, -0.4437760292030870635 ) ) ;
#14042=( BOUNDED_SURFACE ( )  B_SPLINE_SURFACE ( 3, 2, ( 
 ( #20088, #32202, #39750 ),
 ( #32618, #4428, #38989 ),
 ( #11582, #10822, #23394 ),
 ( #20286, #32806, #36665 ),
 ( #29126, #22966, #35487 ),
 ( #19869, #16795, #39951 ),
 ( #21248, #9086, #11769 ),
 ( #37269, #34598, #30703 ),
 ( #2716, #5988, #27614 ),
 ( #21462, #33781, #37678 ),
 ( #37069, #15478, #6400 ),
 ( #9496, #18770, #24539 ),
 ( #24746, #5791, #8887 ),
 ( #18348, #15263, #40355 ) ),
 .UNSPECIFIED., .F., .F., .T. ) 
 B_SPLINE_SURFACE_WITH_KNOTS ( ( 4, 2, 2, 2, 2, 2, 4 ),
 ( 3, 3 ),
 ( -2.179246366695863912E-17, 0.0004568857926695675986, 0.0009137715853391569897, 0.001827543170678335663, 0.002741314756017514120, 0.003198200548687103566, 0.003655086341356693011 ),
 ( 0.000000000000000000, 1.000000000000000000 ),
 .UNSPECIFIED. ) 
 GEOMETRIC_REPRESENTATION_ITEM ( )  RATIONAL_B_SPLINE_SURFACE ( (
 ( 1.000000000000000000, 0.9183064432839357361, 1.000000000000000000),
 ( 1.000000000000000000, 0.9101286041442225860, 1.000000000000000000),
 ( 1.000000000000000000, 0.8997559524681660870, 1.000000000000000000),
 ( 1.000000000000000000, 0.8756591830432681745, 1.000000000000000000),
 ( 1.000000000000000000, 0.8619285237115705822, 1.000000000000000000),
 ( 1.000000000000000000, 0.8162943315712432035, 1.000000000000000000),
 ( 1.000000000000000000, 0.7805544280714898919, 1.000000000000000000),
 ( 1.000000000000000000, 0.7004798398954502625, 1.000000000000000000),
 ( 1.000000000000000000, 0.6558961615331188044, 1.000000000000000000),
 ( 1.000000000000000000, 0.5832821677979773689, 1.000000000000000000),
 ( 1.000000000000000000, 0.5580595141226901701, 1.000000000000000000),
 ( 1.000000000000000000, 0.5067813355089282323, 1.000000000000000000),
 ( 1.000000000000000000, 0.4806792815092485460, 1.000000000000000000),
 ( 1.000000000000000000, 0.4546663607463262702, 1.000000000000000000) ) ) 
 REPRESENTATION_ITEM ( '' )  SURFACE ( )  );
#14052=CARTESIAN_POINT ( 'NONE',  ( 0.5216412942450647794, -1.664807960596781378, -0.4415788522785766834 ) ) ;
#14056=CARTESIAN_POINT ( 'NONE',  ( 0.02113718185538869185, -1.627702592408575288, -0.6650890321891688162 ) ) ;
#14057=TOROIDAL_SURFACE ( 'NONE', #27867, 0.05000000000000000971, 0.1700000000000000400 ) ;
#14060=CARTESIAN_POINT ( 'NONE',  ( 0.3546968572579735635, -1.819852142027485131, -0.4886286422906724325 ) ) ;
#14075=CARTESIAN_POINT ( 'NONE',  ( 0.6539014128097314638, -1.538642141127189777, -0.6149031108187260619 ) ) ;
#14088=CARTESIAN_POINT ( 'NONE',  ( 0.1960722456818423942, -1.288731303253011218, -0.2917126172454974631 ) ) ;
#14089=CARTESIAN_POINT ( 'NONE',  ( 0.4252567597254975906, -1.612150615425755662, -0.6654510194314403604 ) ) ;
#14093=AXIS2_PLACEMENT_3D ( 'NONE', #18992, #37488, #15899 ) ;
#14095=EDGE_LOOP ( 'NONE', ( #5548, #13153, #11439, #29443 ) ) ;
#14104=CARTESIAN_POINT ( 'NONE',  ( 0.4487773978977022127, -1.660532028014278794, -0.6367102607372966405 ) ) ;
#14106=AXIS2_PLACEMENT_3D ( 'NONE', #17409, #11444, #36537 ) ;
#14111=CARTESIAN_POINT ( 'NONE',  ( 0.5716789463609788235, -1.545080002123852214, -0.5247704640587483871 ) ) ;
#14139=CARTESIAN_POINT ( 'NONE',  ( 0.5746532143667183457, -1.612791820318843605, -0.5120221665867487060 ) ) ;
#14143=DIRECTION ( 'NONE',  ( 0.9780874495037195082, 0.000000000000000000, -0.2081944790894049990 ) ) ;
#14147=CARTESIAN_POINT ( 'NONE',  ( 0.5711877923250709976, -1.574828153980617929, -0.4617130944781254187 ) ) ;
#14148=CARTESIAN_POINT ( 'NONE',  ( 0.4137599315575946624, -1.590143257116402697, -0.4137273532990791702 ) ) ;
#14151=CIRCLE ( 'NONE', #15488, 0.2000000000000000111 ) ;
#14164=CARTESIAN_POINT ( 'NONE',  ( 0.5264113014007612001, -1.640729993778266893, -0.5166151207188711680 ) ) ;
#14173=DIRECTION ( 'NONE',  ( 0.8660512985181135770, 0.4999551463232370652, 0.000000000000000000 ) ) ;
#14177=EDGE_CURVE ( 'NONE', #16906, #30709, #1008, .T. ) ;
#14179=CARTESIAN_POINT ( 'NONE',  ( 0.1721177234224999797, -1.269400047185449187, -0.7059945205881884567 ) ) ;
#14183=CARTESIAN_POINT ( 'NONE',  ( 0.1042552114927189771, -1.347860640450032843, -0.3579751000943771633 ) ) ;
#14196=CARTESIAN_POINT ( 'NONE',  ( 0.4469283285619459201, -1.099869350908816878, -0.4033480720695140631 ) ) ;
#14199=CARTESIAN_POINT ( 'NONE',  ( 0.3999999999999787059, -2.183180860297921466, -0.4437760292030870635 ) ) ;
#14216=DIRECTION ( 'NONE',  ( 0.4999551463232372317, -0.8660512985181135770, 0.000000000000000000 ) ) ;
#14218=CARTESIAN_POINT ( 'NONE',  ( 0.3999999999999786504, -1.971318270955308982, -0.3048432623593835822 ) ) ;
#14221=CARTESIAN_POINT ( 'NONE',  ( 0.1909286924077254199, -1.257064795538238577, -0.7137147910238503812 ) ) ;
#14226=DIRECTION ( 'NONE',  ( -0.4999551463232377313, 0.8660512985181132439, -0.000000000000000000 ) ) ;
#14232=CARTESIAN_POINT ( 'NONE',  ( 0.3694960952278112942, -1.758893817052062047, -0.4279539500891009762 ) ) ;
#14233=CARTESIAN_POINT ( 'NONE',  ( 0.4742406144748878005, -1.652140135034469548, -0.3982345435323125238 ) ) ;
#14235=CARTESIAN_POINT ( 'NONE',  ( 0.5033819511562486193, -1.584744444923489981, -0.5494471831687954833 ) ) ;
#14236=CARTESIAN_POINT ( 'NONE',  ( 0.3700000000004778355, -2.070564670722348399, -0.2996183892224198453 ) ) ;
#14237=CARTESIAN_POINT ( 'NONE',  ( 0.3999999999999798161, -2.097675824466503247, -0.2588528740066090017 ) ) ;
#14240=CARTESIAN_POINT ( 'NONE',  ( 0.3479125287944198064, -1.635177719134558894, -0.3750029027766745848 ) ) ;
#14243=CARTESIAN_POINT ( 'NONE',  ( 0.6146019880314795847, -1.612374571812595248, -0.5489582571658230270 ) ) ;
#14249=CARTESIAN_POINT ( 'NONE',  ( 0.3811251628308331418, -1.654782503697138196, -0.6335434503995733824 ) ) ;
#14252=CARTESIAN_POINT ( 'NONE',  ( 0.3391281936521367002, -1.652498152482349880, -0.5834905395359444302 ) ) ;
#14254=DIRECTION ( 'NONE',  ( 0.8660512985181133550, 0.4999551463232373427, 0.000000000000000000 ) ) ;
#14255=CARTESIAN_POINT ( 'NONE',  ( 0.3484951945142048535, -1.627819363848378220, -0.3328913857909800433 ) ) ;
#14261=ORIENTED_EDGE ( 'NONE', *, *, #13424, .T. ) ;
#14262=CARTESIAN_POINT ( 'NONE',  ( 0.1099573354880377524, -1.390855924928339427, -0.6976862894067923371 ) ) ;
#14263=EDGE_CURVE ( 'NONE', #23421, #36711, #27294, .T. ) ;
#14264=CARTESIAN_POINT ( 'NONE',  ( 0.3624369654652807027, -1.771784488814728720, -0.5049173149664405447 ) ) ;
#14267=ADVANCED_FACE ( 'NONE', ( #13285 ), #779, .T. ) ;
#14287=EDGE_CURVE ( 'NONE', #8639, #19627, #39840, .T. ) ;
#14288=CARTESIAN_POINT ( 'NONE',  ( 0.1913350121442598251, -1.664335509868100527, -0.6864462211259728663 ) ) ;
#14302=DIRECTION ( 'NONE',  ( 0.4999551463232372317, -0.8660512985181133550, 0.000000000000000000 ) ) ;
#14307=CARTESIAN_POINT ( 'NONE',  ( 0.4105658344535222937, -1.676523150947434759, -0.6311718820832802335 ) ) ;
#14312=CARTESIAN_POINT ( 'NONE',  ( 0.3984114568195522010, -1.599003643269838904, -0.5155029497116575543 ) ) ;
#14314=CARTESIAN_POINT ( 'NONE',  ( 0.5801945607878721267, -1.527237371078230099, -0.5722706679201888802 ) ) ;
#14327=AXIS2_PLACEMENT_3D ( 'NONE', #14676, #7696, #10792 ) ;
#14333=DIRECTION ( 'NONE',  ( -0.000000000000000000, -0.000000000000000000, 1.000000000000000000 ) ) ;
#14338=CARTESIAN_POINT ( 'NONE',  ( 0.6041280778791606743, -1.590911168834266087, -0.4817497659024419510 ) ) ;
#14344=CARTESIAN_POINT ( 'NONE',  ( 0.5662217921320245040, -1.581573517294255327, -0.5498102858096727275 ) ) ;
#14349=CARTESIAN_POINT ( 'NONE',  ( 0.4771029018757274587, -1.092484280813812880, -0.6132796080549755002 ) ) ;
#14350=CARTESIAN_POINT ( 'NONE',  ( 0.3625960434667522270, -1.762758894398491760, -0.5926935080085824481 ) ) ;
#14356=ORIENTED_EDGE ( 'NONE', *, *, #40303, .F. ) ;
#14358=CARTESIAN_POINT ( 'NONE',  ( 0.001234214386605718763, -1.915398013912305020, -0.3390371575412679528 ) ) ;
#14359=ORIENTED_EDGE ( 'NONE', *, *, #22736, .T. ) ;
#14367=EDGE_LOOP ( 'NONE', ( #3841, #39719, #38750, #23469 ) ) ;
#14368=CARTESIAN_POINT ( 'NONE',  ( 0.02069983512658924232, -1.633280642454262299, -0.6383422127260822698 ) ) ;
#14372=DIRECTION ( 'NONE',  ( -0.4999551463232373427, 0.8660512985181134660, -0.000000000000000000 ) ) ;
#14385=CARTESIAN_POINT ( 'NONE',  ( 0.3830122863959673496, -1.758151531859595940, -0.5806909769145761624 ) ) ;
#14388=ORIENTED_EDGE ( 'NONE', *, *, #22629, .F. ) ;
#14392=CARTESIAN_POINT ( 'NONE',  ( 0.4286120410367322831, -1.695948118333154175, -0.4141277345387682218 ) ) ;
#14400=ORIENTED_EDGE ( 'NONE', *, *, #37284, .F. ) ;
#14403=FACE_OUTER_BOUND ( 'NONE', #10889, .T. ) ;
#14415=CARTESIAN_POINT ( 'NONE',  ( 0.02999607453758957112, -2.087869005097287900, -0.7252195465745518987 ) ) ;
#14417=CARTESIAN_POINT ( 'NONE',  ( 0.3699434352739217058, -1.746858712014902837, -0.4245076167963743874 ) ) ;
#14419=CARTESIAN_POINT ( 'NONE',  ( 0.3438206814357017693, -1.630517872472182717, -0.5974003366333684450 ) ) ;
#14420=DIRECTION ( 'NONE',  ( -0.000000000000000000, 0.9396926207859077618, -0.3420201433256703782 ) ) ;
#14423=CARTESIAN_POINT ( 'NONE',  ( 0.3853365039963215777, -1.652093682163138899, -0.3956870249903656767 ) ) ;
#14425=CARTESIAN_POINT ( 'NONE',  ( 0.6343156381093978391, -1.595758837318228318, -0.5875140676452393906 ) ) ;
#14430=EDGE_CURVE ( 'NONE', #27329, #37901, #17182, .T. ) ;
#14435=CARTESIAN_POINT ( 'NONE',  ( 0.4120109984136325343, -1.649442217255613352, -0.6281670533134574574 ) ) ;
#14436=ADVANCED_FACE ( 'NONE', ( #33423 ), #14708, .F. ) ;
#14441=CARTESIAN_POINT ( 'NONE',  ( 0.2078177976682006600, -1.286321083125659070, -0.6333872262875119841 ) ) ;
#14442=CARTESIAN_POINT ( 'NONE',  ( 0.3922705187144002181, -1.780030872646382489, -0.5047570873693943971 ) ) ;
#14444=CARTESIAN_POINT ( 'NONE',  ( 0.4887921365776448090, -1.679766821171225999, -0.4193976862638449377 ) ) ;
#14448=CARTESIAN_POINT ( 'NONE',  ( -2.141776632491413013E-14, -2.087870288139423547, -0.7252158372584678325 ) ) ;
#14449=ORIENTED_EDGE ( 'NONE', *, *, #22629, .T. ) ;
#14473=CARTESIAN_POINT ( 'NONE',  ( 0.1844445096220149738, -1.686387118119738071, -0.6842090968296730136 ) ) ;
#14474=CARTESIAN_POINT ( 'NONE',  ( 0.3596349888097467029, -1.738430108238112837, -0.5125614369301060291 ) ) ;
#14476=ADVANCED_FACE ( 'NONE', ( #30552 ), #36910, .T. ) ;
#14478=EDGE_CURVE ( 'NONE', #37277, #27529, #27870, .T. ) ;
#14482=ORIENTED_EDGE ( 'NONE', *, *, #38438, .T. ) ;
#14485=EDGE_CURVE ( 'NONE', #16906, #20255, #12813, .T. ) ;
#14491=CARTESIAN_POINT ( 'NONE',  ( 0.4724743651013526557, -1.036800466722356928, -0.6317669042598009765 ) ) ;
#14495=EDGE_CURVE ( 'NONE', #23348, #25087, #4911, .T. ) ;
#14500=CARTESIAN_POINT ( 'NONE',  ( 0.1826252287685201647, -1.735863041130423001, -0.3273879975417062216 ) ) ;
#14513=CARTESIAN_POINT ( 'NONE',  ( 0.4434606427239963788, -1.107327905743432206, -0.6343696257487794199 ) ) ;
#14515=VERTEX_POINT ( 'NONE', #17990 ) ;
#14528=AXIS2_PLACEMENT_3D ( 'NONE', #1398, #23813, #11239 ) ;
#14530=FACE_OUTER_BOUND ( 'NONE', #8476, .T. ) ;
#14531=B_SPLINE_CURVE_WITH_KNOTS ( 'NONE', 3,
 ( #38997, #16994, #14104, #7517, #14307, #26679 ),
 .UNSPECIFIED., .F., .F.,
 ( 4, 2, 4 ),
 ( 1.734723475976807480E-18, 0.001056481483988077653, 0.002112962967976153572 ),
 .UNSPECIFIED. ) ;
#14533=CARTESIAN_POINT ( 'NONE',  ( 0.3925725722532341089, -1.687157587457473129, -0.6235540241194872380 ) ) ;
#14536=CARTESIAN_POINT ( 'NONE',  ( 0.6401971904170186134, -1.582074201254710655, -0.5981628054357688296 ) ) ;
#14537=CARTESIAN_POINT ( 'NONE',  ( 0.09571836153246564283, -1.423919396819204763, -0.6901719388955009915 ) ) ;
#14543=CARTESIAN_POINT ( 'NONE',  ( 0.5812003729376085115, -1.520186550829109029, -0.4529008768009907815 ) ) ;
#14560=CARTESIAN_POINT ( 'NONE',  ( 0.01381577305234537624, -1.692631703545224298, -0.3687587685671118720 ) ) ;
#14562=CARTESIAN_POINT ( 'NONE',  ( 0.3400028867877604721, -1.710946582846349484, -0.5979181485037454724 ) ) ;
#14567=CARTESIAN_POINT ( 'NONE',  ( 0.4559719632891928720, -1.698713290701216350, -0.5155029497116575543 ) ) ;
#14571=CARTESIAN_POINT ( 'NONE',  ( 0.1909286924077254199, -1.257064795538238577, -0.7137147910238503812 ) ) ;
#14586=EDGE_CURVE ( 'NONE', #16852, #34414, #20179, .T. ) ;
#14590=CARTESIAN_POINT ( 'NONE',  ( 0.4264202721361137760, -1.467519734074644200, -0.5166151207188711680 ) ) ;
#14591=CARTESIAN_POINT ( 'NONE',  ( 0.3864838284833568283, -1.745248947331494493, -0.5867414496849889805 ) ) ;
#14598=CARTESIAN_POINT ( 'NONE',  ( 0.4308075356823584112, -1.675781595220191544, -0.4121263904455738647 ) ) ;
#14602=VERTEX_POINT ( 'NONE', #7055 ) ;
#14606=ORIENTED_EDGE ( 'NONE', *, *, #27835, .T. ) ;
#14611=B_SPLINE_CURVE_WITH_KNOTS ( 'NONE', 3,
 ( #16432, #13137, #32465, #32074, #19338, #13947, #26515, #39052, #22637, #32254, #35168, #10883 ),
 .UNSPECIFIED., .F., .F.,
 ( 4, 2, 2, 2, 2, 4 ),
 ( 0.000000000000000000, 0.0004057368307213396106, 0.0008114736614426792212, 0.001622947322885360611, 0.002434420984328041892, 0.003245894645770723390 ),
 .UNSPECIFIED. ) ;
#14626=CARTESIAN_POINT ( 'NONE',  ( 0.4098430630954423282, -1.734253481485309889, -0.4297810291093706048 ) ) ;
#14627=DIRECTION ( 'NONE',  ( -0.2352930446943608811, 0.000000000000000000, 0.9719244739785378728 ) ) ;
#14628=CARTESIAN_POINT ( 'NONE',  ( 0.3879575449432583478, -1.659955875966160344, -0.6176084244450742444 ) ) ;
#14629=CARTESIAN_POINT ( 'NONE',  ( 0.1999999999739020262, -2.089771245945420297, -0.2936552384769813839 ) ) ;
#14634=AXIS2_PLACEMENT_3D ( 'NONE', #10694, #32699, #23052 ) ;
#14635=CARTESIAN_POINT ( 'NONE',  ( 0.1959265899308195724, -1.288818386415671036, -0.7414046965098800568 ) ) ;
#14641=AXIS2_PLACEMENT_3D ( 'NONE', #12890, #15148, #18439 ) ;
#14649=CARTESIAN_POINT ( 'NONE',  ( 0.2628772568534702980, -1.648529995711587093, -0.6889491329077820359 ) ) ;
#14652=CARTESIAN_POINT ( 'NONE',  ( 0.3751224099013009128, -1.759386797955041937, -0.4365224296969196782 ) ) ;
#14659=CARTESIAN_POINT ( 'NONE',  ( 0.1312036698469882245, -1.353276179866121032, -0.7088635643309191270 ) ) ;
#14660=EDGE_LOOP ( 'NONE', ( #2986, #3839, #31931, #98 ) ) ;
#14676=CARTESIAN_POINT ( 'NONE',  ( 0.4712917872827126486, -1.037483146682964819, -0.3984834965322623379 ) ) ;
#14680=EDGE_CURVE ( 'NONE', #38085, #38511, #28050, .T. ) ;
#14685=PLANE ( 'NONE',  #20710 ) ;
#14688=( LENGTH_UNIT ( ) NAMED_UNIT ( * ) SI_UNIT ( $, .METRE. ) );
#14691=CARTESIAN_POINT ( 'NONE',  ( 0.3872487238088446748, -1.838325393793988516, -0.4833546249010213236 ) ) ;
#14698=B_SPLINE_CURVE_WITH_KNOTS ( 'NONE', 3,
 ( #3297, #19155, #40338, #18532, #12167, #24729, #24922, #22060 ),
 .UNSPECIFIED., .F., .F.,
 ( 4, 2, 2, 4 ),
 ( 0.000000000000000000, 0.0003093940741824799281, 0.0006187881483649598563, 0.001237576296729922098 ),
 .UNSPECIFIED. ) ;
#14700=CARTESIAN_POINT ( 'NONE',  ( 0.4738546087217606062, -1.652018268363231845, -0.3975985852014427002 ) ) ;
#14703=DIRECTION ( 'NONE',  ( 0.8660512985181142431, 0.4999551463232357884, 0.000000000000000000 ) ) ;
#14705=VECTOR ( 'NONE', #8064, 39.37007874015748854 ) ;
#14707=ORIENTED_EDGE ( 'NONE', *, *, #22501, .T. ) ;
#14708=CYLINDRICAL_SURFACE ( 'NONE', #4276, 0.04330708661417343591 ) ;
#14718=CARTESIAN_POINT ( 'NONE',  ( 0.2029880746140099723, -1.647471528829948184, -0.3289985474335726523 ) ) ;
#14720=CARTESIAN_POINT ( 'NONE',  ( 0.3409152363046967782, -1.516880185093673061, -0.4991292961807996531 ) ) ;
#14731=CARTESIAN_POINT ( 'NONE',  ( 0.4650133494175291426, -1.133480851973431403, -0.6660426939124520773 ) ) ;
#14735=ADVANCED_FACE ( 'NONE', ( #28679 ), #23836, .F. ) ;
#14736=ORIENTED_EDGE ( 'NONE', *, *, #15454, .F. ) ;
#14738=EDGE_CURVE ( 'NONE', #4182, #16208, #20067, .T. ) ;
#14753=CARTESIAN_POINT ( 'NONE',  ( 0.4849246598550199239, -1.680545844843553516, -0.4179233548962039690 ) ) ;
#14754=EDGE_CURVE ( 'NONE', #6307, #3320, #13843, .T. ) ;
#14755=CARTESIAN_POINT ( 'NONE',  ( 0.6367656802301012720, -1.590386864768770225, -0.5922886263717986877 ) ) ;
#14756=CARTESIAN_POINT ( 'NONE',  ( 0.07358560013947622325, -1.491058954681647286, -0.6787182206095554449 ) ) ;
#14758=CARTESIAN_POINT ( 'NONE',  ( 0.4040663996170131833, -1.731104159697559597, -0.4314341983484236698 ) ) ;
#14761=CARTESIAN_POINT ( 'NONE',  ( 0.4040535148563422774, -1.747957131225893246, -0.5919255406249457341 ) ) ;
#14763=CARTESIAN_POINT ( 'NONE',  ( 0.4162641013412031188, -1.591898979695081096, -0.6171349719147453117 ) ) ;
#14768=CARTESIAN_POINT ( 'NONE',  ( 0.4697623592636160361, -1.061459377010899541, -0.6056023639864148711 ) ) ;
#14773=CARTESIAN_POINT ( 'NONE',  ( 0.6374494578080344143, -1.479249556658666087, -0.3955914010212834286 ) ) ;
#14780=CARTESIAN_POINT ( 'NONE',  ( 0.02999999999997891853, -2.097675824466501915, -0.7286991843995629381 ) ) ;
#14781=ORIENTED_EDGE ( 'NONE', *, *, #38058, .F. ) ;
#14787=DIRECTION ( 'NONE',  ( 0.4999551463232377313, -0.8660512985181132439, -0.000000000000000000 ) ) ;
#14802=DIRECTION ( 'NONE',  ( 0.4999551463232372317, -0.8660512985181134660, 0.000000000000000000 ) ) ;
#14806=EDGE_CURVE ( 'NONE', #2065, #29183, #5314, .T. ) ;
#14814=CARTESIAN_POINT ( 'NONE',  ( 0.2842326993136328195, -1.549395603922531617, -0.7208999815284821144 ) ) ;
#14815=CARTESIAN_POINT ( 'NONE',  ( 0.4010150227249208443, -1.731699465864716236, -0.5966698157887416754 ) ) ;
#14826=ORIENTED_EDGE ( 'NONE', *, *, #12521, .T. ) ;
#14828=ORIENTED_EDGE ( 'NONE', *, *, #7706, .F. ) ;
#14836=EDGE_CURVE ( 'NONE', #38684, #15024, #35393, .T. ) ;
#14839=ORIENTED_EDGE ( 'NONE', *, *, #22051, .F. ) ;
#14847=CARTESIAN_POINT ( 'NONE',  ( 0.4030327056923162510, -1.680968334469415737, -0.4031266960524318987 ) ) ;
#14848=CARTESIAN_POINT ( 'NONE',  ( 0.3866587253291882686, -1.756046511159857770, -0.5714736483329494465 ) ) ;
#14849=CARTESIAN_POINT ( 'NONE',  ( 0.3672875303838387673, -1.616970901354834789, -0.6123576500872188744 ) ) ;
#14853=CARTESIAN_POINT ( 'NONE',  ( 0.3461375923906637730, -1.629180363267989984, -0.4316302822133540884 ) ) ;
#14866=CARTESIAN_POINT ( 'NONE',  ( 0.4867251962510119045, -1.680960026995096612, -0.6125153944539966089 ) ) ;
#14871=CARTESIAN_POINT ( 'NONE',  ( 0.3812071769896464013, -1.763750790280049996, -0.4536492913030988894 ) ) ;
#14872=CARTESIAN_POINT ( 'NONE',  ( 0.5264113014007612001, -1.640729993778266893, -0.5166151207188711680 ) ) ;
#14879=DIRECTION ( 'NONE',  ( 0.8660512985181136880, 0.4999551463232368431, 0.000000000000000000 ) ) ;
#14883=AXIS2_PLACEMENT_3D ( 'NONE', #14567, #9202, #37200 ) ;
#14885=CARTESIAN_POINT ( 'NONE',  ( 0.3871723776641498027, -1.623769666286883462, -0.3715740632108985864 ) ) ;
#14890=FACE_OUTER_BOUND ( 'NONE', #19623, .T. ) ;
#14896=CARTESIAN_POINT ( 'NONE',  ( 0.4052030310269085223, -1.718765290342715080, -0.6036971404997847346 ) ) ;
#14899=CARTESIAN_POINT ( 'NONE',  ( 0.02910065466421945385, -1.575914851856258014, -0.6367838632993687575 ) ) ;
#14904=AXIS2_PLACEMENT_3D ( 'NONE', #34272, #9787, #12466 ) ;
#14905=CARTESIAN_POINT ( 'NONE',  ( 0.1971914821640197435, -2.028516189135913361, -0.6778075598240375088 ) ) ;
#14914=DIRECTION ( 'NONE',  ( 1.000000000000000000, 0.000000000000000000, 0.000000000000000000 ) ) ;
#14915=VERTEX_POINT ( 'NONE', #2718 ) ;
#14923=FACE_OUTER_BOUND ( 'NONE', #11337, .T. ) ;
#14926=CARTESIAN_POINT ( 'NONE',  ( 0.2059273467974225835, -1.283046334493782359, -0.2869361388274796476 ) ) ;
#14939=ORIENTED_EDGE ( 'NONE', *, *, #33344, .T. ) ;
#14942=CARTESIAN_POINT ( 'NONE',  ( 0.4053854983667099510, -1.732300422170438559, -0.5284674333234674615 ) ) ;
#14947=CARTESIAN_POINT ( 'NONE',  ( 0.2059273467974223892, -1.283046334493782137, -0.3614788220720648870 ) ) ;
#14948=CARTESIAN_POINT ( 'NONE',  ( 0.2989471840069001241, -1.160067769014730521, -0.5155029497116575543 ) ) ;
#14950=CIRCLE ( 'NONE', #33353, 0.2499999999999999445 ) ;
#14954=CARTESIAN_POINT ( 'NONE',  ( 0.6418861098210334459, -1.577688375363704099, -0.6007762697806591223 ) ) ;
#14955=CARTESIAN_POINT ( 'NONE',  ( 0.4259519167603003642, -1.697610851774717267, -0.6162422480182934148 ) ) ;
#14965=CARTESIAN_POINT ( 'NONE',  ( 0.4781934768423681814, -1.682642038360963710, -0.6151431148613258904 ) ) ;
#14967=B_SPLINE_SURFACE_WITH_KNOTS ( 'NONE', 3, 3, ( 
 ( #16869, #12472, #25027, #21560 ),
 ( #398, #22176, #21963, #18874 ),
 ( #31413, #3216, #34689, #6494 ),
 ( #12896, #34079, #39569, #5817 ),
 ( #15297, #5624, #30731, #18376 ),
 ( #1955, #27038, #12217, #33597 ),
 ( #18180, #23970, #39783, #30531 ) ),
 .UNSPECIFIED., .F., .F., .F.,
 ( 4, 3, 4 ),
 ( 4, 4 ),
 ( 0.7035562186971585641, 0.8517781093485792265, 1.000000000000000000 ),
 ( 0.4463408799211898148, 0.5556952876593606039 ),
 .UNSPECIFIED. ) ;
#14977=ORIENTED_EDGE ( 'NONE', *, *, #2377, .T. ) ;
#14979=AXIS2_PLACEMENT_3D ( 'NONE', #421, #25470, #32426 ) ;
#14982=CARTESIAN_POINT ( 'NONE',  ( 0.3560528695691858592, -1.750603236759655568, -0.5461972732282710519 ) ) ;
#14987=CARTESIAN_POINT ( 'NONE',  ( 0.4909801108973092520, -1.199306193601649362, -0.5155029497116575543 ) ) ;
#14993=CARTESIAN_POINT ( 'NONE',  ( 0.3299395734357897791, -1.474170237420246332, -0.3144976166544465324 ) ) ;
#14996=CARTESIAN_POINT ( 'NONE',  ( 0.5755462064585110671, -1.567046512275164671, -0.4467185635149386047 ) ) ;
#15002=DIRECTION ( 'NONE',  ( 0.000000000000000000, 0.000000000000000000, -1.000000000000000000 ) ) ;
#15006=TOROIDAL_SURFACE ( 'NONE', #24862, 0.05330708661417342398, 0.01000000000000000021 ) ;
#15013=CARTESIAN_POINT ( 'NONE',  ( 0.3884081897485042734, -1.743572994024308764, -0.5875882558984819592 ) ) ;
#15014=EDGE_CURVE ( 'NONE', #17181, #37380, #17165, .T. ) ;
#15017=( BOUNDED_SURFACE ( )  B_SPLINE_SURFACE ( 3, 2, ( 
 ( #33442, #13900, #14731 ),
 ( #5250, #30163, #1990 ),
 ( #27298, #17803, #4445 ),
 ( #14513, #1806, #39413 ),
 ( #17007, #29550, #26473 ),
 ( #35933, #10844, #23606 ) ),
 .UNSPECIFIED., .F., .F., .F. ) 
 B_SPLINE_SURFACE_WITH_KNOTS ( ( 4, 2, 4 ),
 ( 3, 3 ),
 ( 0.000000000000000000, 0.0006500322046037510827, 0.001300064409207502165 ),
 ( 0.000000000000000000, 1.000000000000000000 ),
 .UNSPECIFIED. ) 
 GEOMETRIC_REPRESENTATION_ITEM ( )  RATIONAL_B_SPLINE_SURFACE ( (
 ( 1.000000000000000000, 0.7071067811865482389, 1.000000000000000000),
 ( 1.000000000000000000, 0.7294884244153418962, 1.000000000000000000),
 ( 1.000000000000000000, 0.7497986155812718101, 1.000000000000000000),
 ( 1.000000000000000000, 0.7883845046990943795, 1.000000000000000000),
 ( 1.000000000000000000, 0.8056655519482062155, 1.000000000000000000),
 ( 1.000000000000000000, 0.8219793159978240338, 1.000000000000000000) ) ) 
 REPRESENTATION_ITEM ( '' )  SURFACE ( )  );
#15019=VERTEX_POINT ( 'NONE', #34600 ) ;
#15024=VERTEX_POINT ( 'NONE', #37893 ) ;
#15025=ORIENTED_EDGE ( 'NONE', *, *, #39400, .T. ) ;
#15031=CARTESIAN_POINT ( 'NONE',  ( 0.5051063752723966571, -1.605425671313008174, -0.4055270845263394541 ) ) ;
#15032=CARTESIAN_POINT ( 'NONE',  ( 0.2923286432308245808, -1.660243258845594649, -0.3694143330441917450 ) ) ;
#15035=CARTESIAN_POINT ( 'NONE',  ( 0.1909291033137781868, -1.257065507333533727, -0.7137147910549515029 ) ) ;
#15040=DIRECTION ( 'NONE',  ( 0.4999551463232373427, -0.8660512985181134660, 0.000000000000000000 ) ) ;
#15046=CARTESIAN_POINT ( 'NONE',  ( 0.4104533603378005546, -1.744126031043197411, -0.4329192950746086899 ) ) ;
#15062=EDGE_CURVE ( 'NONE', #20255, #9760, #30298, .T. ) ;
#15074=CARTESIAN_POINT ( 'NONE',  ( 0.3586646726171237032, -1.755266051717878195, -0.5357449245709422492 ) ) ;
#15075=DIRECTION ( 'NONE',  ( 0.4999551463232373427, -0.8660512985181134660, 0.000000000000000000 ) ) ;
#15088=CARTESIAN_POINT ( 'NONE',  ( 0.4038347882558627200, -1.728811102478955419, -0.5994564538103192008 ) ) ;
#15091=CARTESIAN_POINT ( 'NONE',  ( 0.005216039386364625628, -1.801454245091123063, -0.6400404412376492491 ) ) ;
#15095=CARTESIAN_POINT ( 'NONE',  ( 0.3559771861491330958, -1.881699356250711164, -0.5088919887031481126 ) ) ;
#15096=CARTESIAN_POINT ( 'NONE',  ( 0.1359911470193229943, -1.231045907863504763, -0.5155029497116575543 ) ) ;
#15112=CARTESIAN_POINT ( 'NONE',  ( 0.1916844733273856960, -1.960004612374577793, -0.3277737872114317996 ) ) ;
#15115=CARTESIAN_POINT ( 'NONE',  ( 0.1909286924077255032, -1.257064795538239022, -0.2869361388274796476 ) ) ;
#15117=ORIENTED_EDGE ( 'NONE', *, *, #16498, .F. ) ;
#15120=ORIENTED_EDGE ( 'NONE', *, *, #35638, .F. ) ;
#15127=CARTESIAN_POINT ( 'NONE',  ( 0.3700000000046924642, -2.091145340040783562, -0.6943969493414033911 ) ) ;
#15132=CARTESIAN_POINT ( 'NONE',  ( 0.4671578922472904849, -1.051416226764902762, -0.5155029497116575543 ) ) ;
#15145=CARTESIAN_POINT ( 'NONE',  ( 0.6626570520036878520, -1.467463602353352936, -0.4130250948898684937 ) ) ;
#15146=CARTESIAN_POINT ( 'NONE',  ( 0.06555721432897218537, -1.525479238971202633, -0.6748405168658114794 ) ) ;
#15148=DIRECTION ( 'NONE',  ( 0.4999551463232373427, -0.8660512985181134660, 0.000000000000000000 ) ) ;
#15149=CARTESIAN_POINT ( 'NONE',  ( 0.3699999999999786793, -2.120723258816476609, -0.4622723469118392714 ) ) ;
#15150=B_SPLINE_CURVE_WITH_KNOTS ( 'NONE', 3,
 ( #36427, #8239, #32525, #26174 ),
 .UNSPECIFIED., .F., .F.,
 ( 4, 4 ),
 ( 0.01480563966802933389, 0.01646152871071565604 ),
 .UNSPECIFIED. ) ;
#15151=EDGE_CURVE ( 'NONE', #12338, #40387, #34870, .T. ) ;
#15154=CARTESIAN_POINT ( 'NONE',  ( 0.3659513052091539209, -1.747039640913286451, -0.4990343722649543956 ) ) ;
#15155=CARTESIAN_POINT ( 'NONE',  ( 0.6158309935355448239, -1.474965975646107763, -0.6185374182054230729 ) ) ;
#15164=CIRCLE ( 'NONE', #3324, 0.05000000000000000971 ) ;
#15166=CARTESIAN_POINT ( 'NONE',  ( 0.4829308845308043496, -1.609609321180353714, -0.6424438852754091878 ) ) ;
#15181=ORIENTED_EDGE ( 'NONE', *, *, #32769, .F. ) ;
#15185=CARTESIAN_POINT ( 'NONE',  ( 0.4356662251172991329, -1.610775558009423847, -0.3686272921855576756 ) ) ;
#15188=CARTESIAN_POINT ( 'NONE',  ( 0.5699416983924746605, -1.576656387088807509, -0.4662384028606618158 ) ) ;
#15202=CARTESIAN_POINT ( 'NONE',  ( 0.1999999999999789169, -2.097675824466503247, -0.2588528740066096678 ) ) ;
#15209=CARTESIAN_POINT ( 'NONE',  ( 0.4038347882558627200, -1.728811102478955419, -0.5994564538103192008 ) ) ;
#15210=CARTESIAN_POINT ( 'NONE',  ( 0.2026546822922886959, -1.284935582237593854, -0.2885605078203434259 ) ) ;
#15220=EDGE_CURVE ( 'NONE', #39658, #38602, #11244, .T. ) ;
#15225=CARTESIAN_POINT ( 'NONE',  ( 0.4878806933278804214, -1.547354733665422311, -0.5155029497116575543 ) ) ;
#15246=ADVANCED_FACE ( 'NONE', ( #20540 ), #10091, .T. ) ;
#15263=CARTESIAN_POINT ( 'NONE',  ( 0.3929308436705500340, -1.654878899977479723, -0.4107462969406636688 ) ) ;
#15269=VERTEX_POINT ( 'NONE', #33904 ) ;
#15283=CARTESIAN_POINT ( 'NONE',  ( 0.1909286924077255032, -1.257064795538239022, -0.2869361388274796476 ) ) ;
#15290=ORIENTED_EDGE ( 'NONE', *, *, #15742, .F. ) ;
#15296=VECTOR ( 'NONE', #13871, 39.37007874015748854 ) ;
#15297=CARTESIAN_POINT ( 'NONE',  ( 0.3690044633497405746, -2.059848083720738021, -0.4704986862936899605 ) ) ;
#15300=TOROIDAL_SURFACE ( 'NONE', #27786, 0.05000000000000000971, 0.1700000000000000400 ) ;
#15301=CARTESIAN_POINT ( 'NONE',  ( 0.3717218693272927865, -1.759037576843597073, -0.4317987013060715640 ) ) ;
#15308=ADVANCED_FACE ( 'NONE', ( #5889 ), #31363, .T. ) ;
#15309=CARTESIAN_POINT ( 'NONE',  ( 0.3649451899893845219, -1.762153390321482549, -0.4829678164902960757 ) ) ;
#15317=CARTESIAN_POINT ( 'NONE',  ( -2.112273405726188513E-14, -2.097675824466503691, -0.2907077406111384099 ) ) ;
#15322=ORIENTED_EDGE ( 'NONE', *, *, #38550, .T. ) ;
#15331=CARTESIAN_POINT ( 'NONE',  ( 0.1757500541653520820, -1.230771478115229245, -0.4400554600884079570 ) ) ;
#15342=CARTESIAN_POINT ( 'NONE',  ( 0.1810766014996237627, -1.262752222553218395, -0.2917159793182508842 ) ) ;
#15344=CARTESIAN_POINT ( 'NONE',  ( 0.3999999999999786504, -2.143487347927110598, -0.5325376609221695867 ) ) ;
#15345=CARTESIAN_POINT ( 'NONE',  ( 0.1983600803612964869, -2.021069303733847189, -0.2825292762747920183 ) ) ;
#15358=CARTESIAN_POINT ( 'NONE',  ( 0.6412634316914778143, -1.498276373346698165, -0.4128329508740462561 ) ) ;
#15369=EDGE_CURVE ( 'NONE', #2187, #23858, #21637, .T. ) ;
#15370=CARTESIAN_POINT ( 'NONE',  ( 0.4675494560575759184, -1.684665788739993619, -0.6179439388203937789 ) ) ;
#15372=CARTESIAN_POINT ( 'NONE',  ( 0.5304177574979601628, -1.660704847279741214, -0.5790554921387824905 ) ) ;
#15374=DIRECTION ( 'NONE',  ( -0.4999551463232373427, 0.8660512985181134660, -0.000000000000000000 ) ) ;
#15375=CARTESIAN_POINT ( 'NONE',  ( 0.3984114568195522010, -1.599003643269838904, -0.5155029497116575543 ) ) ;
#15380=DIRECTION ( 'NONE',  ( 0.4999551463232372317, -0.8660512985181135770, 0.000000000000000000 ) ) ;
#15381=EDGE_LOOP ( 'NONE', ( #33339, #36826 ) ) ;
#15385=CARTESIAN_POINT ( 'NONE',  ( 0.1831853279715622285, -1.261726972505375910, -0.3225413305835142519 ) ) ;
#15401=CARTESIAN_POINT ( 'NONE',  ( 0.5623860021574346169, -1.585002265747556871, -0.5017772603597512315 ) ) ;
#15421=CARTESIAN_POINT ( 'NONE',  ( 0.3693979415174998282, -1.758566222085671704, -0.5866259412024878994 ) ) ;
#15423=EDGE_CURVE ( 'NONE', #4341, #7054, #30933, .T. ) ;
#15426=EDGE_CURVE ( 'NONE', #28841, #27374, #31592, .T. ) ;
#15432=EDGE_CURVE ( 'NONE', #23563, #28743, #12566, .T. ) ;
#15445=CARTESIAN_POINT ( 'NONE',  ( 0.4203826191881492313, -1.700944664958275343, -0.4172566670736511107 ) ) ;
#15449=CARTESIAN_POINT ( 'NONE',  ( 0.3853645080447097304, -1.799773605325351467, -0.4824436846277732061 ) ) ;
#15452=AXIS2_PLACEMENT_3D ( 'NONE', #12234, #21299, #33840 ) ;
#15454=EDGE_CURVE ( 'NONE', #5500, #26101, #123, .T. ) ;
#15455=DIRECTION ( 'NONE',  ( 0.000000000000000000, 0.000000000000000000, -1.000000000000000000 ) ) ;
#15457=CARTESIAN_POINT ( 'NONE',  ( 0.5030897102885044658, -1.688833090636736145, -0.4393626443944793625 ) ) ;
#15475=DIRECTION ( 'NONE',  ( 0.8660512985181133550, 0.4999551463232371207, 1.536967049004847180E-15 ) ) ;
#15478=CARTESIAN_POINT ( 'NONE',  ( 0.3787673471718397966, -1.665243962817426704, -0.4196842139337432775 ) ) ;
#15488=AXIS2_PLACEMENT_3D ( 'NONE', #34586, #9693, #28206 ) ;
#15490=ORIENTED_EDGE ( 'NONE', *, *, #29736, .F. ) ;
#15493=FACE_OUTER_BOUND ( 'NONE', #31166, .T. ) ;
#15499=FACE_OUTER_BOUND ( 'NONE', #29069, .T. ) ;
#15507=CLOSED_SHELL ( 'NONE', ( #17310, #28649, #935, #24846, #33006, #6495, #20956, #2911, #25363, #40189, #1610, #3393, #36604, #39072, #14436, #37964, #31924, #18995, #13312, #11153, #10639, #21903, #17184, #17530, #29031, #2699, #25242, #39618, #26083, #27056, #10299, #16623, #26245, #31031, #31282, #9536, #33070, #882, #992, #459, #25344, #6914, #9886, #9665, #14735, #36930, #7138, #12921, #9146, #30801, #14267, #39746, #37930, #21236, #35961, #32821, #33615, #39853, #27003, #39905, #762, #22860, #31582, #5366, #38157, #2612, #3260, #11437, #20006, #11268, #6860, #16674, #10045, #27735, #34939, #30068, #39924, #31599, #33612, #24880, #26201, #14476, #39342, #28585, #10009, #438, #38355, #23375, #10020, #4423, #4700, #17790, #36384, #1869, #31362, #11586, #36561, #7851, #23302, #5369, #34797, #12932, #35421, #21541, #1387, #13230, #7762, #28674, #15246, #1133, #20739, #29885, #15955, #10401, #36447, #19699, #10006, #7076, #26477, #33821, #26113, #27277, #29374, #21629, #34627, #15308, #20910, #35034, #40121, #30648, #33317, #2214, #13977, #25218, #23592, #3703, #37559, #6383, #35511, #19952, #19600, #3629, #22235, #35376, #35360, #17477, #9188, #24265, #3857, #37193, #4127, #13586, #21294, #37411, #12696, #40438 ) ) ;
#15510=CARTESIAN_POINT ( 'NONE',  ( 0.4833848602004494621, -1.629403264803032547, -0.6020753396110556377 ) ) ;
#15515=AXIS2_PLACEMENT_3D ( 'NONE', #7279, #6685, #32190 ) ;
#15519=CARTESIAN_POINT ( 'NONE',  ( 0.3544453792448893359, -1.829125709028288194, -0.5151468183741818585 ) ) ;
#15527=EDGE_CURVE ( 'NONE', #9403, #14602, #30370, .T. ) ;
#15539=CARTESIAN_POINT ( 'NONE',  ( 0.3669548114133807659, -2.020640157311806462, -0.3128670423345359941 ) ) ;
#15553=CARTESIAN_POINT ( 'NONE',  ( 0.3519337645836231876, -1.625834341939006222, -0.3689444309192750904 ) ) ;
#15557=CARTESIAN_POINT ( 'NONE',  ( 0.3962551329634386721, -2.018354224907537464, -0.4857151794559766422 ) ) ;
#15563=CARTESIAN_POINT ( 'NONE',  ( -2.112273405726188513E-14, -2.183180860297921466, -0.7137760292030871367 ) ) ;
#15564=DIRECTION ( 'NONE',  ( -0.4999551463232372317, 0.8660512985181135770, -0.000000000000000000 ) ) ;
#15570=CARTESIAN_POINT ( 'NONE',  ( 0.6100990983602245787, -1.580768839995616126, -0.4597541041496203129 ) ) ;
#15578=FACE_OUTER_BOUND ( 'NONE', #33858, .T. ) ;
#15580=EDGE_CURVE ( 'NONE', #30555, #27179, #37792, .T. ) ;
#15582=CARTESIAN_POINT ( 'NONE',  ( 0.3640014500131175113, -1.990332505625297843, -0.4924098530529640860 ) ) ;
#15585=CARTESIAN_POINT ( 'NONE',  ( 0.5450221536532190436, -1.653079618865306299, -0.5489132167387396066 ) ) ;
#15593=CIRCLE ( 'NONE', #38570, 0.2499999999999999722 ) ;
#15594=EDGE_LOOP ( 'NONE', ( #21362, #3479, #2678, #13024 ) ) ;
#15602=DIRECTION ( 'NONE',  ( 0.4999551463232372317, -0.8660512985181133550, 0.000000000000000000 ) ) ;
#15609=CARTESIAN_POINT ( 'NONE',  ( 0.2046676961208400425, -1.998811770563726720, -0.3203772732607386708 ) ) ;
#15612=CARTESIAN_POINT ( 'NONE',  ( 0.3666666666666453800, -2.097675824466503691, -0.2588528740066097233 ) ) ;
#15615=DIRECTION ( 'NONE',  ( -4.419165872103955473E-15, 0.3420201433256692680, -0.9396926207859082059 ) ) ;
#15620=CARTESIAN_POINT ( 'NONE',  ( 0.7521323256515352051, -1.545065466920227282, -0.5155029497116575543 ) ) ;
#15636=ORIENTED_EDGE ( 'NONE', *, *, #38154, .T. ) ;
#15639=VERTEX_POINT ( 'NONE', #9336 ) ;
#15641=CARTESIAN_POINT ( 'NONE',  ( 0.5030897103603338971, -1.688833090595270425, -0.4393626442577572844 ) ) ;
#15642=DIRECTION ( 'NONE',  ( 0.8660512985181134660, 0.4999551463232372317, 0.000000000000000000 ) ) ;
#15645=ORIENTED_EDGE ( 'NONE', *, *, #4851, .T. ) ;
#15647=CARTESIAN_POINT ( 'NONE',  ( 0.3925301276612754298, -1.756377271995033684, -0.4843757382520948451 ) ) ;
#15675=DIRECTION ( 'NONE',  ( 0.000000000000000000, 0.000000000000000000, -1.000000000000000000 ) ) ;
#15676=ORIENTED_EDGE ( 'NONE', *, *, #34653, .F. ) ;
#15678=ORIENTED_EDGE ( 'NONE', *, *, #29544, .F. ) ;
#15681=CARTESIAN_POINT ( 'NONE',  ( 0.3733765242244403426, -1.670306735275899568, -0.6070209750880516397 ) ) ;
#15686=CARTESIAN_POINT ( 'NONE',  ( 0.1757500541653520820, -1.230771478115229245, -0.4400554600884079570 ) ) ;
#15706=CARTESIAN_POINT ( 'NONE',  ( 0.3616412802241143476, -1.759290408630900693, -0.5212859374495405484 ) ) ;
#15721=ORIENTED_EDGE ( 'NONE', *, *, #29866, .F. ) ;
#15723=CARTESIAN_POINT ( 'NONE',  ( 0.3613124228137278293, -1.955507677535348376, -0.4996853815432704682 ) ) ;
#15726=CARTESIAN_POINT ( 'NONE',  ( -0.004088490883478934287, -1.369644552158580053, -0.6494983983435047570 ) ) ;
#15729=ORIENTED_EDGE ( 'NONE', *, *, #31848, .T. ) ;
#15732=CARTESIAN_POINT ( 'NONE',  ( 0.4875928425406638733, -1.627410370986559940, -0.4328921880033906322 ) ) ;
#15737=UNCERTAINTY_MEASURE_WITH_UNIT (LENGTH_MEASURE( 1.000000000000000082E-05 ), #1126, 'distance_accuracy_value', 'NONE');
#15742=EDGE_CURVE ( 'NONE', #22474, #22431, #11307, .T. ) ;
#15752=CARTESIAN_POINT ( 'NONE',  ( 0.6283006780106592526, -1.606940092472771031, -0.4564006025841033098 ) ) ;
#15762=CARTESIAN_POINT ( 'NONE',  ( 0.4137599315576318548, -1.590143257116449105, -0.4137273532990809466 ) ) ;
#15787=EDGE_LOOP ( 'NONE', ( #33987, #36585, #16596, #32963 ) ) ;
#15796=CARTESIAN_POINT ( 'NONE',  ( 0.4713981431917049214, -1.069104614441775958, -0.6069517949360595521 ) ) ;
#15802=CARTESIAN_POINT ( 'NONE',  ( 0.3159174789885340617, -1.473577620167767277, -0.2869361388274797586 ) ) ;
#15805=CARTESIAN_POINT ( 'NONE',  ( 0.3999999999999787059, -2.166079853131637645, -0.5407606602423824516 ) ) ;
#15806=FACE_OUTER_BOUND ( 'NONE', #26258, .T. ) ;
#15808=CARTESIAN_POINT ( 'NONE',  ( 0.2408414484411625089, -1.826577308757157958, -0.6567176230664488745 ) ) ;
#15809=CARTESIAN_POINT ( 'NONE',  ( 0.3507599413761057772, -1.722433222888394289, -0.4396544696549837816 ) ) ;
#15814=CARTESIAN_POINT ( 'NONE',  ( 0.2923286432308245808, -1.660243258845594649, -0.6250000000000000000 ) ) ;
#15815=ORIENTED_EDGE ( 'NONE', *, *, #36074, .T. ) ;
#15818=CARTESIAN_POINT ( 'NONE',  ( 0.2265531926702374077, -1.599072214040516249, -0.6987977643162676111 ) ) ;
#15820=DIRECTION ( 'NONE',  ( 0.000000000000000000, 0.3306821564015692827, 0.9437421848352484099 ) ) ;
#15833=ORIENTED_EDGE ( 'NONE', *, *, #29326, .F. ) ;
#15842=CARTESIAN_POINT ( 'NONE',  ( -2.112273405726188513E-14, -2.097675824466503691, -0.7286991843995640483 ) ) ;
#15845=CARTESIAN_POINT ( 'NONE',  ( 0.3839874728425691219, -1.826195879522261700, -0.4830234552410120896 ) ) ;
#15846=CARTESIAN_POINT ( 'NONE',  ( 0.3921301437161267556, -1.752887964102751051, -0.4509272787481405365 ) ) ;
#15849=CYLINDRICAL_SURFACE ( 'NONE', #2787, 0.2200000000000000566 ) ;
#15850=CARTESIAN_POINT ( 'NONE',  ( 0.5185821078323552547, -1.679889620551088258, -0.4521106403869140644 ) ) ;
#15860=CARTESIAN_POINT ( 'NONE',  ( 0.3738055494968318682, -1.722068535337600848, -0.4175881411983431435 ) ) ;
#15863=AXIS2_PLACEMENT_3D ( 'NONE', #9288, #3134, #15675 ) ;
#15894=CARTESIAN_POINT ( 'NONE',  ( 0.3758474042836421614, -1.611613784703100016, -0.3604881591361508431 ) ) ;
#15899=DIRECTION ( 'NONE',  ( 0.4999551463232376758, -0.8660512985181131329, 0.000000000000000000 ) ) ;
#15901=CARTESIAN_POINT ( 'NONE',  ( 0.6409058204046232943, -1.459016202299332710, -0.5155029497116575543 ) ) ;
#15917=CARTESIAN_POINT ( 'NONE',  ( 0.2160079821674734668, -1.358042438312749622, -0.3319550444996756111 ) ) ;
#15920=ORIENTED_EDGE ( 'NONE', *, *, #35867, .T. ) ;
#15928=CARTESIAN_POINT ( 'NONE',  ( 0.2247055958334348014, -1.611582774488795611, -0.3560079958479117623 ) ) ;
#15935=EDGE_CURVE ( 'NONE', #8017, #32089, #16562, .T. ) ;
#15937=ORIENTED_EDGE ( 'NONE', *, *, #27646, .T. ) ;
#15945=CARTESIAN_POINT ( 'NONE',  ( 0.4445735045382223638, -1.592385390845466375, -0.4212583484125541622 ) ) ;
#15954=TOROIDAL_SURFACE ( 'NONE', #38934, 0.05330708661417342398, 0.01000000000000000021 ) ;
#15955=ADVANCED_FACE ( 'NONE', ( #4391 ), #21641, .T. ) ;
#15958=CARTESIAN_POINT ( 'NONE',  ( 0.1784968570797965948, -1.218054820023663831, -0.5155029497116575543 ) ) ;
#15965=CARTESIAN_POINT ( 'NONE',  ( 0.6231091328894153847, -1.554071593431288756, -0.4320382102285837966 ) ) ;
#15967=DIRECTION ( 'NONE',  ( -0.4999551463232377313, 0.8660512985181132439, -0.000000000000000000 ) ) ;
#15974=CARTESIAN_POINT ( 'NONE',  ( 0.3632570605522777996, -1.760200006483175095, -0.5108946128509906925 ) ) ;
#15982=EDGE_CURVE ( 'NONE', #16583, #31364, #32994, .T. ) ;
#15983=CARTESIAN_POINT ( 'NONE',  ( 0.4186432780919984720, -1.612034538517055360, -0.6668481824684697745 ) ) ;
#16002=VECTOR ( 'NONE', #1780, 39.37007874015748143 ) ;
#16009=CARTESIAN_POINT ( 'NONE',  ( 0.4738546087217606062, -1.652018268363231845, -0.3975985852014427002 ) ) ;
#16010=CARTESIAN_POINT ( 'NONE',  ( 0.06504549419198706051, -1.972538361174909882, -0.3281045264835606989 ) ) ;
#16019=CIRCLE ( 'NONE', #28485, 0.009999999999999996739 ) ;
#16020=CARTESIAN_POINT ( 'NONE',  ( 0.1999999999999789724, -2.097675824466503691, -0.5196396315034578217 ) ) ;
#16023=CIRCLE ( 'NONE', #26538, 0.2200000000000000566 ) ;
#16024=CARTESIAN_POINT ( 'NONE',  ( 0.1581139529352034445, -1.989394613953671342, -0.6673518793402363203 ) ) ;
#16030=FACE_OUTER_BOUND ( 'NONE', #10290, .T. ) ;
#16040=AXIS2_PLACEMENT_3D ( 'NONE', #24961, #718, #6428 ) ;
#16042=ORIENTED_EDGE ( 'NONE', *, *, #40303, .T. ) ;
#16045=EDGE_CURVE ( 'NONE', #20255, #25087, #2151, .T. ) ;
#16051=DIRECTION ( 'NONE',  ( -0.9780874495037195082, 0.000000000000000000, 0.2081944790894049990 ) ) ;
#16053=VECTOR ( 'NONE', #26545, 39.37007874015748143 ) ;
#16060=ORIENTED_EDGE ( 'NONE', *, *, #10337, .F. ) ;
#16062=CARTESIAN_POINT ( 'NONE',  ( 0.4159916692016358830, -1.069406866067976081, -0.5155029497116575543 ) ) ;
#16068=EDGE_CURVE ( 'NONE', #17175, #26250, #8275, .T. ) ;
#16077=CIRCLE ( 'NONE', #4850, 0.1033070866141734129 ) ;
#16079=CARTESIAN_POINT ( 'NONE',  ( 0.3888255243409498019, -1.692620460247742598, -0.4086109642453172874 ) ) ;
#16097=EDGE_CURVE ( 'NONE', #17902, #36736, #2819, .T. ) ;
#16106=CIRCLE ( 'NONE', #21337, 0.2500000000000000000 ) ;
#16110=CARTESIAN_POINT ( 'NONE',  ( 0.6272581727275550190, -1.617152969708947063, -0.5103538732883908802 ) ) ;
#16119=CARTESIAN_POINT ( 'NONE',  ( 0.5918007220238434840, -1.591304679919291809, -0.5951766354897257694 ) ) ;
#16125=CARTESIAN_POINT ( 'NONE',  ( 0.4412967101137347248, -1.641228763480250485, -0.6201386750407782422 ) ) ;
#16127=DIRECTION ( 'NONE',  ( 0.8660512985181135770, 0.4999551463232370097, 0.000000000000000000 ) ) ;
#16132=CARTESIAN_POINT ( 'NONE',  ( 0.4449199297089959648, -1.104150615014060977, -0.4000593327082896389 ) ) ;
#16139=CIRCLE ( 'NONE', #35197, 0.03000000000000002318 ) ;
#16143=DIRECTION ( 'NONE',  ( -1.000000000000000000, -0.000000000000000000, -0.000000000000000000 ) ) ;
#16146=DIRECTION ( 'NONE',  ( 1.000000000000000000, 0.000000000000000000, 0.000000000000000000 ) ) ;
#16148=ORIENTED_EDGE ( 'NONE', *, *, #16068, .F. ) ;
#16151=EDGE_LOOP ( 'NONE', ( #48, #10410, #35620, #8752, #4895, #11491 ) ) ;
#16152=CARTESIAN_POINT ( 'NONE',  ( 0.6343156381093978391, -1.595758837318228318, -0.5875140676452393906 ) ) ;
#16174=CARTESIAN_POINT ( 'NONE',  ( 0.4220651889022443704, -1.705682529110253753, -0.5196166052937188917 ) ) ;
#16184=AXIS2_PLACEMENT_3D ( 'NONE', #14987, #14787, #11698 ) ;
#16192=CARTESIAN_POINT ( 'NONE',  ( 0.3409152363046967782, -1.516880185093673061, -0.4991292961807996531 ) ) ;
#16193=CARTESIAN_POINT ( 'NONE',  ( 0.4219866632171927479, -1.610104465087647041, -0.3647299066799422618 ) ) ;
#16194=CARTESIAN_POINT ( 'NONE',  ( 0.5612334960093817715, -1.620627794947044897, -0.4868944820179722521 ) ) ;
#16203=CARTESIAN_POINT ( 'NONE',  ( 0.2011892967074958294, -1.251141541415955905, -0.7187326247832954706 ) ) ;
#16208=VERTEX_POINT ( 'NONE', #23294 ) ;
#16217=AXIS2_PLACEMENT_3D ( 'NONE', #14040, #10976, #26618 ) ;
#16224=DIRECTION ( 'NONE',  ( 0.4999551463232373427, -0.8660512985181134660, 0.000000000000000000 ) ) ;
#16225=FACE_OUTER_BOUND ( 'NONE', #40265, .T. ) ;
#16231=CARTESIAN_POINT ( 'NONE',  ( 0.3985951925633877124, -2.053915860785213265, -0.5118549077720337959 ) ) ;
#16249=CARTESIAN_POINT ( 'NONE',  ( 0.5403448000457758971, -1.667326427136834432, -0.4959994330086618941 ) ) ;
#16258=ORIENTED_EDGE ( 'NONE', *, *, #32624, .T. ) ;
#16264=CARTESIAN_POINT ( 'NONE',  ( 0.02988687873307911344, -2.020173214415363461, -0.2839403628030972571 ) ) ;
#16273=B_SPLINE_CURVE_WITH_KNOTS ( 'NONE', 3,
 ( #27794, #30681, #40538, #28002, #34153, #15846, #12360, #2497 ),
 .UNSPECIFIED., .F., .F.,
 ( 4, 2, 2, 4 ),
 ( 1.734723475976807094E-18, 0.0005953189690397796881, 0.0008929784535596708333, 0.001190637938079561978 ),
 .UNSPECIFIED. ) ;
#16284=CARTESIAN_POINT ( 'NONE',  ( 0.1877114757398583578, -1.688462026347908873, -0.6542463691362495615 ) ) ;
#16288=CARTESIAN_POINT ( 'NONE',  ( 0.2156332787663666484, -1.620970839068891944, -0.6635100984292762183 ) ) ;
#16298=CARTESIAN_POINT ( 'NONE',  ( 0.5213789366507165512, -1.637636803980936362, -0.4211300373884619974 ) ) ;
#16309=FACE_OUTER_BOUND ( 'NONE', #11544, .T. ) ;
#16315=CARTESIAN_POINT ( 'NONE',  ( 0.6272266378578528201, -1.617171174196860628, -0.5046292136067113132 ) ) ;
#16325=CARTESIAN_POINT ( 'NONE',  ( 0.4659739283829816836, -1.067701485818283835, -0.6091934467387866148 ) ) ;
#16340=ORIENTED_EDGE ( 'NONE', *, *, #22571, .T. ) ;
#16355=CARTESIAN_POINT ( 'NONE',  ( 0.5209049548566241361, -1.602498953031318729, -0.4230150025751962528 ) ) ;
#16360=CARTESIAN_POINT ( 'NONE',  ( 0.6364841839958734759, -1.591084691710345389, -0.5918496660566199274 ) ) ;
#16361=CARTESIAN_POINT ( 'NONE',  ( 0.2325020897479753157, -1.594945628236600133, -0.3239020423276253724 ) ) ;
#16375=CARTESIAN_POINT ( 'NONE',  ( 0.3595715536228104581, -1.625401886829162867, -0.3696110269036071982 ) ) ;
#16382=CARTESIAN_POINT ( 'NONE',  ( 0.4569551544390156317, -1.119309369577474955, -0.6070915220724588668 ) ) ;
#16395=CARTESIAN_POINT ( 'NONE',  ( 0.1995529058109158649, -2.050896138459939344, -0.3054326997595754878 ) ) ;
#16407=CARTESIAN_POINT ( 'NONE',  ( 0.03333333333331311293, -1.846784381541715314, -0.3501698912633309790 ) ) ;
#16408=CARTESIAN_POINT ( 'NONE',  ( 0.3893341572580266141, -1.754502034563850454, -0.5437939363053549968 ) ) ;
#16415=CARTESIAN_POINT ( 'NONE',  ( 0.3699999999999786793, -2.097675824466503691, -0.5196396315034578217 ) ) ;
#16416=B_SPLINE_CURVE_WITH_KNOTS ( 'NONE', 3,
 ( #23312, #33153, #17110, #7220 ),
 .UNSPECIFIED., .F., .F.,
 ( 4, 4 ),
 ( 0.000000000000000000, 0.001650735412551658380 ),
 .UNSPECIFIED. ) ;
#16422=CARTESIAN_POINT ( 'NONE',  ( 0.6134394428779069708, -1.489641535132577577, -0.4161639220292565611 ) ) ;
#16428=EDGE_CURVE ( 'NONE', #9403, #28175, #36282, .T. ) ;
#16432=CARTESIAN_POINT ( 'NONE',  ( 0.3593346688482154661, -1.735925422213635549, -0.5010936962835144115 ) ) ;
#16436=ORIENTED_EDGE ( 'NONE', *, *, #15423, .T. ) ;
#16439=CARTESIAN_POINT ( 'NONE',  ( 0.2629665421248923995, -1.157745397434066126, -0.5155029497116575543 ) ) ;
#16441=EDGE_LOOP ( 'NONE', ( #18409, #30951, #6756 ) ) ;
#16444=CARTESIAN_POINT ( 'NONE',  ( 0.5457083359927942245, -1.652683498676156271, -0.4845597240607255607 ) ) ;
#16447=CARTESIAN_POINT ( 'NONE',  ( 0.3957364756389608607, -1.753984992610886584, -0.5139882692845931800 ) ) ;
#16450=CARTESIAN_POINT ( 'NONE',  ( 0.09094713279931705696, -1.440988727485061682, -0.3374321700806039992 ) ) ;
#16452=ORIENTED_EDGE ( 'NONE', *, *, #26985, .T. ) ;
#16469=CIRCLE ( 'NONE', #1393, 0.2500000000000000555 ) ;
#16472=CARTESIAN_POINT ( 'NONE',  ( 0.1748174088606663235, -1.825896565190340048, -0.6523992043106852101 ) ) ;
#16475=CARTESIAN_POINT ( 'NONE',  ( 0.2738670336145942463, -1.555218499503542295, -0.6850478759345199897 ) ) ;
#16480=CARTESIAN_POINT ( 'NONE',  ( 0.4741640079579751421, -1.162838329081267830, -0.4122610257295771796 ) ) ;
#16486=ORIENTED_EDGE ( 'NONE', *, *, #14806, .F. ) ;
#16488=EDGE_CURVE ( 'NONE', #21610, #3320, #13143, .T. ) ;
#16490=ORIENTED_EDGE ( 'NONE', *, *, #3161, .F. ) ;
#16494=EDGE_CURVE ( 'NONE', #7054, #2060, #7379, .T. ) ;
#16498=EDGE_CURVE ( 'NONE', #3488, #5149, #26012, .T. ) ;
#16500=CARTESIAN_POINT ( 'NONE',  ( 0.3638878398920847301, -1.759885569913659964, -0.5002684421424647976 ) ) ;
#16503=CARTESIAN_POINT ( 'NONE',  ( 0.6511295279640838540, -1.603372484741562243, -0.5770581850489380216 ) ) ;
#16508=B_SPLINE_CURVE_WITH_KNOTS ( 'NONE', 3,
 ( #4324, #29623, #1675, #32106 ),
 .UNSPECIFIED., .F., .F.,
 ( 4, 4 ),
 ( -6.000000000870814185E-08, 0.001836379686786120558 ),
 .UNSPECIFIED. ) ;
#16510=CARTESIAN_POINT ( 'NONE',  ( 0.4399767927377957188, -1.641420014575965203, -0.3416704067942654133 ) ) ;
#16512=CARTESIAN_POINT ( 'NONE',  ( 0.5455881031540377180, -1.595019605959082654, -0.5473203437262895710 ) ) ;
#16515=EDGE_CURVE ( 'NONE', #23751, #30709, #40247, .T. ) ;
#16518=CARTESIAN_POINT ( 'NONE',  ( 0.4480646913441768131, -1.099213350020603164, -0.6275147848854655264 ) ) ;
#16533=ORIENTED_EDGE ( 'NONE', *, *, #2377, .F. ) ;
#16535=B_SPLINE_CURVE_WITH_KNOTS ( 'NONE', 3,
 ( #7499, #14089, #26663, #23577 ),
 .UNSPECIFIED., .F., .F.,
 ( 4, 4 ),
 ( 0.001814668777126959539, 0.002327282627751500917 ),
 .UNSPECIFIED. ) ;
#16541=CARTESIAN_POINT ( 'NONE',  ( 0.3620662970392556912, -1.757402016409378875, -0.5213949640471970959 ) ) ;
#16545=VERTEX_POINT ( 'NONE', #20157 ) ;
#16551=CARTESIAN_POINT ( 'NONE',  ( 0.4829750487733310838, -1.628965326960139848, -0.4293328069181645001 ) ) ;
#16556=CARTESIAN_POINT ( 'NONE',  ( 0.4584717390208090659, -1.703043547193806573, -0.5155029497116575543 ) ) ;
#16557=CARTESIAN_POINT ( 'NONE',  ( 0.4380378120020821942, -1.691746349159306773, -0.5029009121720273701 ) ) ;
#16560=FACE_OUTER_BOUND ( 'NONE', #24719, .T. ) ;
#16562=CIRCLE ( 'NONE', #27082, 0.02999999999999996420 ) ;
#16565=EDGE_CURVE ( 'NONE', #6307, #15639, #38931, .T. ) ;
#16568=EDGE_CURVE ( 'NONE', #34456, #33739, #30867, .T. ) ;
#16572=CARTESIAN_POINT ( 'NONE',  ( 0.4949988758262525157, -1.646761950602083191, -0.6271208291453260752 ) ) ;
#16574=LINE ( 'NONE', #32005, #15296 ) ;
#16575=CARTESIAN_POINT ( 'NONE',  ( 0.1834925190845456133, -1.244183424859474307, -0.6222488774890111429 ) ) ;
#16579=CIRCLE ( 'NONE', #21853, 0.1700000000000000400 ) ;
#16583=VERTEX_POINT ( 'NONE', #13570 ) ;
#16586=CIRCLE ( 'NONE', #6058, 0.1033070866141732880 ) ;
#16589=CARTESIAN_POINT ( 'NONE',  ( -2.112273405726188513E-14, -2.183180860297921466, -0.2737760292030870235 ) ) ;
#16593=FACE_OUTER_BOUND ( 'NONE', #28315, .T. ) ;
#16596=ORIENTED_EDGE ( 'NONE', *, *, #28518, .F. ) ;
#16608=CARTESIAN_POINT ( 'NONE',  ( 0.08083978255789368850, -1.392018123601084456, -0.3662540681622217242 ) ) ;
#16609=CARTESIAN_POINT ( 'NONE',  ( 0.3409152363046956680, -1.516880185093671951, -0.7462941026102620778 ) ) ;
#16613=CARTESIAN_POINT ( 'NONE',  ( 0.3760351885562613350, -1.762179279381401731, -0.5696997652324998773 ) ) ;
#16614=B_SPLINE_CURVE_WITH_KNOTS ( 'NONE', 3,
 ( #674, #38261, #22061, #34583 ),
 .UNSPECIFIED., .F., .F.,
 ( 4, 4 ),
 ( -6.000000000230091993E-08, 0.001780663706559377666 ),
 .UNSPECIFIED. ) ;
#16617=CARTESIAN_POINT ( 'NONE',  ( 0.3871590699894606469, -1.829451072714431525, -0.6982937763513055174 ) ) ;
#16620=CARTESIAN_POINT ( 'NONE',  ( 0.1943567346968996801, -1.255085851118643125, -0.7153666112938226185 ) ) ;
#16623=ADVANCED_FACE ( 'NONE', ( #23461 ), #35562, .T. ) ;
#16624=CARTESIAN_POINT ( 'NONE',  ( 0.6637426744281501589, -1.463151821187066437, -0.6174834252971218573 ) ) ;
#16633=CARTESIAN_POINT ( 'NONE',  ( 0.4209912206648682154, -1.078067379053157193, -0.5155029497116575543 ) ) ;
#16647=CARTESIAN_POINT ( 'NONE',  ( 0.3466435857699784462, -1.701529685981289175, -0.5540514338380616577 ) ) ;
#16654=CARTESIAN_POINT ( 'NONE',  ( 0.5348150208694708585, -1.670518664781361240, -0.4558810860387588759 ) ) ;
#16655=CARTESIAN_POINT ( 'NONE',  ( 0.1734973056165642902, -1.209394307038482719, -0.5155029497116575543 ) ) ;
#16657=CARTESIAN_POINT ( 'NONE',  ( 0.0005464815904230041358, -1.956929671832038808, -0.3304605512727917804 ) ) ;
#16659=LINE ( 'NONE', #32481, #31650 ) ;
#16666=CARTESIAN_POINT ( 'NONE',  ( 0.4867251962510119045, -1.680960026995096612, -0.6125153944539966089 ) ) ;
#16674=ADVANCED_FACE ( 'NONE', ( #23036 ), #15300, .F. ) ;
#16676=DIRECTION ( 'NONE',  ( 0.2637677594038911888, 0.000000000000000000, -0.9645862165193171966 ) ) ;
#16677=CARTESIAN_POINT ( 'NONE',  ( 0.2262803116713057172, -1.604565100197093308, -0.6672799576086320128 ) ) ;
#16681=CARTESIAN_POINT ( 'NONE',  ( 0.3613318213999966999, -1.782164263199393694, -0.6704317764855626249 ) ) ;
#16685=EDGE_CURVE ( 'NONE', #24957, #24018, #34790, .T. ) ;
#16688=ORIENTED_EDGE ( 'NONE', *, *, #3438, .T. ) ;
#16695=ORIENTED_EDGE ( 'NONE', *, *, #11938, .F. ) ;
#16714=EDGE_LOOP ( 'NONE', ( #17508, #32775, #9701, #31930 ) ) ;
#16716=CYLINDRICAL_SURFACE ( 'NONE', #10650, 0.1033070866141732880 ) ;
#16719=DIRECTION ( 'NONE',  ( 1.000000000000000000, 0.000000000000000000, 0.000000000000000000 ) ) ;
#16728=CARTESIAN_POINT ( 'NONE',  ( 0.4634865284762402782, -1.134362257022321518, -0.3648515278348755109 ) ) ;
#16732=EDGE_CURVE ( 'NONE', #1802, #25148, #12673, .T. ) ;
#16741=ORIENTED_EDGE ( 'NONE', *, *, #37649, .F. ) ;
#16746=ORIENTED_EDGE ( 'NONE', *, *, #36869, .T. ) ;
#16747=CARTESIAN_POINT ( 'NONE',  ( 0.5432023227565030421, -1.654074096829117879, -0.4765337786301755418 ) ) ;
#16751=ORIENTED_EDGE ( 'NONE', *, *, #7469, .F. ) ;
#16754=CARTESIAN_POINT ( 'NONE',  ( 0.3569144835062229015, -1.786313658517578951, -0.4887759019995990273 ) ) ;
#16766=ORIENTED_EDGE ( 'NONE', *, *, #10133, .F. ) ;
#16776=CIRCLE ( 'NONE', #39760, 0.01499999999999999251 ) ;
#16780=CARTESIAN_POINT ( 'NONE',  ( 0.4019978477689601370, -1.758738184043603603, -0.4821875037442184819 ) ) ;
#16783=B_SPLINE_CURVE_WITH_KNOTS ( 'NONE', 3,
 ( #21163, #40061, #9020, #34103 ),
 .UNSPECIFIED., .F., .F.,
 ( 4, 4 ),
 ( 0.000000000000000000, 0.005247268741964242027 ),
 .UNSPECIFIED. ) ;
#16795=CARTESIAN_POINT ( 'NONE',  ( 0.3641524999503367721, -1.715784215955702852, -0.4585743496845985923 ) ) ;
#16803=CARTESIAN_POINT ( 'NONE',  ( -2.112273405726188513E-14, -2.097675824466503691, -0.2907077406111384099 ) ) ;
#16809=CARTESIAN_POINT ( 'NONE',  ( 0.5714440434361192089, -1.545267987928362841, -0.5204514232545197627 ) ) ;
#16812=CIRCLE ( 'NONE', #3679, 0.01000000000000001756 ) ;
#16820=ORIENTED_EDGE ( 'NONE', *, *, #29825, .F. ) ;
#16824=CARTESIAN_POINT ( 'NONE',  ( 0.4946724348411004057, -1.646204522746663956, -0.4040971505047686874 ) ) ;
#16839=CARTESIAN_POINT ( 'NONE',  ( 0.6427025470096586757, -1.447461895507986762, -0.6319542925746485240 ) ) ;
#16842=EDGE_CURVE ( 'NONE', #30237, #2983, #28368, .T. ) ;
#16847=CARTESIAN_POINT ( 'NONE',  ( 0.5716576001687232456, -1.545079331453066418, -0.5060932645805602537 ) ) ;
#16848=CARTESIAN_POINT ( 'NONE',  ( 0.4219866632171688225, -1.610104465087698777, -0.3647299066799567502 ) ) ;
#16852=VERTEX_POINT ( 'NONE', #29700 ) ;
#16853=CARTESIAN_POINT ( 'NONE',  ( 0.3666228249977095399, -1.767104007576765001, -0.5848508674883445835 ) ) ;
#16869=CARTESIAN_POINT ( 'NONE',  ( 0.3623580354614820420, -1.967894635670391912, -0.4765942900942761740 ) ) ;
#16870=CARTESIAN_POINT ( 'NONE',  ( 0.08756027987733720763, -1.379929391113575043, -0.3337043114794515097 ) ) ;
#16882=CARTESIAN_POINT ( 'NONE',  ( 0.4480646913441768131, -1.099213350020603164, -0.6275147848854655264 ) ) ;
#16891=CARTESIAN_POINT ( 'NONE',  ( 0.3994067150627959029, -1.748687336150827276, -0.5749207012357768765 ) ) ;
#16894=ORIENTED_EDGE ( 'NONE', *, *, #33510, .T. ) ;
#16899=CARTESIAN_POINT ( 'NONE',  ( 0.5128132487356600322, -1.640511253658597957, -0.4146624397426829089 ) ) ;
#16903=ORIENTED_EDGE ( 'NONE', *, *, #14485, .T. ) ;
#16904=VERTEX_POINT ( 'NONE', #1544 ) ;
#16906=VERTEX_POINT ( 'NONE', #11182 ) ;
#16910=LINE ( 'NONE', #38292, #22477 ) ;
#16912=ORIENTED_EDGE ( 'NONE', *, *, #11441, .F. ) ;
#16918=FACE_OUTER_BOUND ( 'NONE', #10060, .T. ) ;
#16921=CARTESIAN_POINT ( 'NONE',  ( 0.4387252196728761433, -1.612896326537896829, -0.6609064949533233202 ) ) ;
#16922=CARTESIAN_POINT ( 'NONE',  ( 0.5085763096842138564, -1.618730835354739828, -0.5737883394389590164 ) ) ;
#16927=CARTESIAN_POINT ( 'NONE',  ( 0.4189043378923988925, -1.737431724743732753, -0.5872665585884508932 ) ) ;
#16937=( BOUNDED_SURFACE ( )  B_SPLINE_SURFACE ( 3, 2, ( 
 ( #20277, #38367, #32607 ),
 ( #26444, #29721, #7899 ),
 ( #23166, #32395, #10396 ),
 ( #1565, #33001, #29942 ),
 ( #7710, #22959, #4008 ),
 ( #39197, #13678, #10206 ),
 ( #1358, #4420, #32799 ),
 ( #26240, #32194, #7283 ),
 ( #22773, #35902, #35296 ),
 ( #16572, #38980, #16979 ),
 ( #4808, #10812, #977 ),
 ( #13492, #26057, #38577 ) ),
 .UNSPECIFIED., .F., .F., .F. ) 
 B_SPLINE_SURFACE_WITH_KNOTS ( ( 4, 2, 2, 2, 2, 4 ),
 ( 3, 3 ),
 ( 0.000000000000000000, 0.0009043136984160567724, 0.001356470547624085213, 0.001808627396832113545, 0.002712941095248170426, 0.003617254793664227090 ),
 ( 0.000000000000000000, 1.000000000000000000 ),
 .UNSPECIFIED. ) 
 GEOMETRIC_REPRESENTATION_ITEM ( )  RATIONAL_B_SPLINE_SURFACE ( (
 ( 1.000000000000000000, 0.7071067811865457964, 1.000000000000000000),
 ( 1.000000000000000000, 0.7141572841065146893, 1.000000000000000000),
 ( 1.000000000000000000, 0.7219308286147578801, 1.000000000000000000),
 ( 1.000000000000000000, 0.7336727792982185026, 1.000000000000000000),
 ( 1.000000000000000000, 0.7376634957069627685, 1.000000000000000000),
 ( 1.000000000000000000, 0.7456484326271539675, 1.000000000000000000),
 ( 1.000000000000000000, 0.7496697957975114734, 1.000000000000000000),
 ( 1.000000000000000000, 0.7619968371056987655, 1.000000000000000000),
 ( 1.000000000000000000, 0.7706756004923445147, 1.000000000000000000),
 ( 1.000000000000000000, 0.7883272815239725784, 1.000000000000000000),
 ( 1.000000000000000000, 0.7974260126898345957, 1.000000000000000000),
 ( 1.000000000000000000, 0.8067368806807374559, 1.000000000000000000) ) ) 
 REPRESENTATION_ITEM ( '' )  SURFACE ( )  );
#16939=CARTESIAN_POINT ( 'NONE',  ( 0.02559308416905495959, -1.400621020312459830, -0.6538911019815975001 ) ) ;
#16945=ORIENTED_EDGE ( 'NONE', *, *, #5045, .T. ) ;
#16950=CARTESIAN_POINT ( 'NONE',  ( 0.3624061103390756600, -1.968824918581865591, -0.4968426515054816806 ) ) ;
#16955=EDGE_CURVE ( 'NONE', #23240, #13700, #38863, .T. ) ;
#16957=EDGE_CURVE ( 'NONE', #29368, #28841, #21033, .T. ) ;
#16963=ORIENTED_EDGE ( 'NONE', *, *, #28518, .T. ) ;
#16964=EDGE_CURVE ( 'NONE', #556, #7698, #11362, .T. ) ;
#16979=CARTESIAN_POINT ( 'NONE',  ( 0.4958723899955516101, -1.679082390730774144, -0.6092321650988190562 ) ) ;
#16986=VERTEX_POINT ( 'NONE', #4515 ) ;
#16993=CARTESIAN_POINT ( 'NONE',  ( 0.6335899703865320864, -1.596177751663357736, -0.4443638777805991591 ) ) ;
#16994=CARTESIAN_POINT ( 'NONE',  ( 0.4619737557705557163, -1.656318618979952584, -0.6360981484938359465 ) ) ;
#16995=CARTESIAN_POINT ( 'NONE',  ( 0.2161879510971927709, -1.277123080371499020, -0.7187326247832955817 ) ) ;
#16998=CARTESIAN_POINT ( 'NONE',  ( 0.3597996879153266270, -1.933544513296585166, -0.4937070853543361060 ) ) ;
#16999=CARTESIAN_POINT ( 'NONE',  ( 0.5840964882222685617, -1.491811162635231058, -0.4356935235874836998 ) ) ;
#17001=DIRECTION ( 'NONE',  ( -1.000000000000000000, 0.000000000000000000, 0.000000000000000000 ) ) ;
#17002=ORIENTED_EDGE ( 'NONE', *, *, #721, .F. ) ;
#17004=ORIENTED_EDGE ( 'NONE', *, *, #2221, .F. ) ;
#17007=CARTESIAN_POINT ( 'NONE',  ( 0.4460751111563584503, -1.103507073082631074, -0.6308736239710884819 ) ) ;
#17011=ORIENTED_EDGE ( 'NONE', *, *, #4199, .T. ) ;
#17017=DIRECTION ( 'NONE',  ( -0.4999551463232377313, 0.8660512985181132439, -0.000000000000000000 ) ) ;
#17025=CARTESIAN_POINT ( 'NONE',  ( 0.1734973056165642902, -1.209394307038482719, -0.5155029497116575543 ) ) ;
#17038=CARTESIAN_POINT ( 'NONE',  ( 0.5777123731605773305, -1.533644566602507142, -0.4683381307628363688 ) ) ;
#17042=ORIENTED_EDGE ( 'NONE', *, *, #32785, .F. ) ;
#17059=CARTESIAN_POINT ( 'NONE',  ( 0.1190035864140202432, -1.325422344506462125, -0.3481589277964427520 ) ) ;
#17061=CARTESIAN_POINT ( 'NONE',  ( 0.4844396616870721428, -1.590460616370065194, -0.5829707516598297001 ) ) ;
#17062=CARTESIAN_POINT ( 'NONE',  ( 0.07931082089408725277, -1.397336969168096577, -0.6634856036505109023 ) ) ;
#17063=CYLINDRICAL_SURFACE ( 'NONE', #20737, 0.1033070866141732880 ) ;
#17070=DIRECTION ( 'NONE',  ( 1.000000000000000000, 0.000000000000000000, 0.000000000000000000 ) ) ;
#17077=CARTESIAN_POINT ( 'NONE',  ( 0.2161879510971928264, -1.277123080371499020, -0.3144976166544468099 ) ) ;
#17083=VERTEX_POINT ( 'NONE', #35398 ) ;
#17084=VERTEX_POINT ( 'NONE', #38874 ) ;
#17088=CARTESIAN_POINT ( 'NONE',  ( 0.5347516980328250735, -1.174037678574211263, -0.6056023639864149821 ) ) ;
#17110=CARTESIAN_POINT ( 'NONE',  ( 0.3300460303897821968, -1.638469719739709118, -0.3391576931604809997 ) ) ;
#17122=CARTESIAN_POINT ( 'NONE',  ( 0.4909801108973092520, -1.199306193601649362, -0.5155029497116575543 ) ) ;
#17128=EDGE_CURVE ( 'NONE', #37277, #30555, #9385, .T. ) ;
#17140=ORIENTED_EDGE ( 'NONE', *, *, #13262, .F. ) ;
#17142=CARTESIAN_POINT ( 'NONE',  ( 0.01265409468558189275, -1.700310348714810349, -0.6650692675765490502 ) ) ;
#17143=AXIS2_PLACEMENT_3D ( 'NONE', #22636, #26128, #32253 ) ;
#17146=AXIS2_PLACEMENT_3D ( 'NONE', #17242, #38079, #6402 ) ;
#17151=DIRECTION ( 'NONE',  ( 0.8660512985181132439, 0.4999551463232376758, 0.000000000000000000 ) ) ;
#17158=EDGE_LOOP ( 'NONE', ( #35969, #37037, #28642, #39867 ) ) ;
#17165=B_SPLINE_CURVE_WITH_KNOTS ( 'NONE', 3,
 ( #37465, #17939, #9283, #21863, #28218, #33561, #24147, #18970, #6805, #22682 ),
 .UNSPECIFIED., .F., .F.,
 ( 4, 2, 2, 2, 4 ),
 ( 0.000000000000000000, 0.0003219901686702020174, 0.0006439803373404040347, 0.0009659705060106060521, 0.001287960674680808069 ),
 .UNSPECIFIED. ) ;
#17173=CARTESIAN_POINT ( 'NONE',  ( 0.02988725412889516389, -2.019627616784832380, -0.2840895204354123571 ) ) ;
#17175=VERTEX_POINT ( 'NONE', #36002 ) ;
#17180=EDGE_CURVE ( 'NONE', #25706, #15019, #26863, .T. ) ;
#17181=VERTEX_POINT ( 'NONE', #19575 ) ;
#17182=LINE ( 'NONE', #5230, #22693 ) ;
#17184=ADVANCED_FACE ( 'NONE', ( #39291 ), #37645, .T. ) ;
#17191=CARTESIAN_POINT ( 'NONE',  ( 0.3712555767072253654, -1.761044764944616814, -0.4317137529336340096 ) ) ;
#17197=CARTESIAN_POINT ( 'NONE',  ( 0.5772941663360542375, -1.534806448867990003, -0.4703100941054121353 ) ) ;
#17201=AXIS2_PLACEMENT_3D ( 'NONE', #9100, #21666, #4737 ) ;
#17208=PLANE ( 'NONE',  #23115 ) ;
#17217=CARTESIAN_POINT ( 'NONE',  ( 0.3818164125050786950, -1.758841887392954995, -0.4494967532450438452 ) ) ;
#17219=CARTESIAN_POINT ( 'NONE',  ( 0.3991883495211515087, -1.748813394476138372, -0.5227867695449579521 ) ) ;
#17224=CARTESIAN_POINT ( 'NONE',  ( 0.5982289360768325848, -1.580768761966706348, -0.6063568540101081927 ) ) ;
#17225=CARTESIAN_POINT ( 'NONE',  ( 0.4768848212686895849, -1.682051206446435243, -0.4156371400837835517 ) ) ;
#17233=CARTESIAN_POINT ( 'NONE',  ( 0.5872508345537166274, -1.538326194691165050, -0.6180035471177106610 ) ) ;
#17242=CARTESIAN_POINT ( 'NONE',  ( 0.4763501221259694440, -1.554011115824661893, -0.5166151207188711680 ) ) ;
#17260=CYLINDRICAL_SURFACE ( 'NONE', #826, 0.1033070866141734129 ) ;
#17268=CARTESIAN_POINT ( 'NONE',  ( 0.1617959581636433664, -1.277479963088032244, -0.3330842537329358199 ) ) ;
#17274=AXIS2_PLACEMENT_3D ( 'NONE', #38017, #32228, #35138 ) ;
#17275=DIRECTION ( 'NONE',  ( -1.000000000000000000, 0.000000000000000000, 0.000000000000000000 ) ) ;
#17276=CARTESIAN_POINT ( 'NONE',  ( 0.2196639771989866430, -1.182743154750227843, -0.5155029497116575543 ) ) ;
#17278=CARTESIAN_POINT ( 'NONE',  ( 0.1837824601350801224, -1.244685677561853554, -0.4092841885321224504 ) ) ;
#17283=CIRCLE ( 'NONE', #14634, 0.2500000000000000000 ) ;
#17298=VERTEX_POINT ( 'NONE', #5974 ) ;
#17304=CARTESIAN_POINT ( 'NONE',  ( 0.4497590084914004360, -1.610781099968991992, -0.3722728953286537634 ) ) ;
#17305=CARTESIAN_POINT ( 'NONE',  ( 0.6303272460286932777, -1.599106815577767904, -0.4488814048484467967 ) ) ;
#17310=ADVANCED_FACE ( 'NONE', ( #9877 ), #31073, .T. ) ;
#17312=DIRECTION ( 'NONE',  ( 0.4999551463232373427, -0.8660512985181134660, 0.000000000000000000 ) ) ;
#17320=CARTESIAN_POINT ( 'NONE',  ( 0.4084093395596710141, -1.687879686225770781, -0.4185105672228304208 ) ) ;
#17337=EDGE_CURVE ( 'NONE', #39958, #35001, #19182, .T. ) ;
#17340=CARTESIAN_POINT ( 'NONE',  ( 0.3424206644552083567, -1.681860750042348807, -0.5668114887320723216 ) ) ;
#17349=ORIENTED_EDGE ( 'NONE', *, *, #7196, .T. ) ;
#17351=CARTESIAN_POINT ( 'NONE',  ( 0.0005182934561807130700, -1.951317934876418914, -0.6895229178506784296 ) ) ;
#17352=VECTOR ( 'NONE', #30553, 39.37007874015748143 ) ;
#17378=CARTESIAN_POINT ( 'NONE',  ( 0.4058326211045913401, -1.732063036044662274, -0.4894232243292900852 ) ) ;
#17389=ORIENTED_EDGE ( 'NONE', *, *, #40139, .T. ) ;
#17409=CARTESIAN_POINT ( 'NONE',  ( 0.4159916692016358830, -1.069406866067976081, -0.5155029497116575543 ) ) ;
#17417=DIRECTION ( 'NONE',  ( -0.4999551463232373427, 0.8660512985181134660, -0.000000000000000000 ) ) ;
#17420=ORIENTED_EDGE ( 'NONE', *, *, #3161, .T. ) ;
#17427=CARTESIAN_POINT ( 'NONE',  ( 0.4003286058064897679, -1.748155145941718169, -0.5147095092643340086 ) ) ;
#17433=CARTESIAN_POINT ( 'NONE',  ( 0.6010916754805513129, -1.596410883951256965, -0.5227362160200681451 ) ) ;
#17443=CARTESIAN_POINT ( 'NONE',  ( 0.6050257157783865969, -1.526910860915171364, -0.5980336084688177012 ) ) ;
#17447=B_SPLINE_CURVE_WITH_KNOTS ( 'NONE', 3,
 ( #3547, #16500, #13618, #32136 ),
 .UNSPECIFIED., .F., .F.,
 ( 4, 4 ),
 ( 1.081944681729554441E-16, 0.0007979876146421405712 ),
 .UNSPECIFIED. ) ;
#17448=AXIS2_PLACEMENT_3D ( 'NONE', #21643, #30884, #34166 ) ;
#17450=ORIENTED_EDGE ( 'NONE', *, *, #32637, .T. ) ;
#17452=CARTESIAN_POINT ( 'NONE',  ( 0.3644961020528623141, -1.765334207956099632, -0.5888949161622180073 ) ) ;
#17453=VERTEX_POINT ( 'NONE', #7800 ) ;
#17475=PRODUCT_DEFINITION_FORMATION_WITH_SPECIFIED_SOURCE ( 'ANY', '', #35397, .NOT_KNOWN. ) ;
#17477=ADVANCED_FACE ( 'NONE', ( #29617 ), #40183, .F. ) ;
#17478=CARTESIAN_POINT ( 'NONE',  ( 0.4159916692016358830, -1.069406866067976081, -0.5155029497116575543 ) ) ;
#17485=CARTESIAN_POINT ( 'NONE',  ( 0.2511799810870077310, -1.337738304023724512, -0.3144976166544468099 ) ) ;
#17503=FACE_OUTER_BOUND ( 'NONE', #7860, .T. ) ;
#17508=ORIENTED_EDGE ( 'NONE', *, *, #36044, .F. ) ;
#17514=CARTESIAN_POINT ( 'NONE',  ( 0.6348907386704650824, -1.612746832763798155, -0.4546890026736098434 ) ) ;
#17525=CARTESIAN_POINT ( 'NONE',  ( 0.1999999903896442222, -2.079563169082558893, -0.2654453414298869052 ) ) ;
#17530=ADVANCED_FACE ( 'NONE', ( #32494 ), #19851, .T. ) ;
#17531=CARTESIAN_POINT ( 'NONE',  ( 0.3568477411066238725, -1.622997595545246918, -0.6071924687824667988 ) ) ;
#17532=DIRECTION ( 'NONE',  ( 0.8660512985181142431, 0.4999551463232357884, 0.000000000000000000 ) ) ;
#17533=LINE ( 'NONE', #35844, #5479 ) ;
#17535=CARTESIAN_POINT ( 'NONE',  ( 0.3850224864643204126, -1.658839704013842065, -0.4046842732936995479 ) ) ;
#17548=CARTESIAN_POINT ( 'NONE',  ( 0.4069111126224479458, -1.648375263996657347, -0.6326914302627749676 ) ) ;
#17559=ORIENTED_EDGE ( 'NONE', *, *, #26108, .T. ) ;
#17561=CARTESIAN_POINT ( 'NONE',  ( 0.02678764122032725042, -1.589661793665505307, -0.6397169502282477049 ) ) ;
#17586=CARTESIAN_POINT ( 'NONE',  ( 0.3948342593773176423, -1.754451107475622162, -0.7138391223717516221 ) ) ;
#17590=CARTESIAN_POINT ( 'NONE',  ( 0.3699999999999786793, -2.097675824466503691, -0.5196396315034578217 ) ) ;
#17591=CARTESIAN_POINT ( 'NONE',  ( 0.1174979645898149572, -1.377733081079238753, -0.3274860884505732539 ) ) ;
#17599=FACE_OUTER_BOUND ( 'NONE', #16714, .T. ) ;
#17604=CARTESIAN_POINT ( 'NONE',  ( 0.3695052819757340123, -1.758428263776099287, -0.4278193900811940176 ) ) ;
#17605=CARTESIAN_POINT ( 'NONE',  ( 0.5129602329048122966, -1.030748725941331267, -0.5155029497116575543 ) ) ;
#17607=DIRECTION ( 'NONE',  ( 0.8660512985181135770, 0.4999551463232370652, -6.610988856618918076E-16 ) ) ;
#17610=ORIENTED_EDGE ( 'NONE', *, *, #8921, .T. ) ;
#17633=CARTESIAN_POINT ( 'NONE',  ( 0.6182805410152977243, -1.621742373187212261, -0.5380257021149844610 ) ) ;
#17635=CARTESIAN_POINT ( 'NONE',  ( 0.02999778723028691946, -2.087755359801442445, -0.2623954751430958021 ) ) ;
#17639=CARTESIAN_POINT ( 'NONE',  ( 0.5776621282381364519, -1.563796264554554227, -0.5899727365385690758 ) ) ;
#17640=CARTESIAN_POINT ( 'NONE',  ( 0.4192378292399245865, -1.648733790552149081, -0.6219568095148814146 ) ) ;
#17645=CARTESIAN_POINT ( 'NONE',  ( 0.3734578206545139389, -1.768187696252267571, -0.5721167227818628742 ) ) ;
#17647=CARTESIAN_POINT ( 'NONE',  ( 0.6194230288292433828, -1.535705225211028147, -0.4012506026892472821 ) ) ;
#17652=CARTESIAN_POINT ( 'NONE',  ( 0.01044944019094518409, -1.729937559987831275, -0.3655757404049914672 ) ) ;
#17654=CARTESIAN_POINT ( 'NONE',  ( 0.3590286451914425081, -1.755833398155118186, -0.5341343048503752744 ) ) ;
#17661=DIRECTION ( 'NONE',  ( -0.4999551463232373427, 0.8660512985181134660, -0.000000000000000000 ) ) ;
#17662=CARTESIAN_POINT ( 'NONE',  ( 0.3679555284477226129, -2.044013266926633765, -0.5096248211185702148 ) ) ;
#17665=CARTESIAN_POINT ( 'NONE',  ( 0.5450221724342032559, -1.653079607787938166, -0.5489131283297039587 ) ) ;
#17669=DIRECTION ( 'NONE',  ( 0.000000000000000000, 0.000000000000000000, -1.000000000000000000 ) ) ;
#17670=CARTESIAN_POINT ( 'NONE',  ( 0.02999999999997886302, -2.183180860297921466, -0.4937760292030871079 ) ) ;
#17675=CARTESIAN_POINT ( 'NONE',  ( 0.4362865664533659982, -1.115424303768361325, -0.3894947692426334873 ) ) ;
#17685=CARTESIAN_POINT ( 'NONE',  ( 0.4114935271033751674, -1.686083435099646977, -0.4173439381843800922 ) ) ;
#17691=EDGE_CURVE ( 'NONE', #13011, #38249, #25765, .T. ) ;
#17696=CARTESIAN_POINT ( 'NONE',  ( 0.4584717390208090659, -1.703043547193806573, -0.5155029497116575543 ) ) ;
#17714=CARTESIAN_POINT ( 'NONE',  ( 0.3360297777558891585, -1.646801663888270317, -0.6479318779998786137 ) ) ;
#17715=CARTESIAN_POINT ( 'NONE',  ( 0.1998231473750205767, -2.070638627232769480, -0.2997811547186691739 ) ) ;
#17717=FACE_OUTER_BOUND ( 'NONE', #35362, .T. ) ;
#17719=CARTESIAN_POINT ( 'NONE',  ( 0.6129340932688779331, -1.613573864442072292, -0.5426322817999900128 ) ) ;
#17726=CARTESIAN_POINT ( 'NONE',  ( 0.3745565332565439221, -1.612774642522065704, -0.6154719560940745682 ) ) ;
#17729=CARTESIAN_POINT ( 'NONE',  ( 0.02999999999976839596, -2.097673604718639062, -0.7286983764821324261 ) ) ;
#17735=CARTESIAN_POINT ( 'NONE',  ( 0.3717145517045183922, -1.760210800595612080, -0.4321619518649676972 ) ) ;
#17736=CARTESIAN_POINT ( 'NONE',  ( 0.3868278802867940458, -1.884152038337740143, -0.4995641518168190687 ) ) ;
#17737=EDGE_LOOP ( 'NONE', ( #23608, #16746 ) ) ;
#17742=ORIENTED_EDGE ( 'NONE', *, *, #5018, .T. ) ;
#17743=CARTESIAN_POINT ( 'NONE',  ( 0.003249118729953440199, -1.844392804249546103, -0.6741495493879861023 ) ) ;
#17751=CARTESIAN_POINT ( 'NONE',  ( 0.1734973056165641514, -1.209394307038482497, -0.5155029497116575543 ) ) ;
#17757=DIRECTION ( 'NONE',  ( -0.8062136690494358104, -0.4849338684320062542, 0.3389080451765882351 ) ) ;
#17768=CARTESIAN_POINT ( 'NONE',  ( 0.2285553773980233683, -1.596574492821664526, -0.6995327739724715999 ) ) ;
#17775=CARTESIAN_POINT ( 'NONE',  ( 0.4136942338497008320, -1.674605337725208143, -0.3991494578240276647 ) ) ;
#17784=DIRECTION ( 'NONE',  ( 0.000000000000000000, 0.000000000000000000, -1.000000000000000000 ) ) ;
#17788=DIRECTION ( 'NONE',  ( -0.8660512985181130219, -0.4999551463232380644, 0.000000000000000000 ) ) ;
#17790=ADVANCED_FACE ( 'NONE', ( #21788, #20273 ), #32793, .F. ) ;
#17797=ORIENTED_EDGE ( 'NONE', *, *, #19114, .T. ) ;
#17803=CARTESIAN_POINT ( 'NONE',  ( 0.4581930876178143541, -1.105887789949125510, -0.6551259416095572830 ) ) ;
#17809=CARTESIAN_POINT ( 'NONE',  ( 0.1837600765269550573, -1.884334881598526579, -0.3110488970864131453 ) ) ;
#17817=AXIS2_PLACEMENT_3D ( 'NONE', #24752, #37274, #9091 ) ;
#17818=LINE ( 'NONE', #13912, #11495 ) ;
#17825=CARTESIAN_POINT ( 'NONE',  ( 0.5857764079363468879, -1.600142216809019802, -0.5816357325289774893 ) ) ;
#17826=CARTESIAN_POINT ( 'NONE',  ( 0.02977875364827006072, -2.019445173720740616, -0.7044873537940673502 ) ) ;
#17831=CARTESIAN_POINT ( 'NONE',  ( 0.4102222551943826567, -1.708906198810314248, -0.6086602454107996607 ) ) ;
#17837=CARTESIAN_POINT ( 'NONE',  ( 0.4789169902643273247, -1.099522405089615962, -0.6159558956687188891 ) ) ;
#17845=FACE_OUTER_BOUND ( 'NONE', #31246, .T. ) ;
#17859=EDGE_LOOP ( 'NONE', ( #37581, #16486, #31418, #38949 ) ) ;
#17860=CARTESIAN_POINT ( 'NONE',  ( 0.4265829747943327699, -1.610301022689196060, -0.3658488903366757805 ) ) ;
#17863=CARTESIAN_POINT ( 'NONE',  ( 0.1758314180332314625, -1.266529637424046006, -0.3265915900978382247 ) ) ;
#17880=DIRECTION ( 'NONE',  ( -0.2067069058495574485, -0.1193280138680813535, -0.9710989033977958096 ) ) ;
#17882=ORIENTED_EDGE ( 'NONE', *, *, #2147, .F. ) ;
#17883=CARTESIAN_POINT ( 'NONE',  ( 0.3324871086615504012, -1.659137217475707304, -0.6399689536651966826 ) ) ;
#17892=CIRCLE ( 'NONE', #31707, 0.08830708661417341343 ) ;
#17897=CARTESIAN_POINT ( 'NONE',  ( 0.5462348416196848300, -1.594646255991501560, -0.4868944820179722521 ) ) ;
#17902=VERTEX_POINT ( 'NONE', #7704 ) ;
#17912=DIRECTION ( 'NONE',  ( 0.1611076279721909144, -0.2660824569950847041, 0.9503917393836255334 ) ) ;
#17914=CARTESIAN_POINT ( 'NONE',  ( 0.4131462650696018368, -1.740755752022009606, -0.5824989720263729076 ) ) ;
#17917=DIRECTION ( 'NONE',  ( 0.4999551463232373427, -0.8660512985181134660, 0.000000000000000000 ) ) ;
#17920=CARTESIAN_POINT ( 'NONE',  ( 0.3929308436716468234, -1.654878899976784501, -0.4107462969407084108 ) ) ;
#17932=CARTESIAN_POINT ( 'NONE',  ( 0.4043366342594306162, -1.595583149648728272, -0.6186662175067518810 ) ) ;
#17939=CARTESIAN_POINT ( 'NONE',  ( 0.4730652175054185782, -1.158518077264399260, -0.6186948529734398461 ) ) ;
#17943=CARTESIAN_POINT ( 'NONE',  ( 0.3778411022549617582, -1.761430872877596698, -0.4448008592944453499 ) ) ;
#17944=DIRECTION ( 'NONE',  ( 0.000000000000000000, 0.000000000000000000, -1.000000000000000000 ) ) ;
#17949=CARTESIAN_POINT ( 'NONE',  ( 0.06635375273718516209, -1.430634853383571770, -0.6831062175902198330 ) ) ;
#17950=CARTESIAN_POINT ( 'NONE',  ( 0.3580990748662325474, -1.735866295672110038, -0.5196385737601301180 ) ) ;
#17964=ORIENTED_EDGE ( 'NONE', *, *, #13267, .T. ) ;
#17968=EDGE_CURVE ( 'NONE', #38602, #39658, #29037, .T. ) ;
#17976=CARTESIAN_POINT ( 'NONE',  ( 0.1852394899523307770, -1.940955445487499098, -0.6926550664574201432 ) ) ;
#17977=EDGE_CURVE ( 'NONE', #15024, #8017, #1883, .T. ) ;
#17982=CIRCLE ( 'NONE', #35082, 0.05000000000000000971 ) ;
#17983=DIRECTION ( 'NONE',  ( 0.4999551463232372317, -0.8660512985181133550, 0.000000000000000000 ) ) ;
#17986=B_SPLINE_CURVE_WITH_KNOTS ( 'NONE', 3,
 ( #6896, #12465, #9172, #6079, #6295, #25227, #19058, #37976, #31595, #18867 ),
 .UNSPECIFIED., .F., .F.,
 ( 4, 2, 2, 2, 4 ),
 ( 0.007788013979030915246, 0.009512064120430865563, 0.01037408919113082945, 0.01080510172648081225, 0.01123611426183079333 ),
 .UNSPECIFIED. ) ;
#17990=CARTESIAN_POINT ( 'NONE',  ( 0.7303750569129517922, -1.407367292694915895, -0.5155029497116575543 ) ) ;
#18000=CARTESIAN_POINT ( 'NONE',  ( 0.3579113904514451550, -1.818604591836422868, -0.5224471374048138550 ) ) ;
#18009=CARTESIAN_POINT ( 'NONE',  ( 0.7471327741883029283, -1.536404953935046391, -0.5155029497116575543 ) ) ;
#18016=CARTESIAN_POINT ( 'NONE',  ( 0.4448603323116310793, -1.593566437326633833, -0.6098708555474791071 ) ) ;
#18017=CARTESIAN_POINT ( 'NONE',  ( 0.3902240973675495384, -1.938317844694748882, -0.2990241803344498850 ) ) ;
#18037=CARTESIAN_POINT ( 'NONE',  ( 0.6350421536969704794, -1.594263220348614007, -0.5890555079769790314 ) ) ;
#18040=CARTESIAN_POINT ( 'NONE',  ( 0.3940498717738633028, -1.740175311725885576, -0.4363121077653914215 ) ) ;
#18041=DIRECTION ( 'NONE',  ( 1.060606950627616773E-16, 6.122684696619993730E-17, 1.000000000000000000 ) ) ;
#18043=ORIENTED_EDGE ( 'NONE', *, *, #14478, .F. ) ;
#18053=ORIENTED_EDGE ( 'NONE', *, *, #15982, .F. ) ;
#18056=DIRECTION ( 'NONE',  ( 0.8660512985181124668, 0.4999551463232388415, 0.000000000000000000 ) ) ;
#18064=EDGE_LOOP ( 'NONE', ( #18945, #4522, #9292, #20991 ) ) ;
#18072=DIRECTION ( 'NONE',  ( 0.4999551463232372317, -0.8660512985181135770, 0.000000000000000000 ) ) ;
#18078=CARTESIAN_POINT ( 'NONE',  ( 0.2047952255614176320, -1.936887964834772102, -0.3318900947218276776 ) ) ;
#18081=CARTESIAN_POINT ( 'NONE',  ( 0.005374783099221854855, -1.803624522921790652, -0.3583957701598275980 ) ) ;
#18096=AXIS2_PLACEMENT_3D ( 'NONE', #8000, #29828, #27555 ) ;
#18102=ORIENTED_EDGE ( 'NONE', *, *, #15062, .T. ) ;
#18120=CARTESIAN_POINT ( 'NONE',  ( 0.2547684209294985291, -1.595179263533379910, -0.3507741123912141989 ) ) ;
#18134=CARTESIAN_POINT ( 'NONE',  ( 0.3324871086615415194, -1.659137217475705306, -0.6399689536651991251 ) ) ;
#18135=CARTESIAN_POINT ( 'NONE',  ( 0.1999999999999786671, -2.166079853131637645, -0.4467913981637915977 ) ) ;
#18138=CARTESIAN_POINT ( 'NONE',  ( 0.3999999999999787059, -2.166079853131637645, -0.4467913981637915422 ) ) ;
#18139=AXIS2_PLACEMENT_3D ( 'NONE', #29471, #1724, #10753 ) ;
#18159=CARTESIAN_POINT ( 'NONE',  ( 0.1817870711851117815, -1.296977422222274523, -0.7345968740143652420 ) ) ;
#18169=DIRECTION ( 'NONE',  ( 0.8660512985181130219, 0.4999551463232378978, 0.000000000000000000 ) ) ;
#18180=CARTESIAN_POINT ( 'NONE',  ( 0.3699999999999786793, -2.097675824466503691, -0.4685644896151254235 ) ) ;
#18190=CARTESIAN_POINT ( 'NONE',  ( 0.3697217270809275425, -2.079157444975821001, -0.5163575626078683589 ) ) ;
#18208=CARTESIAN_POINT ( 'NONE',  ( 0.1888132638007787578, -1.709137045139594857, -0.3586210806981278143 ) ) ;
#18224=CARTESIAN_POINT ( 'NONE',  ( 0.1262945646573275515, -1.315309522507558837, -0.3176315144292584103 ) ) ;
#18225=ORIENTED_EDGE ( 'NONE', *, *, #29900, .T. ) ;
#18228=CARTESIAN_POINT ( 'NONE',  ( 0.1818679406367339213, -1.742646577052884727, -0.3269862635956189978 ) ) ;
#18231=DIRECTION ( 'NONE',  ( 0.4999551463232373427, -0.8660512985181134660, 0.000000000000000000 ) ) ;
#18232=EDGE_CURVE ( 'NONE', #19186, #3583, #29264, .T. ) ;
#18236=CARTESIAN_POINT ( 'NONE',  ( 0.2059273467974226113, -1.283046334493782803, -0.3194715457588298557 ) ) ;
#18243=CARTESIAN_POINT ( 'NONE',  ( 0.6138443103785190536, -1.548954526385655672, -0.4055369609750524296 ) ) ;
#18244=CARTESIAN_POINT ( 'NONE',  ( 0.1354314573857386406, -1.346930980521078736, -0.7110692366758478711 ) ) ;
#18251=CARTESIAN_POINT ( 'NONE',  ( 0.5948637837280855711, -1.483193241468645507, -0.6457934574185902887 ) ) ;
#18253=CARTESIAN_POINT ( 'NONE',  ( 0.3699999999999786793, -2.097675824466503691, -0.4688691127277797022 ) ) ;
#18256=EDGE_CURVE ( 'NONE', #1239, #5197, #16508, .T. ) ;
#18257=CARTESIAN_POINT ( 'NONE',  ( 0.5014952879983503031, -1.689753520674470710, -0.5927250297527999479 ) ) ;
#18258=( BOUNDED_SURFACE ( )  B_SPLINE_SURFACE ( 3, 2, ( 
 ( #40282, #25480, #10247 ),
 ( #25893, #12930, #6939 ),
 ( #810, #19512, #38015 ),
 ( #16609, #26100, #4261 ) ),
 .UNSPECIFIED., .F., .F., .T. ) 
 B_SPLINE_SURFACE_WITH_KNOTS ( ( 4, 4 ),
 ( 3, 3 ),
 ( -3.816391647148975608E-16, 0.002151548051257935051 ),
 ( 0.000000000000000000, 0.7423884024711013829 ),
 .UNSPECIFIED. ) 
 GEOMETRIC_REPRESENTATION_ITEM ( )  RATIONAL_B_SPLINE_SURFACE ( (
 ( 1.000000000000000000, 0.7823248912590446968, 0.8878487349899315539),
 ( 1.000000000000000000, 0.7825950437676943983, 0.8879879238285908194),
 ( 1.000000000000000000, 0.7825604363545956010, 0.8879700932866414487),
 ( 1.000000000000000000, 0.7825594711904613199, 0.8879695960116924525) ) ) 
 REPRESENTATION_ITEM ( '' )  SURFACE ( )  );
#18271=CARTESIAN_POINT ( 'NONE',  ( 0.1720329558925851321, -1.269480774308429982, -0.3269759641248038973 ) ) ;
#18273=CARTESIAN_POINT ( 'NONE',  ( 0.3495654075459491694, -1.736963291591081759, -0.5687247700623858648 ) ) ;
#18276=DIRECTION ( 'NONE',  ( 0.8660512985181130219, 0.4999551463232378978, -4.627692199633250344E-15 ) ) ;
#18279=ORIENTED_EDGE ( 'NONE', *, *, #24850, .T. ) ;
#18284=FACE_OUTER_BOUND ( 'NONE', #19091, .T. ) ;
#18288=CARTESIAN_POINT ( 'NONE',  ( 0.05370873345334652160, -1.468804715554985707, -0.3745649705647907113 ) ) ;
#18289=EDGE_CURVE ( 'NONE', #26169, #10778, #27105, .T. ) ;
#18291=EDGE_CURVE ( 'NONE', #2983, #26971, #16586, .T. ) ;
#18301=CARTESIAN_POINT ( 'NONE',  ( 0.5705655853683049283, -1.576197229824741974, -0.5665877336259347308 ) ) ;
#18305=CARTESIAN_POINT ( 'NONE',  ( 0.1993697748527691604, -1.286830511351394923, -0.2901526353474664366 ) ) ;
#18306=ORIENTED_EDGE ( 'NONE', *, *, #14430, .T. ) ;
#18348=CARTESIAN_POINT ( 'NONE',  ( 0.3445219659099013620, -1.630113034087284030, -0.4330379103484557346 ) ) ;
#18360=CARTESIAN_POINT ( 'NONE',  ( 0.6424732214804906860, -1.458111371101026954, -0.4022076521922505754 ) ) ;
#18376=CARTESIAN_POINT ( 'NONE',  ( 0.3690006080204021321, -2.059917255124906532, -0.5191234088178223738 ) ) ;
#18377=( NAMED_UNIT ( * ) PLANE_ANGLE_UNIT ( ) SI_UNIT ( $, .RADIAN. ) );
#18379=CARTESIAN_POINT ( 'NONE',  ( -2.104432723530627271E-14, -2.062071153782512933, -0.6845211759026355036 ) ) ;
#18384=FACE_OUTER_BOUND ( 'NONE', #31480, .T. ) ;
#18388=CARTESIAN_POINT ( 'NONE',  ( 0.2169964291290918945, -1.302220840841494365, -0.4117811260064771495 ) ) ;
#18400=DIRECTION ( 'NONE',  ( -0.4999551463232377313, 0.8660512985181132439, 0.000000000000000000 ) ) ;
#18402=CARTESIAN_POINT ( 'NONE',  ( 0.3673504507587657120, -2.034217874421845096, -0.4825990138407615926 ) ) ;
#18405=CARTESIAN_POINT ( 'NONE',  ( 0.1909286924077255032, -1.257064795538239022, -0.7462941026102624109 ) ) ;
#18407=VERTEX_POINT ( 'NONE', #30041 ) ;
#18409=ORIENTED_EDGE ( 'NONE', *, *, #20732, .F. ) ;
#18414=DIRECTION ( 'NONE',  ( 0.4999551463232372872, -0.8660512985181134660, 0.000000000000000000 ) ) ;
#18415=DIRECTION ( 'NONE',  ( 0.4999551463232373427, -0.8660512985181134660, 0.000000000000000000 ) ) ;
#18416=CARTESIAN_POINT ( 'NONE',  ( 0.3932181676567889084, -1.978278275894043148, -0.4945254564861773505 ) ) ;
#18419=B_SPLINE_CURVE_WITH_KNOTS ( 'NONE', 3,
 ( #38852, #5455, #24405, #36940 ),
 .UNSPECIFIED., .F., .F.,
 ( 4, 4 ),
 ( 0.000000000000000000, 0.001604995851825731599 ),
 .UNSPECIFIED. ) ;
#18424=DIRECTION ( 'NONE',  ( 0.000000000000000000, 0.000000000000000000, -1.000000000000000000 ) ) ;
#18434=CARTESIAN_POINT ( 'NONE',  ( 0.6327495122412205575, -1.496409968128172396, -0.3957395255592697225 ) ) ;
#18439=DIRECTION ( 'NONE',  ( 0.8660512985181135770, 0.4999551463232370652, 0.000000000000000000 ) ) ;
#18445=CARTESIAN_POINT ( 'NONE',  ( 0.4170115945640066046, -1.702980413955158756, -0.6123808887097250686 ) ) ;
#18447=CARTESIAN_POINT ( 'NONE',  ( 0.5423380835500176689, -1.654573018669519335, -0.5568946855831939935 ) ) ;
#18476=CARTESIAN_POINT ( 'NONE',  ( 0.5934892211655993233, -1.486388914344519696, -0.3866566986715374021 ) ) ;
#18477=B_SPLINE_CURVE_WITH_KNOTS ( 'NONE', 3,
 ( #22791, #3827, #22581, #996 ),
 .UNSPECIFIED., .F., .F.,
 ( 4, 4 ),
 ( 0.4999999999999995559, 1.000000000000000000 ),
 .UNSPECIFIED. ) ;
#18484=CARTESIAN_POINT ( 'NONE',  ( 0.02022720027586020000, -1.618081545761635986, -0.6352904068409364058 ) ) ;
#18495=( BOUNDED_SURFACE ( )  B_SPLINE_SURFACE ( 3, 2, ( 
 ( #35277, #34858, #25206 ),
 ( #35462, #3192, #19643 ),
 ( #22149, #148, #19449 ),
 ( #37749, #7263, #32177 ),
 ( #7072, #31987, #3988 ),
 ( #16355, #13470, #3799 ),
 ( #13065, #3600, #28890 ),
 ( #19038, #15732, #22750 ),
 ( #22945, #16551, #31569 ),
 ( #31388, #9571, #25428 ),
 ( #28282, #35069, #38559 ),
 ( #751, #22541, #15945 ),
 ( #28490, #25827, #12642 ),
 ( #37957, #13257, #25616 ) ),
 .UNSPECIFIED., .F., .F., .T. ) 
 B_SPLINE_SURFACE_WITH_KNOTS ( ( 4, 2, 2, 2, 2, 2, 4 ),
 ( 3, 3 ),
 ( 1.517883041479706208E-18, 0.0009569864225024638437, 0.001435479633753695061, 0.001913972845004926170, 0.002392466056256157495, 0.002870959267507388821, 0.003827945690009851038 ),
 ( 0.000000000000000000, 1.000000000000000000 ),
 .UNSPECIFIED. ) 
 GEOMETRIC_REPRESENTATION_ITEM ( )  RATIONAL_B_SPLINE_SURFACE ( (
 ( 1.000000000000000000, 0.7071067811865471286, 1.000000000000000000),
 ( 1.000000000000000000, 0.6948232385253381160, 1.000000000000000000),
 ( 1.000000000000000000, 0.6807618830700954415, 1.000000000000000000),
 ( 1.000000000000000000, 0.6583014577179361337, 1.000000000000000000),
 ( 1.000000000000000000, 0.6505217571340542460, 1.000000000000000000),
 ( 1.000000000000000000, 0.6345534479354342228, 1.000000000000000000),
 ( 1.000000000000000000, 0.6262961088974926538, 1.000000000000000000),
 ( 1.000000000000000000, 0.6089017105673123487, 1.000000000000000000),
 ( 1.000000000000000000, 0.5996869661009254227, 1.000000000000000000),
 ( 1.000000000000000000, 0.5806079066951357337, 1.000000000000000000),
 ( 1.000000000000000000, 0.5707163240679670180, 1.000000000000000000),
 ( 1.000000000000000000, 0.5396746807496910492, 1.000000000000000000),
 ( 1.000000000000000000, 0.5169777448399269781, 1.000000000000000000),
 ( 1.000000000000000000, 0.4928180116091783747, 1.000000000000000000) ) ) 
 REPRESENTATION_ITEM ( '' )  SURFACE ( )  );
#18503=EDGE_CURVE ( 'NONE', #2063, #2060, #27808, .T. ) ;
#18513=EDGE_LOOP ( 'NONE', ( #35311, #32462, #23071, #31171, #11136 ) ) ;
#18522=CARTESIAN_POINT ( 'NONE',  ( 0.4778962374169136162, -1.100111666534134391, -0.4145951911632163034 ) ) ;
#18523=DIRECTION ( 'NONE',  ( -0.4999551463232377313, 0.8660512985181132439, -0.000000000000000000 ) ) ;
#18526=CIRCLE ( 'NONE', #6027, 0.02999999999999994685 ) ;
#18532=CARTESIAN_POINT ( 'NONE',  ( 0.4535584603515609992, -1.087313623170466759, -0.4112464619727521642 ) ) ;
#18547=DIRECTION ( 'NONE',  ( -0.4999551463232377313, 0.8660512985181132439, -0.000000000000000000 ) ) ;
#18562=ORIENTED_EDGE ( 'NONE', *, *, #14287, .T. ) ;
#18568=CARTESIAN_POINT ( 'NONE',  ( 0.3601266045266868776, -1.712180511123387872, -0.5700849473641345089 ) ) ;
#18589=AXIS2_PLACEMENT_3D ( 'NONE', #36265, #30111, #36486 ) ;
#18593=EDGE_CURVE ( 'NONE', #23137, #17453, #3463, .T. ) ;
#18599=CARTESIAN_POINT ( 'NONE',  ( 0.3583058169873264420, -1.905560598654033155, -0.4886429218441480371 ) ) ;
#18616=CARTESIAN_POINT ( 'NONE',  ( 0.3638611582725052584, -1.770072597806926940, -0.3444173258735140908 ) ) ;
#18623=ORIENTED_EDGE ( 'NONE', *, *, #17977, .F. ) ;
#18625=DIRECTION ( 'NONE',  ( -0.4999551463232377313, 0.8660512985181132439, 0.000000000000000000 ) ) ;
#18627=CIRCLE ( 'NONE', #23898, 0.009999999999999995004 ) ;
#18631=CARTESIAN_POINT ( 'NONE',  ( 0.1509261766453387776, -1.286374238887308064, -0.3063610351341911620 ) ) ;
#18633=CARTESIAN_POINT ( 'NONE',  ( 0.3999999999999784284, -2.047156491238096621, -0.7141923294504529673 ) ) ;
#18634=CARTESIAN_POINT ( 'NONE',  ( 0.1940479051238430952, -1.673580430301878641, -0.3295078277357051388 ) ) ;
#18641=CARTESIAN_POINT ( 'NONE',  ( 0.4441836334028865796, -1.145505455753590418, -0.6481113851292223949 ) ) ;
#18647=CARTESIAN_POINT ( 'NONE',  ( 0.6398031614116831411, -1.462875994906407850, -0.3971521418811111981 ) ) ;
#18656=CARTESIAN_POINT ( 'NONE',  ( 0.3808107057333847134, -1.740972190922900120, -0.5768324160695250669 ) ) ;
#18662=CARTESIAN_POINT ( 'NONE',  ( 0.5467981811930778813, -1.652054351292815637, -0.5405695263049933308 ) ) ;
#18669=EDGE_LOOP ( 'NONE', ( #10470, #20590, #6566, #27381 ) ) ;
#18678=DIRECTION ( 'NONE',  ( 0.000000000000000000, 0.7055763269171819729, 0.7086339301035887717 ) ) ;
#18679=EDGE_LOOP ( 'NONE', ( #9447, #33244, #13193, #39305, #13000, #12496, #18279, #37278 ) ) ;
#18686=CARTESIAN_POINT ( 'NONE',  ( 0.2298507129413651373, -1.629337845148150166, -0.3572920125246931145 ) ) ;
#18688=CIRCLE ( 'NONE', #322, 0.009999999999999995004 ) ;
#18690=CARTESIAN_POINT ( 'NONE',  ( 0.4200748011392089198, -1.654004974025707897, -0.2869361388274795921 ) ) ;
#18693=DIRECTION ( 'NONE',  ( -0.000000000000000000, 0.9396926207859082059, 0.3420201433256691570 ) ) ;
#18696=CARTESIAN_POINT ( 'NONE',  ( 0.08052762188558729162, -1.822603993077213103, -0.6442490663871589529 ) ) ;
#18711=CARTESIAN_POINT ( 'NONE',  ( 0.1880670007137922317, -1.959169693390261591, -0.6952383742845916759 ) ) ;
#18712=CARTESIAN_POINT ( 'NONE',  ( 0.2011892967074958294, -1.251141541415955905, -0.3144976166544465324 ) ) ;
#18713=AXIS2_PLACEMENT_3D ( 'NONE', #13813, #16719, #38302 ) ;
#18720=DIRECTION ( 'NONE',  ( 0.8660512985181134660, 0.4999551463232373427, 0.000000000000000000 ) ) ;
#18726=EDGE_CURVE ( 'NONE', #858, #23391, #5722, .T. ) ;
#18736=CARTESIAN_POINT ( 'NONE',  ( 0.1984950629327257021, -1.252696871964387393, -0.5155029497116575543 ) ) ;
#18741=CARTESIAN_POINT ( 'NONE',  ( 0.4688459138424371786, -1.061988423737608045, -0.4248180574663140141 ) ) ;
#18750=APPLICATION_CONTEXT ( 'configuration controlled 3d designs of mechanical parts and assemblies' ) ;
#18770=CARTESIAN_POINT ( 'NONE',  ( 0.3850572304970821258, -1.658899166394309788, -0.4146413147361216467 ) ) ;
#18802=LINE ( 'NONE', #28063, #35815 ) ;
#18805=EDGE_CURVE ( 'NONE', #23204, #30458, #23215, .T. ) ;
#18827=CIRCLE ( 'NONE', #1120, 0.04330708661417340122 ) ;
#18829=ORIENTED_EDGE ( 'NONE', *, *, #9032, .T. ) ;
#18831=CARTESIAN_POINT ( 'NONE',  ( 0.4159916692016358830, -1.069406866067976081, -0.5155029497116575543 ) ) ;
#18834=CARTESIAN_POINT ( 'NONE',  ( 0.3579523269453451229, -1.819438262761551073, -0.3432675831194216820 ) ) ;
#18851=CARTESIAN_POINT ( 'NONE',  ( 0.7237670104885922662, -1.526800250143491189, -0.6194292131661300882 ) ) ;
#18858=DIRECTION ( 'NONE',  ( 0.4999551463232372872, -0.8660512985181134660, 0.000000000000000000 ) ) ;
#18867=CARTESIAN_POINT ( 'NONE',  ( 0.3999999999999787059, -2.097675824466503691, -0.4688691127277797022 ) ) ;
#18873=CARTESIAN_POINT ( 'NONE',  ( 0.4072427871757727247, -1.593905482146963148, -0.4124169901356457557 ) ) ;
#18874=CARTESIAN_POINT ( 'NONE',  ( 0.3641226214008350115, -1.992333883506425929, -0.5205058662226371702 ) ) ;
#18876=CARTESIAN_POINT ( 'NONE',  ( 0.3686268575871315401, -2.054613415874774862, -0.4779605220224154571 ) ) ;
#18880=CARTESIAN_POINT ( 'NONE',  ( 0.5198360076875652158, -1.665829548412769201, -0.5914331627923441470 ) ) ;
#18897=ORIENTED_EDGE ( 'NONE', *, *, #3504, .F. ) ;
#18905=CARTESIAN_POINT ( 'NONE',  ( 0.1475835875794125895, -1.275005690054430874, -0.3395826425993545561 ) ) ;
#18907=CARTESIAN_POINT ( 'NONE',  ( -2.128333683970191216E-14, -2.097675824466503691, -0.2907100122647986451 ) ) ;
#18908=CARTESIAN_POINT ( 'NONE',  ( 0.2999999999999791167, -2.097675824466505023, -0.2588528740066098344 ) ) ;
#18913=CARTESIAN_POINT ( 'NONE',  ( 0.09553074791598278881, -1.668408090489538864, -0.6432190139176878763 ) ) ;
#18923=CARTESIAN_POINT ( 'NONE',  ( 0.5860224930377164743, -1.538459444162366019, -0.4143855572951781197 ) ) ;
#18924=CARTESIAN_POINT ( 'NONE',  ( 0.1846519493495785980, -1.936915843690041994, -0.6921256737722615293 ) ) ;
#18944=CARTESIAN_POINT ( 'NONE',  ( 0.3699999999999786793, -2.183180860297921466, -0.4937760292030871079 ) ) ;
#18945=ORIENTED_EDGE ( 'NONE', *, *, #36099, .T. ) ;
#18947=CARTESIAN_POINT ( 'NONE',  ( 0.4667255516235201407, -1.094999438749613585, -0.3992978201560059559 ) ) ;
#18948=FACE_OUTER_BOUND ( 'NONE', #38324, .T. ) ;
#18957=DIRECTION ( 'NONE',  ( 0.8660512985181133550, 0.4999551463232372872, -1.835254611910146959E-15 ) ) ;
#18964=EDGE_CURVE ( 'NONE', #16904, #24117, #16574, .T. ) ;
#18970=CARTESIAN_POINT ( 'NONE',  ( 0.4488015593626361044, -1.143595277755407036, -0.6412565985276246217 ) ) ;
#18975=VERTEX_POINT ( 'NONE', #19660 ) ;
#18977=DIRECTION ( 'NONE',  ( -0.4999551463232369541, 0.8660512985181135770, 0.000000000000000000 ) ) ;
#18978=CARTESIAN_POINT ( 'NONE',  ( 0.3393113466938358358, -1.652445952795071227, -0.5834520628848905988 ) ) ;
#18983=DIRECTION ( 'NONE',  ( 0.000000000000000000, 0.000000000000000000, -1.000000000000000000 ) ) ;
#18986=CARTESIAN_POINT ( 'NONE',  ( 0.3978748429313913038, -1.632648866504059049, -0.3859154407376138018 ) ) ;
#18988=CARTESIAN_POINT ( 'NONE',  ( 0.5759858430877791147, -1.611702281530391856, -0.5409994141166248882 ) ) ;
#18992=CARTESIAN_POINT ( 'NONE',  ( 0.2923286432308245808, -1.660243258845594649, -0.6250000000000000000 ) ) ;
#18995=ADVANCED_FACE ( 'NONE', ( #32610 ), #36304, .F. ) ;
#18999=B_SPLINE_CURVE_WITH_KNOTS ( 'NONE', 3,
 ( #22975, #13694, #600, #13094, #25652, #39213 ),
 .UNSPECIFIED., .F., .F.,
 ( 4, 2, 4 ),
 ( 0.000000000000000000, 0.0006234106414633451380, 0.001246821282926690276 ),
 .UNSPECIFIED. ) ;
#19009=EDGE_CURVE ( 'NONE', #39975, #3578, #5030, .T. ) ;
#19020=VERTEX_POINT ( 'NONE', #31103 ) ;
#19021=VERTEX_POINT ( 'NONE', #23776 ) ;
#19026=CARTESIAN_POINT ( 'NONE',  ( 0.2578922072143235433, -1.569585936607025944, -0.3484340070010775170 ) ) ;
#19034=ORIENTED_EDGE ( 'NONE', *, *, #38663, .T. ) ;
#19038=CARTESIAN_POINT ( 'NONE',  ( 0.5065174388604494204, -1.605197562044919701, -0.4068557283993430862 ) ) ;
#19056=CARTESIAN_POINT ( 'NONE',  ( 0.6089144417693378442, -1.582852168051670505, -0.4632939045166076242 ) ) ;
#19058=CARTESIAN_POINT ( 'NONE',  ( 0.3996070378906176890, -2.075685236164255265, -0.4730688532139160629 ) ) ;
#19064=EDGE_CURVE ( 'NONE', #33803, #7743, #11361, .T. ) ;
#19068=CARTESIAN_POINT ( 'NONE',  ( 0.1734973056165642902, -1.209394307038482497, -0.5155029497116575543 ) ) ;
#19070=CARTESIAN_POINT ( 'NONE',  ( 0.4072455522228593527, -1.612170731801505941, -0.6686547157232122229 ) ) ;
#19076=DIRECTION ( 'NONE',  ( 0.4999551463232373427, -0.8660512985181134660, 0.000000000000000000 ) ) ;
#19091=EDGE_LOOP ( 'NONE', ( #5998, #19170, #25974, #239, #13028, #13366, #4245, #21871, #35052, #9921 ) ) ;
#19108=CARTESIAN_POINT ( 'NONE',  ( 0.1591109521009923256, -1.922302435482596383, -0.6593845993814091422 ) ) ;
#19114=EDGE_CURVE ( 'NONE', #34037, #34358, #23862, .T. ) ;
#19119=CARTESIAN_POINT ( 'NONE',  ( 0.1833713392910780726, -1.690506555516771092, -0.6838718444642555294 ) ) ;
#19126=ORIENTED_EDGE ( 'NONE', *, *, #6142, .T. ) ;
#19136=ORIENTED_EDGE ( 'NONE', *, *, #25522, .T. ) ;
#19140=CARTESIAN_POINT ( 'NONE',  ( 0.3812071769896587803, -1.763750790280042002, -0.4536492913031247021 ) ) ;
#19143=CARTESIAN_POINT ( 'NONE',  ( -0.004088490883478934287, -1.369644552158580053, -0.6494983983435047570 ) ) ;
#19154=VECTOR ( 'NONE', #9027, 39.37007874015748143 ) ;
#19155=CARTESIAN_POINT ( 'NONE',  ( 0.4483572554135741850, -1.096823335528599674, -0.4056879302696327350 ) ) ;
#19157=DIRECTION ( 'NONE',  ( 0.4999551463232373427, -0.8660512985181134660, 0.000000000000000000 ) ) ;
#19159=CARTESIAN_POINT ( 'NONE',  ( 0.3696577572605105888, -1.751079222393305823, -0.4256963421901115430 ) ) ;
#19170=ORIENTED_EDGE ( 'NONE', *, *, #26043, .T. ) ;
#19173=AXIS2_PLACEMENT_3D ( 'NONE', #33348, #17912, #39729 ) ;
#19175=CARTESIAN_POINT ( 'NONE',  ( 0.4768848212686795929, -1.682051206446436797, -0.4156371400837810537 ) ) ;
#19177=ORIENTED_EDGE ( 'NONE', *, *, #11210, .T. ) ;
#19178=ORIENTED_EDGE ( 'NONE', *, *, #7018, .T. ) ;
#19179=CARTESIAN_POINT ( 'NONE',  ( 0.5260973920735738663, -1.675551188129234204, -0.5699138614793077817 ) ) ;
#19181=ORIENTED_EDGE ( 'NONE', *, *, #40315, .F. ) ;
#19182=CIRCLE ( 'NONE', #4064, 0.2232808441893194829 ) ;
#19183=CARTESIAN_POINT ( 'NONE',  ( 0.6278493015080260919, -1.616811722168019605, -0.5276078387673933667 ) ) ;
#19185=DIRECTION ( 'NONE',  ( 0.8185200378235019114, 0.4725162423735941863, -0.3267313091433876049 ) ) ;
#19186=VERTEX_POINT ( 'NONE', #11628 ) ;
#19189=CARTESIAN_POINT ( 'NONE',  ( 0.3941416742250357097, -1.601254223528187470, -0.3530575408666304371 ) ) ;
#19191=CARTESIAN_POINT ( 'NONE',  ( 0.6062242576285924445, -1.566401754662989587, -0.6176321414136997090 ) ) ;
#19193=ORIENTED_EDGE ( 'NONE', *, *, #34731, .F. ) ;
#19196=EDGE_CURVE ( 'NONE', #25557, #5600, #32370, .T. ) ;
#19214=ORIENTED_EDGE ( 'NONE', *, *, #26046, .T. ) ;
#19232=ORIENTED_EDGE ( 'NONE', *, *, #33062, .T. ) ;
#19234=ORIENTED_EDGE ( 'NONE', *, *, #13496, .F. ) ;
#19245=CARTESIAN_POINT ( 'NONE',  ( 0.3699999999999786793, -2.183180860297921466, -0.5437760292030870968 ) ) ;
#19250=CARTESIAN_POINT ( 'NONE',  ( 0.2914072444767246695, -1.544007756657866270, -0.3072620149518441313 ) ) ;
#19257=CARTESIAN_POINT ( 'NONE',  ( 0.3544525855956190963, -1.628498139902242681, -0.6593841416022943047 ) ) ;
#19262=CIRCLE ( 'NONE', #24526, 0.05330708661417327826 ) ;
#19278=DIRECTION ( 'NONE',  ( 0.4999551463232373427, -0.8660512985181134660, 0.000000000000000000 ) ) ;
#19279=CIRCLE ( 'NONE', #26501, 0.04330708661417340122 ) ;
#19282=DIRECTION ( 'NONE',  ( -0.7956551220374292743, -0.4593167559955302903, 0.3949190352937497761 ) ) ;
#19293=DIRECTION ( 'NONE',  ( 0.4999551463232373427, -0.8660512985181134660, 0.000000000000000000 ) ) ;
#19294=CARTESIAN_POINT ( 'NONE',  ( 0.1970768337340418341, -2.011495956325795920, -0.3159642937727323853 ) ) ;
#19303=CARTESIAN_POINT ( 'NONE',  ( 0.5284862694945503536, -1.177654592776627318, -0.5155029497116575543 ) ) ;
#19313=CARTESIAN_POINT ( 'NONE',  ( 0.1949656944119497748, -2.006413414762151515, -0.7037340768493718368 ) ) ;
#19315=AXIS2_PLACEMENT_3D ( 'NONE', #24808, #25981, #10334 ) ;
#19327=B_SPLINE_CURVE_WITH_KNOTS ( 'NONE', 3,
 ( #27714, #15582, #30604, #9388, #18876, #21965, #40043, #18253 ),
 .UNSPECIFIED., .F., .F.,
 ( 4, 2, 2, 4 ),
 ( 0.000000000000000000, 0.001677695221323086258, 0.002516542831984629278, 0.003355390442646172516 ),
 .UNSPECIFIED. ) ;
#19329=CARTESIAN_POINT ( 'NONE',  ( 0.2488895021796825036, -1.574756068310029455, -0.7071313240274791356 ) ) ;
#19332=AXIS2_PLACEMENT_3D ( 'NONE', #34282, #6305, #27519 ) ;
#19333=ORIENTED_EDGE ( 'NONE', *, *, #37220, .F. ) ;
#19338=CARTESIAN_POINT ( 'NONE',  ( 0.3543393621149266148, -1.718158840355286765, -0.4818782773072323722 ) ) ;
#19340=CARTESIAN_POINT ( 'NONE',  ( 0.1984950629327257021, -1.252696871964387393, -0.5155029497116575543 ) ) ;
#19341=VERTEX_POINT ( 'NONE', #15209 ) ;
#19345=VERTEX_POINT ( 'NONE', #37012 ) ;
#19348=CARTESIAN_POINT ( 'NONE',  ( 0.1959282438327735465, -1.265725308457275045, -0.3194741108003418262 ) ) ;
#19352=CARTESIAN_POINT ( 'NONE',  ( 0.04109334229010794953, -1.703983732577595056, -0.3380635556694617239 ) ) ;
#19357=CARTESIAN_POINT ( 'NONE',  ( 0.4751758298663427693, -1.652426242819087010, -0.6334442537810193175 ) ) ;
#19361=( BOUNDED_SURFACE ( )  B_SPLINE_SURFACE ( 3, 2, ( 
 ( #34895, #3641, #4023 ),
 ( #35494, #19672, #13511 ),
 ( #26074, #4236, #38592 ),
 ( #16203, #10414, #28738 ) ),
 .UNSPECIFIED., .F., .F., .T. ) 
 B_SPLINE_SURFACE_WITH_KNOTS ( ( 4, 4 ),
 ( 3, 3 ),
 ( -8.673617379884035472E-19, 0.0003267904260525523758 ),
 ( 0.000000000000000000, 1.000000000000000000 ),
 .UNSPECIFIED. ) 
 GEOMETRIC_REPRESENTATION_ITEM ( )  RATIONAL_B_SPLINE_SURFACE ( (
 ( 1.000000000000000000, 0.7071189998922904341, 1.000000000000000000),
 ( 1.000000000000000000, 0.7071106962636509730, 1.000000000000000000),
 ( 1.000000000000000000, 0.7071067813167358773, 1.000000000000000000),
 ( 1.000000000000000000, 0.7071067811865512365, 1.000000000000000000) ) ) 
 REPRESENTATION_ITEM ( '' )  SURFACE ( )  );
#19371=CARTESIAN_POINT ( 'NONE',  ( 0.4434344506101033923, -1.107353083073178146, -0.6343966985258274738 ) ) ;
#19377=CARTESIAN_POINT ( 'NONE',  ( 0.1801850755352660816, -1.895435244648604245, -0.6572603376541747977 ) ) ;
#19379=CARTESIAN_POINT ( 'NONE',  ( 0.4101899714674371866, -1.674693119776962336, -0.5152975299054542990 ) ) ;
#19391=CIRCLE ( 'NONE', #1665, 0.04330708661417327632 ) ;
#19399=CARTESIAN_POINT ( 'NONE',  ( 0.6209541335343498059, -1.620792173117170609, -0.5418768570690311037 ) ) ;
#19413=CARTESIAN_POINT ( 'NONE',  ( 0.4521982902084413225, -1.612316853396095429, -0.6577709497374332193 ) ) ;
#19417=CARTESIAN_POINT ( 'NONE',  ( 0.4959778976180506116, -1.681391946368784751, -0.5155029497116575543 ) ) ;
#19437=EDGE_LOOP ( 'NONE', ( #19493, #6925, #34294, #10218 ) ) ;
#19449=CARTESIAN_POINT ( 'NONE',  ( 0.5008954076588254534, -1.585800327213603200, -0.4745784240349925631 ) ) ;
#19455=VERTEX_POINT ( 'NONE', #21413 ) ;
#19463=B_SPLINE_CURVE_WITH_KNOTS ( 'NONE', 3,
 ( #8773, #30789, #17826, #27101, #37361, #34072, #36749, #12281, #30181, #24423, #2418, #15146, #14756, #33660, #14537, #30385, #5873, #20742, #18244, #2011, #24225, #12075, #30987, #40457 ),
 .UNSPECIFIED., .F., .F.,
 ( 4, 2, 2, 2, 2, 2, 2, 2, 2, 2, 2, 4 ),
 ( 0.000000000000000000, 0.002721158394890018685, 0.005442316789780037370, 0.008163475184670055187, 0.01088463357956007474, 0.01360579197445009429, 0.01632695036934011037, 0.01768752956678512275, 0.01904810876423013166, 0.01972839836295263091, 0.02040868796167513710, 0.02176926715912013560 ),
 .UNSPECIFIED. ) ;
#19475=ORIENTED_EDGE ( 'NONE', *, *, #5018, .F. ) ;
#19476=CARTESIAN_POINT ( 'NONE',  ( 0.4738786505895521417, -1.126875767161299002, -0.6503782676396133722 ) ) ;
#19479=DIRECTION ( 'NONE',  ( -0.8660512985181130219, -0.4999551463232377868, 0.000000000000000000 ) ) ;
#19483=CIRCLE ( 'NONE', #27364, 0.04330708661417327632 ) ;
#19490=DIRECTION ( 'NONE',  ( 0.8660512985181134660, 0.4999551463232373427, 0.000000000000000000 ) ) ;
#19493=ORIENTED_EDGE ( 'NONE', *, *, #3868, .T. ) ;
#19497=ORIENTED_EDGE ( 'NONE', *, *, #34585, .F. ) ;
#19499=EDGE_CURVE ( 'NONE', #28471, #31608, #34116, .T. ) ;
#19507=ORIENTED_EDGE ( 'NONE', *, *, #11400, .F. ) ;
#19509=CARTESIAN_POINT ( 'NONE',  ( 0.4787354706056592413, -1.098877335703110969, -0.6155895193482675554 ) ) ;
#19512=CARTESIAN_POINT ( 'NONE',  ( 0.3890391140888923016, -1.644011320431554513, -0.7368878597108073913 ) ) ;
#19514=CARTESIAN_POINT ( 'NONE',  ( 0.1999999999999760025, -1.903589451742650818, -0.3294945365547880534 ) ) ;
#19518=CARTESIAN_POINT ( 'NONE',  ( 0.3933511135026758199, -1.980813283754576659, -0.7022017663186461700 ) ) ;
#19531=CARTESIAN_POINT ( 'NONE',  ( -2.134683096299215694E-14, -2.107936428766274073, -0.2870436526301869407 ) ) ;
#19544=CARTESIAN_POINT ( 'NONE',  ( 0.4597632563371517600, -1.044138351040537982, -0.6056023639864149821 ) ) ;
#19557=CARTESIAN_POINT ( 'NONE',  ( 0.02125805212145761777, -1.630277869852022166, -0.3723835954392284986 ) ) ;
#19568=DIRECTION ( 'NONE',  ( 0.8660512985181135770, 0.4999551463232368431, 0.000000000000000000 ) ) ;
#19569=CARTESIAN_POINT ( 'NONE',  ( 0.4709867352971914833, -1.164672508904967652, -0.5155029497116575543 ) ) ;
#19570=CARTESIAN_POINT ( 'NONE',  ( 0.4922290639190164963, -1.198585196483133553, -0.6250000000000000000 ) ) ;
#19575=CARTESIAN_POINT ( 'NONE',  ( 0.4752104778612297187, -1.162234221663497546, -0.6186948529734399571 ) ) ;
#19576=CARTESIAN_POINT ( 'NONE',  ( 0.6400160853294423191, -1.459529829645036081, -0.3976988710621562895 ) ) ;
#19581=ORIENTED_EDGE ( 'NONE', *, *, #24305, .T. ) ;
#19582=CARTESIAN_POINT ( 'NONE',  ( 0.4611535779349406061, -1.147956045046751639, -0.4054009984114392284 ) ) ;
#19595=CARTESIAN_POINT ( 'NONE',  ( 0.6106509172825420606, -1.615137135503808441, -0.5296025793890921651 ) ) ;
#19599=ORIENTED_EDGE ( 'NONE', *, *, #13789, .F. ) ;
#19600=ADVANCED_FACE ( 'NONE', ( #25498 ), #6107, .F. ) ;
#19602=AXIS2_PLACEMENT_3D ( 'NONE', #1551, #4792, #20056 ) ;
#19605=EDGE_LOOP ( 'NONE', ( #29813, #16436, #24851, #17389, #39110 ) ) ;
#19606=CARTESIAN_POINT ( 'NONE',  ( 0.6379677523173985509, -1.610970530585465355, -0.5598555352671841234 ) ) ;
#19611=CARTESIAN_POINT ( 'NONE',  ( 0.5280871129044060197, -1.601407886612749021, -0.5973377142089556502 ) ) ;
#19615=CARTESIAN_POINT ( 'NONE',  ( 0.4781054596003559420, -1.118034740588623954, -0.3965712557909421565 ) ) ;
#19623=EDGE_LOOP ( 'NONE', ( #40325, #4171, #24661, #23400, #20646 ) ) ;
#19627=VERTEX_POINT ( 'NONE', #32667 ) ;
#19633=ORIENTED_EDGE ( 'NONE', *, *, #8735, .T. ) ;
#19634=FACE_OUTER_BOUND ( 'NONE', #34232, .T. ) ;
#19643=CARTESIAN_POINT ( 'NONE',  ( 0.5040251875448504837, -1.584373116627600275, -0.4836906369935438654 ) ) ;
#19649=CARTESIAN_POINT ( 'NONE',  ( 0.6638313581005879094, -1.459541049076493735, -0.6171250890061030780 ) ) ;
#19650=CARTESIAN_POINT ( 'NONE',  ( 0.2524564437961140939, -1.572036326075024526, -0.3190288371789616328 ) ) ;
#19658=FACE_OUTER_BOUND ( 'NONE', #26636, .T. ) ;
#19660=CARTESIAN_POINT ( 'NONE',  ( 0.4738546087217606062, -1.652018268363231845, -0.3975985852014427002 ) ) ;
#19661=CARTESIAN_POINT ( 'NONE',  ( 0.1798596100760564143, -1.237890289190527904, -0.6192247734168379036 ) ) ;
#19663=CARTESIAN_POINT ( 'NONE',  ( 0.4806378395295556882, -1.105637800341302102, -0.6194292131661300882 ) ) ;
#19664=CARTESIAN_POINT ( 'NONE',  ( 0.3972854997516396258, -1.646912688252536006, -0.3935780560914288184 ) ) ;
#19672=CARTESIAN_POINT ( 'NONE',  ( 0.1842694382075218962, -1.260909057897439789, -0.7430131060672421350 ) ) ;
#19680=ORIENTED_EDGE ( 'NONE', *, *, #23081, .T. ) ;
#19691=CARTESIAN_POINT ( 'NONE',  ( 0.5376330384393707140, -1.631732069091240689, -0.4370647559278275085 ) ) ;
#19692=CARTESIAN_POINT ( 'NONE',  ( 0.1961868571575540177, -1.348426346360368955, -0.3372674651588674632 ) ) ;
#19695=FACE_OUTER_BOUND ( 'NONE', #3088, .T. ) ;
#19699=ADVANCED_FACE ( 'NONE', ( #26300 ), #10344, .T. ) ;
#19701=CARTESIAN_POINT ( 'NONE',  ( 0.3890272469822507184, -1.925427499875787651, -0.6972876674577032086 ) ) ;
#19703=CARTESIAN_POINT ( 'NONE',  ( 0.3582292064121807007, -1.745863530688037013, -0.4681685754184095605 ) ) ;
#19715=CARTESIAN_POINT ( 'NONE',  ( 0.5368059768295552203, -1.632287305134593858, -0.5948306701282568554 ) ) ;
#19720=EDGE_LOOP ( 'NONE', ( #26248, #16688, #26171, #12292 ) ) ;
#19728=CARTESIAN_POINT ( 'NONE',  ( 0.3324871086615489024, -1.659137217475706860, -0.6399689536651946842 ) ) ;
#19730=CARTESIAN_POINT ( 'NONE',  ( 0.5305894487643406654, -1.569038067003539316, -0.5473203437262895710 ) ) ;
#19732=TOROIDAL_SURFACE ( 'NONE', #34840, 0.1333070866141732314, 0.02999999999999999889 ) ;
#19736=LINE ( 'NONE', #29205, #33888 ) ;
#19737=B_SPLINE_CURVE_WITH_KNOTS ( 'NONE', 3,
 ( #28610, #9868, #31077, #9067, #15845, #15449, #5963, #3713, #479, #15647 ),
 .UNSPECIFIED., .F., .F.,
 ( 4, 2, 2, 2, 4 ),
 ( -2.424788074806314843E-05, 0.002669425500014234020, 0.004016262190395372689, 0.004689680535585941806, 0.005363098880776510057 ),
 .UNSPECIFIED. ) ;
#19756=CARTESIAN_POINT ( 'NONE',  ( 0.1798968830709493649, -1.237954855633865536, -0.4125659523519146221 ) ) ;
#19760=CARTESIAN_POINT ( 'NONE',  ( 0.3573610978452740894, -1.882114898915002055, -0.4864032973032175744 ) ) ;
#19764=EDGE_LOOP ( 'NONE', ( #25812, #2995, #15676, #29154 ) ) ;
#19777=CARTESIAN_POINT ( 'NONE',  ( 0.6277051948539001947, -1.616894912232479831, -0.5046519086154381828 ) ) ;
#19784=CARTESIAN_POINT ( 'NONE',  ( 0.4170376818810827002, -1.621705073591293678, -0.3781026430796730065 ) ) ;
#19796=CARTESIAN_POINT ( 'NONE',  ( 0.5314857169285645000, -1.600448699198730562, -0.5913921701293719524 ) ) ;
#19803=CARTESIAN_POINT ( 'NONE',  ( 0.4511230681663170872, -1.093032438009407192, -0.6231826621457485782 ) ) ;
#19812=CARTESIAN_POINT ( 'NONE',  ( 0.4123050674383867409, -1.729694699482061671, -0.5155029497116575543 ) ) ;
#19817=CARTESIAN_POINT ( 'NONE',  ( 0.3999999999999787059, -2.097675824466503691, -0.7286991843995640483 ) ) ;
#19820=CARTESIAN_POINT ( 'NONE',  ( 0.2764337282391428618, -1.207704344519209938, -0.5166151207188711680 ) ) ;
#19831=ORIENTED_EDGE ( 'NONE', *, *, #26502, .F. ) ;
#19844=B_SPLINE_CURVE_WITH_KNOTS ( 'NONE', 3,
 ( #15088, #27644, #14896, #30317, #20882, #5211 ),
 .UNSPECIFIED., .F., .F.,
 ( 4, 2, 4 ),
 ( 0.0004700531327201783335, 0.0008837629426271082726, 0.001297472752534038374 ),
 .UNSPECIFIED. ) ;
#19845=CARTESIAN_POINT ( 'NONE',  ( 0.2161879510971927432, -1.277123080371499242, -0.3144976166544468099 ) ) ;
#19846=B_SPLINE_CURVE_WITH_KNOTS ( 'NONE', 3,
 ( #31730, #3150, #38298, #6227, #22291, #37911, #38098, #6610, #711, #34806, #19191, #37699, #28658, #16119, #22705, #32139, #22488, #6420, #9522, #22098, #18988, #28440, #35013, #314 ),
 .UNSPECIFIED., .F., .F.,
 ( 4, 2, 2, 2, 2, 2, 2, 2, 2, 2, 2, 4 ),
 ( 0.000000000000000000, 0.0009274901291892772215, 0.001854980258378554443, 0.002782470387567831556, 0.003709960516757108886, 0.004637450645946387950, 0.005101195710541035939, 0.005564940775135683929, 0.006028685839730332785, 0.006492430904324981641, 0.006956175968919630498, 0.007419921033514278487 ),
 .UNSPECIFIED. ) ;
#19849=DIRECTION ( 'NONE',  ( 0.8660512985181132439, 0.4999551463232379533, 0.000000000000000000 ) ) ;
#19850=AXIS2_PLACEMENT_3D ( 'NONE', #29253, #35230, #32730 ) ;
#19851=TOROIDAL_SURFACE ( 'NONE', #33636, 0.05000000000000000971, 0.2000000000000000111 ) ;
#19855=DIRECTION ( 'NONE',  ( -0.8660512985181131329, -0.4999551463232376758, 0.000000000000000000 ) ) ;
#19866=CARTESIAN_POINT ( 'NONE',  ( 0.4650133494175291982, -1.133480851973431847, -0.6660426939124519663 ) ) ;
#19869=CARTESIAN_POINT ( 'NONE',  ( 0.3514318747802386289, -1.706361087322654235, -0.4728986729284584412 ) ) ;
#19872=VERTEX_POINT ( 'NONE', #21140 ) ;
#19882=CARTESIAN_POINT ( 'NONE',  ( 0.4709867352971914833, -1.164672508904967652, -0.5155029497116575543 ) ) ;
#19890=CARTESIAN_POINT ( 'NONE',  ( 0.4763501221259693330, -1.554011115824661893, -0.5166151207188711680 ) ) ;
#19893=ORIENTED_EDGE ( 'NONE', *, *, #4613, .F. ) ;
#19894=ORIENTED_EDGE ( 'NONE', *, *, #24543, .F. ) ;
#19897=CARTESIAN_POINT ( 'NONE',  ( 0.5135328215522156903, -1.640276221155167358, -0.4151541396484864088 ) ) ;
#19899=DIRECTION ( 'NONE',  ( 1.060606950627616773E-16, 6.122684696619993730E-17, 1.000000000000000000 ) ) ;
#19903=CARTESIAN_POINT ( 'NONE',  ( 0.3969700875656219652, -1.750093955434198989, -0.5306525527942704823 ) ) ;
#19906=CARTESIAN_POINT ( 'NONE',  ( 0.3842624604883869144, -1.722789849446889177, -0.7210690300480241399 ) ) ;
#19911=CARTESIAN_POINT ( 'NONE',  ( 0.6348086598072710807, -1.524658463883513004, -0.6128917709820664861 ) ) ;
#19914=CARTESIAN_POINT ( 'NONE',  ( 0.4112193008909481584, -1.591609915475934889, -0.6177460231409163116 ) ) ;
#19919=CARTESIAN_POINT ( 'NONE',  ( 0.5659382422188921069, -1.581708796928036342, -0.4824204755890118546 ) ) ;
#19929=AXIS2_PLACEMENT_3D ( 'NONE', #29049, #23103, #7432 ) ;
#19937=CARTESIAN_POINT ( 'NONE',  ( 0.3562792623313784657, -1.606250998287605869, -0.3924671920701706118 ) ) ;
#19944=CARTESIAN_POINT ( 'NONE',  ( 0.02998331132317445802, -2.054508416935759474, -0.2740450252055757763 ) ) ;
#19946=CARTESIAN_POINT ( 'NONE',  ( 0.3999999999999787059, -2.183180860297921466, -0.4937760292030871079 ) ) ;
#19951=CIRCLE ( 'NONE', #19315, 0.2200000000000001121 ) ;
#19952=ADVANCED_FACE ( 'NONE', ( #1829 ), #20314, .F. ) ;
#19967=TOROIDAL_SURFACE ( 'NONE', #30480, 0.05330708661417323663, 0.01000000000000000021 ) ;
#19968=TOROIDAL_SURFACE ( 'NONE', #2875, 0.2200000000000000011, 0.02999999999999999889 ) ;
#19970=CARTESIAN_POINT ( 'NONE',  ( 0.3571704890607551586, -1.830049479072539231, -0.6659963912414424980 ) ) ;
#19973=EDGE_CURVE ( 'NONE', #19021, #37901, #12999, .T. ) ;
#19976=ORIENTED_EDGE ( 'NONE', *, *, #29019, .F. ) ;
#19985=CARTESIAN_POINT ( 'NONE',  ( 0.5082546964191734240, -1.641980856392960098, -0.4117015674416750204 ) ) ;
#19986=VERTEX_POINT ( 'NONE', #3417 ) ;
#19989=EDGE_LOOP ( 'NONE', ( #38843, #6722, #4822, #26814 ) ) ;
#19991=ORIENTED_EDGE ( 'NONE', *, *, #39193, .F. ) ;
#19994=CARTESIAN_POINT ( 'NONE',  ( 0.6126863732757561465, -1.613714656222153154, -0.4894191377505581197 ) ) ;
#20006=ADVANCED_FACE ( 'NONE', ( #25237 ), #14967, .F. ) ;
#20007=CARTESIAN_POINT ( 'NONE',  ( 0.4739235880194173633, -1.591156355542383105, -0.4387572789578180754 ) ) ;
#20011=CARTESIAN_POINT ( 'NONE',  ( 0.4544607142047081272, -1.663558774996698464, -0.4080516749217623640 ) ) ;
#20013=CARTESIAN_POINT ( 'NONE',  ( 0.5202445037400105221, -1.603350735003311156, -0.6087954913505664312 ) ) ;
#20020=DIRECTION ( 'NONE',  ( 0.4999551463232372317, -0.8660512985181134660, 0.000000000000000000 ) ) ;
#20044=CARTESIAN_POINT ( 'NONE',  ( 0.3336071016620586471, -1.750777463471590023, -0.4969093018047625043 ) ) ;
#20049=VERTEX_POINT ( 'NONE', #20883 ) ;
#20056=DIRECTION ( 'NONE',  ( -0.8735110198817035432, 0.000000000000000000, 0.4868043735888433754 ) ) ;
#20059=ORIENTED_EDGE ( 'NONE', *, *, #995, .T. ) ;
#20061=ORIENTED_EDGE ( 'NONE', *, *, #11959, .T. ) ;
#20065=CIRCLE ( 'NONE', #33824, 0.1333070866141734812 ) ;
#20066=DIRECTION ( 'NONE',  ( -0.5176477751948445061, -0.2988283368828927866, -0.8017121714877678551 ) ) ;
#20067=CIRCLE ( 'NONE', #2324, 0.1700000000000000400 ) ;
#20088=CARTESIAN_POINT ( 'NONE',  ( 0.3593346688482150775, -1.735925422213634661, -0.5010936962835139674 ) ) ;
#20095=CARTESIAN_POINT ( 'NONE',  ( 0.4219866632171650478, -1.610104465087853765, -0.3647299066799348233 ) ) ;
#20098=DIRECTION ( 'NONE',  ( 1.060606950627616773E-16, 6.122684696619993730E-17, 1.000000000000000000 ) ) ;
#20101=CARTESIAN_POINT ( 'NONE',  ( 0.3582455198832254495, -1.774135343334821924, -0.4890060775958486872 ) ) ;
#20102=CARTESIAN_POINT ( 'NONE',  ( 0.5713772049386515173, -1.545306863045628143, -0.5074489717415853196 ) ) ;
#20104=CIRCLE ( 'NONE', #31294, 0.1033070866141734129 ) ;
#20109=DIRECTION ( 'NONE',  ( -0.4999551463232371207, 0.8660512985181134660, 0.000000000000000000 ) ) ;
#20110=CARTESIAN_POINT ( 'NONE',  ( 0.1841497487818726797, -1.740483164027640584, -0.3571093288873294358 ) ) ;
#20115=DIRECTION ( 'NONE',  ( 0.000000000000000000, 0.000000000000000000, -1.000000000000000000 ) ) ;
#20118=CARTESIAN_POINT ( 'NONE',  ( 0.5612334960093817715, -1.620627794947044897, -0.4868944820179721966 ) ) ;
#20122=CARTESIAN_POINT ( 'NONE',  ( 0.5652024041994130332, -1.318123455396758681, -0.6186948529734399571 ) ) ;
#20139=CARTESIAN_POINT ( 'NONE',  ( 0.5791375636586371112, -1.530547062312576534, -0.5677195341231595638 ) ) ;
#20140=CARTESIAN_POINT ( 'NONE',  ( -2.134683096299215694E-14, -2.104523772034943452, -0.2882857580878072090 ) ) ;
#20145=ORIENTED_EDGE ( 'NONE', *, *, #31085, .T. ) ;
#20146=CARTESIAN_POINT ( 'NONE',  ( 0.3655542017575511005, -1.763257256764854786, -0.5881144261364762427 ) ) ;
#20149=DIRECTION ( 'NONE',  ( -0.4999551463232377313, 0.8660512985181132439, 0.000000000000000000 ) ) ;
#20154=AXIS2_PLACEMENT_3D ( 'NONE', #39879, #30417, #2248 ) ;
#20155=FACE_OUTER_BOUND ( 'NONE', #17158, .T. ) ;
#20157=CARTESIAN_POINT ( 'NONE',  ( 0.3999999999999787059, -2.166079853131637645, -0.5407606602423824516 ) ) ;
#20161=DIRECTION ( 'NONE',  ( 0.4999551463232373427, -0.8660512985181134660, 0.000000000000000000 ) ) ;
#20164=CARTESIAN_POINT ( 'NONE',  ( 0.0006437153440169360308, -1.950600395569651369, -0.3015213215365759036 ) ) ;
#20168=CARTESIAN_POINT ( 'NONE',  ( 0.01374200611896923829, -1.689473050622495753, -0.6374908651714740193 ) ) ;
#20179=B_SPLINE_CURVE_WITH_KNOTS ( 'NONE', 3,
 ( #5424, #12026, #18388, #31544, #22515, #34642, #22312, #10551 ),
 .UNSPECIFIED., .F., .F.,
 ( 4, 2, 2, 4 ),
 ( 0.000000000000000000, 0.0002979882110954391503, 0.0005959764221908783006, 0.001191952844381744675 ),
 .UNSPECIFIED. ) ;
#20184=CARTESIAN_POINT ( 'NONE',  ( 0.3923243630925510872, -1.966611948492501316, -0.4968729097670202544 ) ) ;
#20203=CARTESIAN_POINT ( 'NONE',  ( 0.6335899703864817933, -1.596177751663389710, -0.4443638777805609119 ) ) ;
#20205=CARTESIAN_POINT ( 'NONE',  ( 0.3139458383965972321, -1.186049307970273858, -0.5155029497116575543 ) ) ;
#20214=CARTESIAN_POINT ( 'NONE',  ( 0.4209655804235680754, -1.724695148018828839, -0.5155029497116575543 ) ) ;
#20219=EDGE_CURVE ( 'NONE', #39958, #18975, #27842, .T. ) ;
#20242=CARTESIAN_POINT ( 'NONE',  ( 0.6445923553667830541, -1.422221564968557894, -0.6250000000000000000 ) ) ;
#20249=CARTESIAN_POINT ( 'NONE',  ( 0.03182674568678287019, -1.845213679978619403, -0.6754919065654066967 ) ) ;
#20251=CARTESIAN_POINT ( 'NONE',  ( 0.1991480113865206902, -2.054949600705703983, -0.6841806413415666421 ) ) ;
#20255=VERTEX_POINT ( 'NONE', #3155 ) ;
#20265=CARTESIAN_POINT ( 'NONE',  ( 0.6386829715298258936, -1.585896454429429392, -0.5957020523142678714 ) ) ;
#20270=EDGE_CURVE ( 'NONE', #9403, #16208, #6824, .T. ) ;
#20273=FACE_BOUND ( 'NONE', #2390, .T. ) ;
#20276=CARTESIAN_POINT ( 'NONE',  ( 0.04870459694554082897, -1.634362537833374818, -0.3424663835692939307 ) ) ;
#20277=CARTESIAN_POINT ( 'NONE',  ( 0.5605867575437347705, -1.621001144914625991, -0.5473203437262896820 ) ) ;
#20286=CARTESIAN_POINT ( 'NONE',  ( 0.3555724811773333660, -1.722873613718818975, -0.4858523300028667613 ) ) ;
#20290=EDGE_LOOP ( 'NONE', ( #12534, #27470, #16490, #40162 ) ) ;
#20297=CARTESIAN_POINT ( 'NONE',  ( 0.3545325911476117642, -1.827139849489873402, -0.4887235082572288780 ) ) ;
#20300=CARTESIAN_POINT ( 'NONE',  ( 0.1909286924077255032, -1.257064795538239022, -0.4125659523519144001 ) ) ;
#20301=ORIENTED_EDGE ( 'NONE', *, *, #12667, .F. ) ;
#20307=VERTEX_POINT ( 'NONE', #2677 ) ;
#20308=CARTESIAN_POINT ( 'NONE',  ( 0.4559719632891929830, -1.698713290701216350, -0.5155029497116575543 ) ) ;
#20314=( BOUNDED_SURFACE ( )  B_SPLINE_SURFACE ( 3, 2, ( 
 ( #5483, #2619, #27713 ),
 ( #7958, #17640, #14763 ),
 ( #33274, #8782, #24233 ),
 ( #24044, #27326, #39857 ) ),
 .UNSPECIFIED., .F., .F., .F. ) 
 B_SPLINE_SURFACE_WITH_KNOTS ( ( 4, 4 ),
 ( 3, 3 ),
 ( 0.001772558173964181201, 0.002238911299073404176 ),
 ( 0.000000000000000000, 1.000000000000000000 ),
 .UNSPECIFIED. ) 
 GEOMETRIC_REPRESENTATION_ITEM ( )  RATIONAL_B_SPLINE_SURFACE ( (
 ( 1.000000000000000000, 0.4461867090274512226, 1.000000000000000000),
 ( 1.000000000000000000, 0.4650446221766792454, 1.000000000000000000),
 ( 1.000000000000000000, 0.4838440862043267288, 1.000000000000000000),
 ( 1.000000000000000000, 0.5022121722253944931, 1.000000000000000000) ) ) 
 REPRESENTATION_ITEM ( '' )  SURFACE ( )  );
#20315=CARTESIAN_POINT ( 'NONE',  ( 0.3873689179426565432, -1.755636530304691689, -0.4507512901387274451 ) ) ;
#20322=DIRECTION ( 'NONE',  ( 0.8660512985181135770, 0.4999551463232370652, 0.000000000000000000 ) ) ;
#20326=CARTESIAN_POINT ( 'NONE',  ( 0.6163751027920442160, -1.623333184780543448, -0.5127481645887516093 ) ) ;
#20333=CARTESIAN_POINT ( 'NONE',  ( 0.5616368264987144920, -1.585529113978794591, -0.5096405943624068291 ) ) ;
#20339=VERTEX_POINT ( 'NONE', #37426 ) ;
#20342=CARTESIAN_POINT ( 'NONE',  ( 0.3740153396470256575, -1.763885720033750992, -0.5728934586661176276 ) ) ;
#20349=EDGE_LOOP ( 'NONE', ( #9895, #4529, #38380 ) ) ;
#20353=DIRECTION ( 'NONE',  ( 0.8660512985181135770, 0.4999551463232370652, 0.000000000000000000 ) ) ;
#20358=CARTESIAN_POINT ( 'NONE',  ( 0.1519263329367288584, -1.326104206834778143, -0.3123460348997796343 ) ) ;
#20361=CARTESIAN_POINT ( 'NONE',  ( 0.005199229819682637393, -1.801804716922572602, -0.6418151134160050564 ) ) ;
#20362=DIRECTION ( 'NONE',  ( 0.8660512985181132439, 0.4999551463232376758, 0.000000000000000000 ) ) ;
#20369=LINE ( 'NONE', #26153, #16053 ) ;
#20378=CARTESIAN_POINT ( 'NONE',  ( 0.4044319497911501027, -1.745786362538516823, -0.5913871057305363221 ) ) ;
#20387=FACE_OUTER_BOUND ( 'NONE', #21519, .T. ) ;
#20391=ORIENTED_EDGE ( 'NONE', *, *, #10693, .F. ) ;
#20414=CARTESIAN_POINT ( 'NONE',  ( 0.3999999999999788169, -2.042495778117167315, -0.2760839614659731378 ) ) ;
#20426=CARTESIAN_POINT ( 'NONE',  ( -2.112273405726188513E-14, -2.097675824466503691, -0.7286991843995640483 ) ) ;
#20429=CARTESIAN_POINT ( 'NONE',  ( 0.5494268846431774600, -1.650536850169864067, -0.5155029497116575543 ) ) ;
#20435=ORIENTED_EDGE ( 'NONE', *, *, #28868, .F. ) ;
#20436=CARTESIAN_POINT ( 'NONE',  ( -2.114758357748986011E-14, -2.063353092206445805, -0.6849817048858417579 ) ) ;
#20439=CARTESIAN_POINT ( 'NONE',  ( 0.1996617404659777606, -2.072851997774555421, -0.6888320016018293357 ) ) ;
#20442=CIRCLE ( 'NONE', #3363, 0.01499999999999997689 ) ;
#20444=ORIENTED_EDGE ( 'NONE', *, *, #9477, .T. ) ;
#20455=CARTESIAN_POINT ( 'NONE',  ( 0.6449069409503503936, -1.569348338378467211, -0.6050967068392708592 ) ) ;
#20456=VECTOR ( 'NONE', #15602, 39.37007874015748854 ) ;
#20470=CARTESIAN_POINT ( 'NONE',  ( 0.1511623735954494840, -1.326999691097843659, -0.3126952349615497728 ) ) ;
#20475=B_SPLINE_CURVE_WITH_KNOTS ( 'NONE', 3,
 ( #14425, #5168, #26806, #29887, #30267, #14243, #17719, #26393, #26608, #26994, #39523, #33167, #38923, #8267, #4972, #20839 ),
 .UNSPECIFIED., .F., .F.,
 ( 4, 2, 2, 2, 2, 2, 2, 4 ),
 ( 6.254634441385511532E-18, 0.0005051770138873787602, 0.001010354027774751232, 0.001515531041662123487, 0.002020708055549495959, 0.003031062083324246106, 0.003536239097211621180, 0.004041416111098996254 ),
 .UNSPECIFIED. ) ;
#20476=ORIENTED_EDGE ( 'NONE', *, *, #37872, .T. ) ;
#20490=CIRCLE ( 'NONE', #38857, 0.01000000000000002970 ) ;
#20499=CIRCLE ( 'NONE', #6676, 0.05000000000000000971 ) ;
#20505=DIRECTION ( 'NONE',  ( 0.000000000000000000, 0.000000000000000000, -1.000000000000000000 ) ) ;
#20510=ORIENTED_EDGE ( 'NONE', *, *, #31331, .T. ) ;
#20514=CARTESIAN_POINT ( 'NONE',  ( 0.3715710887045398647, -1.757287345216594909, -0.4310581837286736606 ) ) ;
#20520=CARTESIAN_POINT ( 'NONE',  ( 0.4584973792621093169, -1.056415778228135149, -0.5155029497116575543 ) ) ;
#20522=AXIS2_PLACEMENT_3D ( 'NONE', #25274, #38411, #34924 ) ;
#20523=CARTESIAN_POINT ( 'NONE',  ( 0.6300615908075114513, -1.604447140824846185, -0.5783957320051906770 ) ) ;
#20531=CARTESIAN_POINT ( 'NONE',  ( 0.5851536363839501265, -1.491939059043950522, -0.5963745793978136867 ) ) ;
#20540=FACE_OUTER_BOUND ( 'NONE', #20349, .T. ) ;
#20550=EDGE_CURVE ( 'NONE', #7698, #30237, #6761, .T. ) ;
#20553=CARTESIAN_POINT ( 'NONE',  ( 0.4203826191881492313, -1.700944664958275343, -0.4172566670736511107 ) ) ;
#20560=FACE_BOUND ( 'NONE', #2061, .T. ) ;
#20564=CARTESIAN_POINT ( 'NONE',  ( 0.1615127891059936760, -1.277671110434810631, -0.7015317095148801974 ) ) ;
#20567=EDGE_CURVE ( 'NONE', #9543, #19186, #25892, .T. ) ;
#20584=CARTESIAN_POINT ( 'NONE',  ( 0.3827280947354409490, -1.758315590366831049, -0.5716786788641499140 ) ) ;
#20585=CIRCLE ( 'NONE', #12660, 0.2000000000000000666 ) ;
#20589=CIRCLE ( 'NONE', #9419, 0.01000000000000002970 ) ;
#20590=ORIENTED_EDGE ( 'NONE', *, *, #37343, .T. ) ;
#20619=CARTESIAN_POINT ( 'NONE',  ( 0.1999999999999794720, -2.097675824466503247, -0.2588528740066096678 ) ) ;
#20621=CARTESIAN_POINT ( 'NONE',  ( 0.3990506063816511295, -1.683314032604188437, -0.4045594003095706048 ) ) ;
#20624=CARTESIAN_POINT ( 'NONE',  ( 0.3478153622845648885, -1.628211818192446536, -0.6007519914469682254 ) ) ;
#20627=CARTESIAN_POINT ( 'NONE',  ( 0.1999999999999789724, -2.097675824466503247, -0.2588528740066097233 ) ) ;
#20628=VECTOR ( 'NONE', #4292, 39.37007874015748854 ) ;
#20641=CARTESIAN_POINT ( 'NONE',  ( 0.09999999999998190892, -1.871552131921257578, -0.6463968910507320587 ) ) ;
#20644=CARTESIAN_POINT ( 'NONE',  ( 0.2169591561341989161, -1.302156274398155622, -0.6184399470714007085 ) ) ;
#20646=ORIENTED_EDGE ( 'NONE', *, *, #14754, .T. ) ;
#20647=CARTESIAN_POINT ( 'NONE',  ( 0.5029538533377585496, -1.673443447161921727, -0.4264433612092255466 ) ) ;
#20649=ORIENTED_EDGE ( 'NONE', *, *, #24266, .F. ) ;
#20651=CARTESIAN_POINT ( 'NONE',  ( 0.1379511725373750997, -1.300921670157717758, -0.6912193855582036139 ) ) ;
#20662=CARTESIAN_POINT ( 'NONE',  ( 0.1999999922267132468, -2.089163595796008188, -0.2938764050442146392 ) ) ;
#20675=CARTESIAN_POINT ( 'NONE',  ( 0.4484726360943441792, -1.685722521223443904, -0.5155029497116575543 ) ) ;
#20680=CARTESIAN_POINT ( 'NONE',  ( 0.4299129845042397591, -1.697471419175033747, -0.5152995808109321896 ) ) ;
#20687=CARTESIAN_POINT ( 'NONE',  ( 0.09620807403327706619, -1.426205906121508882, -0.3356627542665827635 ) ) ;
#20689=ORIENTED_EDGE ( 'NONE', *, *, #36086, .T. ) ;
#20691=CARTESIAN_POINT ( 'NONE',  ( 0.4534978277988769846, -1.047755265242954037, -0.5155029497116575543 ) ) ;
#20696=B_SPLINE_CURVE_WITH_KNOTS ( 'NONE', 1,
 ( #11041, #20300, #39408, #23414 ),
 .UNSPECIFIED., .F., .F.,
 ( 2, 1, 1, 2 ),
 ( -0.0007619999999999984642, 2.276824562219559311E-18, 0.0007620000000000012831, 0.001523999999999997145 ),
 .UNSPECIFIED. ) ;
#20707=CARTESIAN_POINT ( 'NONE',  ( 0.3546785580517292646, -1.844992007381027976, -0.4891695103279160572 ) ) ;
#20708=CARTESIAN_POINT ( 'NONE',  ( 0.5744812595043889969, -1.541517170152952643, -0.5460780551203860966 ) ) ;
#20710=AXIS2_PLACEMENT_3D ( 'NONE', #8702, #24571, #1954 ) ;
#20720=ORIENTED_EDGE ( 'NONE', *, *, #38971, .F. ) ;
#20730=CARTESIAN_POINT ( 'NONE',  ( 0.3967637807842907538, -1.750213052463736485, -0.4985867268025130916 ) ) ;
#20732=EDGE_CURVE ( 'NONE', #22699, #27179, #24241, .T. ) ;
#20735=CARTESIAN_POINT ( 'NONE',  ( 0.3674370130824703429, -1.724856795990272973, -0.6064096210563775236 ) ) ;
#20737=AXIS2_PLACEMENT_3D ( 'NONE', #20776, #10483, #20362 ) ;
#20739=ADVANCED_FACE ( 'NONE', ( #17845 ), #19968, .T. ) ;
#20740=CARTESIAN_POINT ( 'NONE',  ( 0.5771669516282522672, -1.610595408416737540, -0.5496873730034127492 ) ) ;
#20742=CARTESIAN_POINT ( 'NONE',  ( 0.1306785186278567601, -1.354088256797956191, -0.7085892327543563685 ) ) ;
#20750=CARTESIAN_POINT ( 'NONE',  ( 0.5728032096484048097, -1.543894942757779720, -0.5357990152665924599 ) ) ;
#20765=CARTESIAN_POINT ( 'NONE',  ( 0.4287117948289022595, -1.695887552032223411, -0.4140898068348377037 ) ) ;
#20770=DIRECTION ( 'NONE',  ( 0.000000000000000000, 0.000000000000000000, -1.000000000000000000 ) ) ;
#20773=CIRCLE ( 'NONE', #24069, 0.1033070866141732325 ) ;
#20774=VERTEX_POINT ( 'NONE', #27337 ) ;
#20776=CARTESIAN_POINT ( 'NONE',  ( 0.4159916692016358830, -1.069406866067976081, -0.5155029497116575543 ) ) ;
#20797=CARTESIAN_POINT ( 'NONE',  ( 0.3964872829018378786, -1.750372669497358258, -0.5853913325796881173 ) ) ;
#20802=ORIENTED_EDGE ( 'NONE', *, *, #13480, .T. ) ;
#20818=CARTESIAN_POINT ( 'NONE',  ( 0.3999999999999787059, -2.097675824466503691, -0.2588528740066097233 ) ) ;
#20821=EDGE_LOOP ( 'NONE', ( #2284, #21575, #22653, #15815 ) ) ;
#20829=CARTESIAN_POINT ( 'NONE',  ( 0.4111244031346745209, -1.715100544966072116, -0.4234454618225184652 ) ) ;
#20830=CARTESIAN_POINT ( 'NONE',  ( 0.6784119790018648954, -1.437364601474310222, -0.5155029497116575543 ) ) ;
#20836=DIRECTION ( 'NONE',  ( 0.4999551463232373427, -0.8660512985181134660, 0.000000000000000000 ) ) ;
#20839=CARTESIAN_POINT ( 'NONE',  ( 0.6335899703865320864, -1.596177751663357736, -0.4443638777805991591 ) ) ;
#20850=CARTESIAN_POINT ( 'NONE',  ( 0.3526790567758040229, -1.721859164019411637, -0.5374078869160439087 ) ) ;
#20855=CARTESIAN_POINT ( 'NONE',  ( 0.3695052819757338458, -1.758428263776098843, -0.4278193900811941286 ) ) ;
#20856=CARTESIAN_POINT ( 'NONE',  ( 0.3941594819206604150, -1.750901474553208548, -0.4851235437278881846 ) ) ;
#20858=CIRCLE ( 'NONE', #21506, 0.01500000000000000638 ) ;
#20864=CARTESIAN_POINT ( 'NONE',  ( 0.1323247281835593092, -1.307327334972417265, -0.7167432404901448173 ) ) ;
#20882=CARTESIAN_POINT ( 'NONE',  ( 0.4125610653371456493, -1.705653404133229634, -0.6104586881356433015 ) ) ;
#20883=CARTESIAN_POINT ( 'NONE',  ( 0.3757471142192211344, -1.766731021160330428, -0.5680748514784754732 ) ) ;
#20887=CARTESIAN_POINT ( 'NONE',  ( 0.2842326993136112812, -1.549395603922541831, -0.7208999815284790058 ) ) ;
#20893=LINE ( 'NONE', #33414, #16002 ) ;
#20894=CARTESIAN_POINT ( 'NONE',  ( 0.4615400415883951779, -1.655602614066592260, -0.3952887662183799389 ) ) ;
#20897=DIRECTION ( 'NONE',  ( 0.8660512985181124668, 0.4999551463232388415, 0.000000000000000000 ) ) ;
#20898=AXIS2_PLACEMENT_3D ( 'NONE', #31071, #25101, #258 ) ;
#20902=CARTESIAN_POINT ( 'NONE',  ( 0.3984114568195522010, -1.599003643269838904, -0.5155029497116575543 ) ) ;
#20907=CARTESIAN_POINT ( 'NONE',  ( 0.3812071769896587803, -1.763750790280042002, -0.4536492913031247021 ) ) ;
#20910=ADVANCED_FACE ( 'NONE', ( #10416 ), #29186, .T. ) ;
#20912=CARTESIAN_POINT ( 'NONE',  ( 0.3999999999999787059, -2.097675824466503691, -0.5196396315034578217 ) ) ;
#20915=ORIENTED_EDGE ( 'NONE', *, *, #19499, .T. ) ;
#20922=FACE_OUTER_BOUND ( 'NONE', #20290, .T. ) ;
#20925=CARTESIAN_POINT ( 'NONE',  ( 0.3883123751121188572, -1.905506865536376493, -0.5089180440232635716 ) ) ;
#20936=CARTESIAN_POINT ( 'NONE',  ( 0.5762373068470778570, -1.611384107284732137, -0.4870925628601384672 ) ) ;
#20956=ADVANCED_FACE ( 'NONE', ( #16593 ), #22633, .T. ) ;
#20960=DIRECTION ( 'NONE',  ( -0.8660512985181132439, -0.4999551463232374537, 0.000000000000000000 ) ) ;
#20961=ORIENTED_EDGE ( 'NONE', *, *, #7371, .T. ) ;
#20967=ORIENTED_EDGE ( 'NONE', *, *, #15369, .F. ) ;
#20988=CARTESIAN_POINT ( 'NONE',  ( 0.3769667398768312694, -1.761641512302731138, -0.5722193458963301671 ) ) ;
#20991=ORIENTED_EDGE ( 'NONE', *, *, #11200, .T. ) ;
#21005=CARTESIAN_POINT ( 'NONE',  ( 0.1909286924077255032, -1.257064795538239022, -0.3194753470178354759 ) ) ;
#21007=CARTESIAN_POINT ( 'NONE',  ( 0.2624674271213696675, -1.608515928549841822, -0.3523228403142553145 ) ) ;
#21010=CARTESIAN_POINT ( 'NONE',  ( 0.2059273467974227778, -1.283046334493782359, -0.7137159211901564770 ) ) ;
#21014=CYLINDRICAL_SURFACE ( 'NONE', #8636, 0.04330708661417343591 ) ;
#21015=CARTESIAN_POINT ( 'NONE',  ( 0.1809966328114128442, -1.222385076516254054, -0.5155029497116575543 ) ) ;
#21020=DIRECTION ( 'NONE',  ( 0.8660512985181134660, 0.4999551463232372317, 0.000000000000000000 ) ) ;
#21025=CARTESIAN_POINT ( 'NONE',  ( 0.3884858366675985053, -1.658196668589008382, -0.4078262653169359431 ) ) ;
#21033=B_SPLINE_CURVE_WITH_KNOTS ( 'NONE', 3,
 ( #8085, #20662, #11384, #5001 ),
 .UNSPECIFIED., .F., .F.,
 ( 4, 4 ),
 ( -6.000000000270394880E-08, 0.001522235525887978384 ),
 .UNSPECIFIED. ) ;
#21041=CARTESIAN_POINT ( 'NONE',  ( 0.3695052819757338458, -1.758428263776098621, -0.4278193900811942396 ) ) ;
#21042=CARTESIAN_POINT ( 'NONE',  ( 0.3839459786000343211, -1.830045642923745941, -0.5208591197437392184 ) ) ;
#21043=ORIENTED_EDGE ( 'NONE', *, *, #34585, .T. ) ;
#21047=CARTESIAN_POINT ( 'NONE',  ( 0.1512218670170321910, -1.285950302238538345, -0.7264183920055864441 ) ) ;
#21056=DIRECTION ( 'NONE',  ( -0.4999551463232372317, 0.8660512985181135770, -0.000000000000000000 ) ) ;
#21066=ORIENTED_EDGE ( 'NONE', *, *, #39929, .T. ) ;
#21076=CARTESIAN_POINT ( 'NONE',  ( 0.1363389461966361682, -1.302049561124409838, -0.6870159582249631969 ) ) ;
#21081=CARTESIAN_POINT ( 'NONE',  ( 0.1862037248930970834, -1.944818472745344584, -0.6629142544188069142 ) ) ;
#21084=DIRECTION ( 'NONE',  ( -0.4999551463232372317, 0.8660512985181135770, -0.000000000000000000 ) ) ;
#21089=DIRECTION ( 'NONE',  ( 0.8660512985181126888, 0.4999551463232385085, 0.000000000000000000 ) ) ;
#21114=AXIS2_PLACEMENT_3D ( 'NONE', #40572, #846, #38649 ) ;
#21116=ORIENTED_EDGE ( 'NONE', *, *, #33780, .T. ) ;
#21117=CARTESIAN_POINT ( 'NONE',  ( 0.1994740068363775598, -2.042640899752901085, -0.2765909798240092643 ) ) ;
#21131=CARTESIAN_POINT ( 'NONE',  ( 0.6103063930502474754, -1.581064649372068143, -0.5712514945930247112 ) ) ;
#21139=CARTESIAN_POINT ( 'NONE',  ( 0.3746913172999769004, -1.707304890831578659, -0.6133074500811318552 ) ) ;
#21140=CARTESIAN_POINT ( 'NONE',  ( 0.3999999999999787059, -2.097675824466503691, -0.4688691127277797022 ) ) ;
#21142=PLANE ( 'NONE',  #33796 ) ;
#21163=CARTESIAN_POINT ( 'NONE',  ( 0.1424029337235096226, -1.400533250147911746, -0.3244367222852112542 ) ) ;
#21167=ORIENTED_EDGE ( 'NONE', *, *, #36924, .T. ) ;
#21172=CARTESIAN_POINT ( 'NONE',  ( 0.5351545789516157781, -1.658325038984146405, -0.5717893983912645250 ) ) ;
#21198=EDGE_LOOP ( 'NONE', ( #21777, #21470, #29241, #21628 ) ) ;
#21201=EDGE_LOOP ( 'NONE', ( #34854, #9966, #20444, #8084 ) ) ;
#21222=CARTESIAN_POINT ( 'NONE',  ( 0.3859792353386746755, -1.738628747592057211, -0.4467605215525291551 ) ) ;
#21227=EDGE_CURVE ( 'NONE', #21815, #21610, #16077, .T. ) ;
#21236=ADVANCED_FACE ( 'NONE', ( #32418 ), #973, .T. ) ;
#21238=AXIS2_PLACEMENT_3D ( 'NONE', #15814, #38629, #28366 ) ;
#21246=AXIS2_PLACEMENT_3D ( 'NONE', #2315, #5581, #24927 ) ;
#21248=CARTESIAN_POINT ( 'NONE',  ( 0.3494216204373458701, -1.697238143783349695, -0.4672182159968431558 ) ) ;
#21256=ORIENTED_EDGE ( 'NONE', *, *, #25102, .T. ) ;
#21265=ORIENTED_EDGE ( 'NONE', *, *, #2167, .T. ) ;
#21271=DIRECTION ( 'NONE',  ( 0.5154377295227949851, -0.8569270371416612964, 0.000000000000000000 ) ) ;
#21292=CARTESIAN_POINT ( 'NONE',  ( 0.4250902526234662804, -1.669131906446581270, -0.3966677131679292034 ) ) ;
#21294=ADVANCED_FACE ( 'NONE', ( #8738 ), #29870, .T. ) ;
#21298=EDGE_LOOP ( 'NONE', ( #19633, #34955, #22179, #19475 ) ) ;
#21299=DIRECTION ( 'NONE',  ( -0.9739500565613357086, -0.01953031614056561713, 0.2259200169874744923 ) ) ;
#21307=ORIENTED_EDGE ( 'NONE', *, *, #9958, .F. ) ;
#21308=CARTESIAN_POINT ( 'NONE',  ( -2.106244131833921715E-14, -2.101105179789023669, -0.6980525405474647949 ) ) ;
#21314=CARTESIAN_POINT ( 'NONE',  ( 0.1965730157716580884, -2.006121492102985293, -0.3172943880574278785 ) ) ;
#21316=DIRECTION ( 'NONE',  ( 0.4999551463232373427, -0.8660512985181134660, 0.000000000000000000 ) ) ;
#21320=EDGE_CURVE ( 'NONE', #22853, #9058, #21364, .T. ) ;
#21332=CARTESIAN_POINT ( 'NONE',  ( 0.1990989110834594789, -2.031922935036753142, -0.2796108765274104013 ) ) ;
#21333=AXIS2_PLACEMENT_3D ( 'NONE', #32649, #17017, #4453 ) ;
#21337=AXIS2_PLACEMENT_3D ( 'NONE', #17670, #36793, #15002 ) ;
#21338=AXIS2_PLACEMENT_3D ( 'NONE', #11036, #4437, #1194 ) ;
#21339=CARTESIAN_POINT ( 'NONE',  ( 0.3699999999999786793, -2.097675824466503691, -0.4688691127277797022 ) ) ;
#21343=AXIS2_PLACEMENT_3D ( 'NONE', #16556, #965, #26044 ) ;
#21347=CARTESIAN_POINT ( 'NONE',  ( 0.4768848212686895849, -1.682051206446435243, -0.4156371400837835517 ) ) ;
#21349=CARTESIAN_POINT ( 'NONE',  ( 0.6598601525370707543, -1.502959539027199254, -0.4120828692936505666 ) ) ;
#21350=FACE_OUTER_BOUND ( 'NONE', #29693, .T. ) ;
#21352=DIRECTION ( 'NONE',  ( 0.2067069058495553946, 0.1193280138680803265, 0.9710989033977963647 ) ) ;
#21356=CARTESIAN_POINT ( 'NONE',  ( 0.3992403239432279483, -1.683235622436119128, -0.6263438071736162627 ) ) ;
#21359=FACE_OUTER_BOUND ( 'NONE', #32421, .T. ) ;
#21362=ORIENTED_EDGE ( 'NONE', *, *, #39400, .F. ) ;
#21363=CARTESIAN_POINT ( 'NONE',  ( 0.4714772250923787711, -1.069474201788713108, -0.6070170271373026560 ) ) ;
#21364=CIRCLE ( 'NONE', #28578, 0.2000000000000000666 ) ;
#21391=CARTESIAN_POINT ( 'NONE',  ( 0.1348608168514592864, -1.985670591994486367, -0.3242396390482729096 ) ) ;
#21400=CARTESIAN_POINT ( 'NONE',  ( 0.1601079512667811788, -1.855210257011521202, -0.6514173194225818531 ) ) ;
#21410=( BOUNDED_SURFACE ( )  B_SPLINE_SURFACE ( 3, 2, ( 
 ( #2428, #30997, #14965 ),
 ( #11865, #24433, #15370 ),
 ( #36965, #8784, #37179 ),
 ( #8996, #31219, #21561 ),
 ( #40467, #21750, #34080 ),
 ( #24849, #5885, #18445 ) ),
 .UNSPECIFIED., .F., .F., .F. ) 
 B_SPLINE_SURFACE_WITH_KNOTS ( ( 4, 2, 4 ),
 ( 3, 3 ),
 ( -2.168404344971008868E-19, 0.001064962965551008965, 0.002129925931102017930 ),
 ( 0.000000000000000000, 1.000000000000000000 ),
 .UNSPECIFIED. ) 
 GEOMETRIC_REPRESENTATION_ITEM ( )  RATIONAL_B_SPLINE_SURFACE ( (
 ( 1.000000000000000000, 0.8067368806807361237, 1.000000000000000000),
 ( 1.000000000000000000, 0.8240497396349234505, 1.000000000000000000),
 ( 1.000000000000000000, 0.8393628034582739650, 1.000000000000000000),
 ( 1.000000000000000000, 0.8610007399255795724, 1.000000000000000000),
 ( 1.000000000000000000, 0.8667168599303205490, 1.000000000000000000),
 ( 1.000000000000000000, 0.8659230874819840995, 1.000000000000000000) ) ) 
 REPRESENTATION_ITEM ( '' )  SURFACE ( )  );
#21413=CARTESIAN_POINT ( 'NONE',  ( 0.4634865284762403892, -1.134362257022321518, -0.3648515278348755109 ) ) ;
#21415=B_SPLINE_CURVE_WITH_KNOTS ( 'NONE', 3,
 ( #15445, #27997, #24717, #9464, #37247, #6169, #12548, #6376 ),
 .UNSPECIFIED., .F., .F.,
 ( 4, 2, 2, 4 ),
 ( 0.000000000000000000, 0.0001840052804137891915, 0.0003680105608275783830, 0.0007360211216551754143 ),
 .UNSPECIFIED. ) ;
#21428=ORIENTED_EDGE ( 'NONE', *, *, #27040, .F. ) ;
#21437=ORIENTED_EDGE ( 'NONE', *, *, #11506, .T. ) ;
#21448=CARTESIAN_POINT ( 'NONE',  ( 0.3782034578509241851, -1.662383355070864654, -0.6252036213791186681 ) ) ;
#21454=CARTESIAN_POINT ( 'NONE',  ( 0.1784968570797965948, -1.218054820023663831, -0.5155029497116575543 ) ) ;
#21459=ORIENTED_EDGE ( 'NONE', *, *, #18593, .F. ) ;
#21462=CARTESIAN_POINT ( 'NONE',  ( 0.3437180095255871204, -1.654344192420559967, -0.4444229222738684815 ) ) ;
#21470=ORIENTED_EDGE ( 'NONE', *, *, #22995, .T. ) ;
#21472=DIRECTION ( 'NONE',  ( -0.4999551463232373427, 0.8660512985181134660, -0.000000000000000000 ) ) ;
#21473=DIRECTION ( 'NONE',  ( 1.000000000000000000, 0.000000000000000000, 0.000000000000000000 ) ) ;
#21483=CARTESIAN_POINT ( 'NONE',  ( 0.1909286924077255032, -1.257064795538239022, -0.7462941026102624109 ) ) ;
#21498=FACE_OUTER_BOUND ( 'NONE', #36542, .T. ) ;
#21504=EDGE_CURVE ( 'NONE', #18975, #34456, #7531, .T. ) ;
#21506=AXIS2_PLACEMENT_3D ( 'NONE', #22463, #7012, #34782 ) ;
#21507=CARTESIAN_POINT ( 'NONE',  ( 0.1804782205544497031, -1.898145329168058781, -0.6575140397730463437 ) ) ;
#21511=ORIENTED_EDGE ( 'NONE', *, *, #37564, .F. ) ;
#21519=EDGE_LOOP ( 'NONE', ( #23167, #6522, #6401, #22767 ) ) ;
#21523=CARTESIAN_POINT ( 'NONE',  ( 0.3758909033093429386, -1.726409976104785526, -0.3411215252611376481 ) ) ;
#21530=EDGE_CURVE ( 'NONE', #13465, #17453, #5567, .T. ) ;
#21536=CARTESIAN_POINT ( 'NONE',  ( 0.3699999999999783462, -2.097675824466504135, -0.5196396315034577107 ) ) ;
#21539=CARTESIAN_POINT ( 'NONE',  ( 0.5053588047760252389, -1.583603243833816565, -0.5401600205605632254 ) ) ;
#21540=CARTESIAN_POINT ( 'NONE',  ( 0.3942985600065282425, -1.769819547351404454, -0.5278219303748407087 ) ) ;
#21541=ADVANCED_FACE ( 'NONE', ( #14403 ), #12806, .F. ) ;
#21552=CARTESIAN_POINT ( 'NONE',  ( 0.6469206375993061808, -1.465334083252977093, -0.4112288931193002761 ) ) ;
#21559=CARTESIAN_POINT ( 'NONE',  ( 0.3975019948776055134, -1.696135473892855572, -0.6064691975985911920 ) ) ;
#21560=CARTESIAN_POINT ( 'NONE',  ( 0.3623221021055049729, -1.968029003640406449, -0.5215600955572180508 ) ) ;
#21561=CARTESIAN_POINT ( 'NONE',  ( 0.4356923561510381848, -1.693540257987297792, -0.6182874616928464295 ) ) ;
#21563=CARTESIAN_POINT ( 'NONE',  ( 0.5378106547832601780, -1.668789341594314024, -0.5701368517888846243 ) ) ;
#21569=EDGE_LOOP ( 'NONE', ( #37565, #19126, #27137, #3059 ) ) ;
#21574=CARTESIAN_POINT ( 'NONE',  ( 0.1999999999999789724, -2.183180860297921466, -0.7437760292030870524 ) ) ;
#21575=ORIENTED_EDGE ( 'NONE', *, *, #1678, .T. ) ;
#21576=EDGE_CURVE ( 'NONE', #5500, #17083, #34525, .T. ) ;
#21581=CARTESIAN_POINT ( 'NONE',  ( 0.4634712904840411762, -1.711704060178987241, -0.5155029497116575543 ) ) ;
#21587=CARTESIAN_POINT ( 'NONE',  ( 0.1357105165892661391, -2.051761019322187796, -0.3074898295655506542 ) ) ;
#21589=CARTESIAN_POINT ( 'NONE',  ( 0.01393220626005791697, -1.691440753321579615, -0.3707258672847664194 ) ) ;
#21596=CARTESIAN_POINT ( 'NONE',  ( 0.1974716765470868052, -1.244701664176973255, -0.7187326247832954706 ) ) ;
#21603=CARTESIAN_POINT ( 'NONE',  ( 0.3439431471759914483, -1.238012385881360533, -0.5155029497116575543 ) ) ;
#21610=VERTEX_POINT ( 'NONE', #15225 ) ;
#21626=DIRECTION ( 'NONE',  ( 0.4999551463232372317, -0.8660512985181135770, 0.000000000000000000 ) ) ;
#21628=ORIENTED_EDGE ( 'NONE', *, *, #3123, .T. ) ;
#21629=ADVANCED_FACE ( 'NONE', ( #3098 ), #11409, .T. ) ;
#21630=CARTESIAN_POINT ( 'NONE',  ( 0.4688459138424371786, -1.061988423737608045, -0.4248180574663140141 ) ) ;
#21637=B_SPLINE_CURVE_WITH_KNOTS ( 'NONE', 3,
 ( #9390, #21967, #34496, #6308 ),
 .UNSPECIFIED., .F., .F.,
 ( 4, 4 ),
 ( 0.000000000000000000, 0.001175067160604181338 ),
 .UNSPECIFIED. ) ;
#21641=( BOUNDED_SURFACE ( )  B_SPLINE_SURFACE ( 3, 2, ( 
 ( #32574, #14448, #39543 ),
 ( #20436, #10776, #35871 ),
 ( #13840, #32768, #33385 ),
 ( #7684, #17351, #39354 ),
 ( #36680, #38947, #29694 ),
 ( #11175, #17743, #20249 ),
 ( #4570, #11377, #39163 ),
 ( #23549, #33190, #30293 ),
 ( #26827, #17142, #23945 ),
 ( #36259, #14056, #30103 ),
 ( #17561, #23349, #23732 ),
 ( #1536, #8486, #1751 ),
 ( #5387, #29910, #5188 ),
 ( #26635, #17949, #2125 ),
 ( #33574, #26414, #4994 ),
 ( #36479, #36066, #14262 ),
 ( #1934, #24156, #27016 ),
 ( #10992, #7865, #14659 ),
 ( #8292, #32973, #27228 ),
 ( #1333, #4777, #8077 ),
 ( #20651, #20864, #39764 ),
 ( #11594, #21047, #27626 ),
 ( #12390, #40369, #18159 ),
 ( #22088, #11783, #9096 ) ),
 .UNSPECIFIED., .F., .F., .F. ) 
 B_SPLINE_SURFACE_WITH_KNOTS ( ( 4, 2, 2, 2, 2, 2, 2, 2, 2, 2, 2, 4 ),
 ( 3, 3 ),
 ( 0.004472361800415559571, 0.007241614148789993731, 0.01001086649716442789, 0.01278011884553886292, 0.01554937119391329794, 0.01831862354228773471, 0.02108787589066216800, 0.02247250206484938465, 0.02385712823903660129, 0.02454944132613021135, 0.02524175441322381794, 0.02662638058741103458 ),
 ( 0.000000000000000000, 1.000000000000000000 ),
 .UNSPECIFIED. ) 
 GEOMETRIC_REPRESENTATION_ITEM ( )  RATIONAL_B_SPLINE_SURFACE ( (
 ( 1.000000000000000000, 0.7071530416912251704, 1.000000000000000000),
 ( 1.000000000000000000, 0.7073709362457231142, 1.000000000000000000),
 ( 1.000000000000000000, 0.7092808763967833885, 1.000000000000000000),
 ( 1.000000000000000000, 0.7141524243381439652, 1.000000000000000000),
 ( 1.000000000000000000, 0.7171571039999593555, 1.000000000000000000),
 ( 1.000000000000000000, 0.7235522545071346734, 1.000000000000000000),
 ( 1.000000000000000000, 0.7269749645788134984, 1.000000000000000000),
 ( 1.000000000000000000, 0.7340382794361808294, 1.000000000000000000),
 ( 1.000000000000000000, 0.7376893573657878900, 1.000000000000000000),
 ( 1.000000000000000000, 0.7449955946419650754, 1.000000000000000000),
 ( 1.000000000000000000, 0.7486754894461632448, 1.000000000000000000),
 ( 1.000000000000000000, 0.7552984250705360170, 1.000000000000000000),
 ( 1.000000000000000000, 0.7583398789584828714, 1.000000000000000000),
 ( 1.000000000000000000, 0.7606811803337633071, 1.000000000000000000),
 ( 1.000000000000000000, 0.7610729208801710888, 1.000000000000000000),
 ( 1.000000000000000000, 0.7601897444684649896, 1.000000000000000000),
 ( 1.000000000000000000, 0.7589468570669724024, 1.000000000000000000),
 ( 1.000000000000000000, 0.7545561764466856003, 1.000000000000000000),
 ( 1.000000000000000000, 0.7526619229726708715, 1.000000000000000000),
 ( 1.000000000000000000, 0.7476192217998193223, 1.000000000000000000),
 ( 1.000000000000000000, 0.7444481429157411290, 1.000000000000000000),
 ( 1.000000000000000000, 0.7327145509101834486, 1.000000000000000000),
 ( 1.000000000000000000, 0.7217852786214301597, 1.000000000000000000),
 ( 1.000000000000000000, 0.7071189998922933206, 1.000000000000000000) ) ) 
 REPRESENTATION_ITEM ( '' )  SURFACE ( )  );
#21643=CARTESIAN_POINT ( 'NONE',  ( 0.4634712904840415093, -1.711704060178988129, -0.5155029497116575543 ) ) ;
#21644=B_SPLINE_CURVE_WITH_KNOTS ( 'NONE', 3,
 ( #18476, #31249, #30829, #24680, #2460, #5917, #28157, #2852, #14996, #33705, #15188, #27549, #27957, #15401, #40497, #3251 ),
 .UNSPECIFIED., .F., .F.,
 ( 4, 2, 2, 2, 2, 2, 2, 4 ),
 ( 0.000000000000000000, 0.001141425056121503443, 0.001712137584182261887, 0.002282850112243020764, 0.002853562640303779208, 0.003424275168364537651, 0.003994987696425296095, 0.004565700224486055406 ),
 .UNSPECIFIED. ) ;
#21660=VERTEX_POINT ( 'NONE', #1063 ) ;
#21663=CARTESIAN_POINT ( 'NONE',  ( 0.3621938380462905172, -1.694500576257093494, -0.5862319126744306441 ) ) ;
#21666=DIRECTION ( 'NONE',  ( 0.4999551463232373427, -0.8660512985181134660, 0.000000000000000000 ) ) ;
#21669=CARTESIAN_POINT ( 'NONE',  ( 0.2211959769661342168, -1.309495541150525799, -0.2869361388274796476 ) ) ;
#21681=CARTESIAN_POINT ( 'NONE',  ( 0.001114027946886548409, -1.914171052033790899, -0.6529051036212328851 ) ) ;
#21687=CARTESIAN_POINT ( 'NONE',  ( 0.1779790066342687160, -1.874427033017872279, -0.6554133151439877070 ) ) ;
#21699=ORIENTED_EDGE ( 'NONE', *, *, #26108, .F. ) ;
#21702=DIRECTION ( 'NONE',  ( 0.8056764635542885689, 0.4651018882076579097, -0.3668319365326945247 ) ) ;
#21704=CARTESIAN_POINT ( 'NONE',  ( 0.3727196660074906243, -1.733127303661048613, -0.5289265956312534378 ) ) ;
#21705=DIRECTION ( 'NONE',  ( -0.8660512985181130219, -0.4999551463232380644, 0.000000000000000000 ) ) ;
#21715=DIRECTION ( 'NONE',  ( -0.2221717918550268900, -0.8554093761208125812, -0.4678829919419264516 ) ) ;
#21721=CARTESIAN_POINT ( 'NONE',  ( 0.3997154711467377219, -2.078397263467336664, -0.4724987659684973806 ) ) ;
#21730=B_SPLINE_CURVE_WITH_KNOTS ( 'NONE', 3,
 ( #15706, #40600, #37308, #15519, #30739, #15095, #28252, #37498, #5823, #116, #8515, #9120 ),
 .UNSPECIFIED., .F., .F.,
 ( 4, 2, 2, 2, 2, 4 ),
 ( 0.002469872543621277027, 0.003821559213351475789, 0.005173245883081675420, 0.006524932552811874183, 0.007200775887676973130, 0.007876619222542072946 ),
 .UNSPECIFIED. ) ;
#21735=CIRCLE ( 'NONE', #1404, 0.03000000000000006134 ) ;
#21736=CARTESIAN_POINT ( 'NONE',  ( 0.5838521633088137319, -1.602265608861538793, -0.4542598492692566658 ) ) ;
#21744=CARTESIAN_POINT ( 'NONE',  ( 0.3599187094839055856, -1.738735253168089967, -0.5101712951092032267 ) ) ;
#21745=CARTESIAN_POINT ( 'NONE',  ( 0.3819143772994754715, -1.729703839012011857, -0.5841330926933957501 ) ) ;
#21750=CARTESIAN_POINT ( 'NONE',  ( 0.4179778656386031743, -1.682263187816546157, -0.6165510159742800811 ) ) ;
#21752=EDGE_LOOP ( 'NONE', ( #3573, #26079, #1974, #25190 ) ) ;
#21759=DIRECTION ( 'NONE',  ( 0.000000000000000000, 0.000000000000000000, 1.000000000000000000 ) ) ;
#21771=CARTESIAN_POINT ( 'NONE',  ( 0.1909286924077255032, -1.257064795538239022, -0.3194753470178354759 ) ) ;
#21776=ORIENTED_EDGE ( 'NONE', *, *, #24977, .F. ) ;
#21777=ORIENTED_EDGE ( 'NONE', *, *, #29736, .T. ) ;
#21781=CARTESIAN_POINT ( 'NONE',  ( 0.2060189241777141689, -2.107936428766273629, -0.2870436526301869407 ) ) ;
#21785=TOROIDAL_SURFACE ( 'NONE', #11928, 0.2200000000000000566, 0.02999999999999999889 ) ;
#21788=FACE_OUTER_BOUND ( 'NONE', #39010, .T. ) ;
#21796=LINE ( 'NONE', #15202, #33053 ) ;
#21807=B_SPLINE_SURFACE_WITH_KNOTS ( 'NONE', 1, 3, ( 
 ( #40423, #9343, #15331, #30563 ),
 ( #18405, #39817, #2386, #15115 ),
 ( #37139, #27675, #11642, #14926 ),
 ( #33855, #2993, #30957, #2782 ) ),
 .UNSPECIFIED., .F., .F., .F.,
 ( 2, 1, 1, 2 ),
 ( 4, 4 ),
 ( -1.012000000000000233, 0.000000000000000000, 1.000000000000000000, 2.018000000000001126 ),
 ( -0.005833846140041338939, 0.005833846140041338071 ),
 .UNSPECIFIED. ) ;
#21815=VERTEX_POINT ( 'NONE', #5904 ) ;
#21816=VECTOR ( 'NONE', #3194, 39.37007874015748143 ) ;
#21822=CARTESIAN_POINT ( 'NONE',  ( 0.5087011370554738177, -1.685593719371816679, -0.4274642268707216641 ) ) ;
#21824=CYLINDRICAL_SURFACE ( 'NONE', #38422, 0.1033070866141734129 ) ;
#21830=EDGE_CURVE ( 'NONE', #4931, #14515, #37487, .T. ) ;
#21842=B_SPLINE_CURVE_WITH_KNOTS ( 'NONE', 3,
 ( #22881, #35396, #7190, #13596 ),
 .UNSPECIFIED., .F., .F.,
 ( 4, 4 ),
 ( 8.673617379883999842E-19, 0.0003267947208782233685 ),
 .UNSPECIFIED. ) ;
#21853=AXIS2_PLACEMENT_3D ( 'NONE', #18135, #14420, #39327 ) ;
#21858=CARTESIAN_POINT ( 'NONE',  ( 0.5538850894636544453, -1.624718492099754830, -0.5678182754891358819 ) ) ;
#21863=CARTESIAN_POINT ( 'NONE',  ( 0.4651649163319350189, -1.149540594742337607, -0.6230854793619403642 ) ) ;
#21868=EDGE_LOOP ( 'NONE', ( #4638, #12762, #3926, #17882 ) ) ;
#21871=ORIENTED_EDGE ( 'NONE', *, *, #930, .F. ) ;
#21881=CARTESIAN_POINT ( 'NONE',  ( 0.3677258932907612188, -1.634674973640408036, -0.3778581608314561802 ) ) ;
#21884=CARTESIAN_POINT ( 'NONE',  ( 0.6291968284940171463, -1.616033820151582034, -0.4930595378406338880 ) ) ;
#21890=DIRECTION ( 'NONE',  ( 0.4999551463232372317, -0.8660512985181133550, 0.000000000000000000 ) ) ;
#21893=CARTESIAN_POINT ( 'NONE',  ( 0.5114126470110641476, -1.614748454822723556, -0.5166151207188711680 ) ) ;
#21903=ADVANCED_FACE ( 'NONE', ( #27733 ), #40268, .F. ) ;
#21918=EDGE_LOOP ( 'NONE', ( #9517, #11324, #22755 ) ) ;
#21920=CARTESIAN_POINT ( 'NONE',  ( 0.1890194704680109583, -1.936495776297340710, -0.3324113174558592787 ) ) ;
#21925=EDGE_LOOP ( 'NONE', ( #33322, #26362, #31481, #30630 ) ) ;
#21930=DIRECTION ( 'NONE',  ( 0.8660512985181135770, 0.4999551463232370097, 0.000000000000000000 ) ) ;
#21933=CARTESIAN_POINT ( 'NONE',  ( 0.3374716419252246080, -1.644379157745376574, -0.6493782657834309413 ) ) ;
#21937=EDGE_CURVE ( 'NONE', #3488, #16904, #28302, .T. ) ;
#21938=LINE ( 'NONE', #18851, #6160 ) ;
#21939=CARTESIAN_POINT ( 'NONE',  ( 0.2388414923709098747, -1.586845850796878121, -0.3224580823847754130 ) ) ;
#21955=DIRECTION ( 'NONE',  ( -0.9107505893967028365, 0.000000000000000000, -0.4129568547845627324 ) ) ;
#21963=CARTESIAN_POINT ( 'NONE',  ( 0.3641313327837605307, -1.992291791370100373, -0.5052991671685238551 ) ) ;
#21965=CARTESIAN_POINT ( 'NONE',  ( 0.3696433192220597852, -2.076078244643423609, -0.4731903481153287849 ) ) ;
#21967=CARTESIAN_POINT ( 'NONE',  ( 0.3927971208821917082, -1.752502930713592200, -0.5454495665901371027 ) ) ;
#21987=EDGE_LOOP ( 'NONE', ( #13906, #38494, #31256, #33384 ) ) ;
#21994=CIRCLE ( 'NONE', #21343, 0.1050228153667111808 ) ;
#21996=CARTESIAN_POINT ( 'NONE',  ( -0.001553869254396566353, -1.875183443470214151, -0.3468731710442038985 ) ) ;
#21998=CARTESIAN_POINT ( 'NONE',  ( 0.6118202138478362473, -1.459615948755139003, -0.6250000000000000000 ) ) ;
#22001=CARTESIAN_POINT ( 'NONE',  ( 0.2999999999999784506, -1.937578511955589278, -0.3171235303465976818 ) ) ;
#22006=CARTESIAN_POINT ( 'NONE',  ( 0.0009544144440424411633, -1.789965111182992175, -0.6370759315579171966 ) ) ;
#22009=AXIS2_PLACEMENT_3D ( 'NONE', #37086, #15075, #14879 ) ;
#22016=AXIS2_PLACEMENT_3D ( 'NONE', #11641, #21316, #24388 ) ;
#22025=ORIENTED_EDGE ( 'NONE', *, *, #4613, .T. ) ;
#22040=CARTESIAN_POINT ( 'NONE',  ( 0.2927350798623002959, -1.544518291098198715, -0.6925464747855896164 ) ) ;
#22050=AXIS2_PLACEMENT_3D ( 'NONE', #32615, #32403, #7094 ) ;
#22051=EDGE_CURVE ( 'NONE', #13521, #1646, #3981, .T. ) ;
#22060=CARTESIAN_POINT ( 'NONE',  ( 0.4688459138424372341, -1.061988423737608045, -0.4248180574663140141 ) ) ;
#22061=CARTESIAN_POINT ( 'NONE',  ( 0.3034770402916767695, -1.538524164614652578, -0.7285408748657138389 ) ) ;
#22063=CARTESIAN_POINT ( 'NONE',  ( 0.4173046189016191287, -1.738355212467242561, -0.5155029497116575543 ) ) ;
#22075=ORIENTED_EDGE ( 'NONE', *, *, #38058, .T. ) ;
#22076=CARTESIAN_POINT ( 'NONE',  ( 0.4640112847229192483, -1.150115029303059089, -0.4078508934533979780 ) ) ;
#22081=CARTESIAN_POINT ( 'NONE',  ( 0.5473076987003111515, -1.651760216406904513, -0.4929644493450987541 ) ) ;
#22083=CIRCLE ( 'NONE', #24077, 0.04330708661417336652 ) ;
#22088=CARTESIAN_POINT ( 'NONE',  ( 0.1909286924077255587, -1.257064795538239466, -0.7137159211901569211 ) ) ;
#22089=CARTESIAN_POINT ( 'NONE',  ( 0.3393515303230732472, -1.642456816116736107, -0.5888195431444244177 ) ) ;
#22090=B_SPLINE_CURVE_WITH_KNOTS ( 'NONE', 3,
 ( #15805, #24464, #27961, #31036 ),
 .UNSPECIFIED., .F., .F.,
 ( 4, 4 ),
 ( 0.000000000000000000, 0.001818400350217978497 ),
 .UNSPECIFIED. ) ;
#22096=CARTESIAN_POINT ( 'NONE',  ( 0.1909286924077255032, -1.257064795538239022, -0.4400554600884079015 ) ) ;
#22098=CARTESIAN_POINT ( 'NONE',  ( 0.5767571638091754105, -1.611000162511842415, -0.5470636458226728616 ) ) ;
#22100=ORIENTED_EDGE ( 'NONE', *, *, #18593, .T. ) ;
#22101=EDGE_CURVE ( 'NONE', #24018, #4341, #37949, .T. ) ;
#22105=VECTOR ( 'NONE', #35379, 39.37007874015748854 ) ;
#22125=CARTESIAN_POINT ( 'NONE',  ( 0.3572222731481287661, -1.622781385286526934, -0.3671481750039431446 ) ) ;
#22128=ORIENTED_EDGE ( 'NONE', *, *, #30517, .T. ) ;
#22137=CARTESIAN_POINT ( 'NONE',  ( 0.3571444853020102617, -1.839383662986079138, -0.5196660627627504025 ) ) ;
#22144=CIRCLE ( 'NONE', #4373, 0.2500000000000000000 ) ;
#22147=CARTESIAN_POINT ( 'NONE',  ( 0.6630839938131345423, -1.446213159395746128, -0.6155857397476032222 ) ) ;
#22149=CARTESIAN_POINT ( 'NONE',  ( 0.5412176055846257272, -1.597081727404586093, -0.4604589859954540398 ) ) ;
#22151=CARTESIAN_POINT ( 'NONE',  ( 0.4112193008909481584, -1.591609915475934889, -0.6177460231409163116 ) ) ;
#22167=B_SPLINE_CURVE_WITH_KNOTS ( 'NONE', 3,
 ( #8204, #11509, #1856, #36181 ),
 .UNSPECIFIED., .F., .F.,
 ( 4, 4 ),
 ( 0.000000000000000000, 0.0002765389585800600018 ),
 .UNSPECIFIED. ) ;
#22168=CARTESIAN_POINT ( 'NONE',  ( 0.6328450409950655553, -1.528231567268848234, -0.4195382387927960588 ) ) ;
#22175=CARTESIAN_POINT ( 'NONE',  ( 0.3830941788893716948, -1.614634721936343498, -0.3633953494663126893 ) ) ;
#22176=CARTESIAN_POINT ( 'NONE',  ( 0.3641400453962177486, -1.992249701587664790, -0.4900924681091965440 ) ) ;
#22177=CARTESIAN_POINT ( 'NONE',  ( 0.5508559616054408137, -1.661258531014996986, -0.4933326546058601214 ) ) ;
#22179=ORIENTED_EDGE ( 'NONE', *, *, #37220, .T. ) ;
#22180=CARTESIAN_POINT ( 'NONE',  ( 0.5399038930177494366, -1.667580954481910904, -0.5371941175943450997 ) ) ;
#22185=DIRECTION ( 'NONE',  ( 0.4999551463232373427, -0.8660512985181134660, 0.000000000000000000 ) ) ;
#22203=CARTESIAN_POINT ( 'NONE',  ( 0.5922249234364754811, -1.371803823430798541, -0.6250000000000000000 ) ) ;
#22211=CARTESIAN_POINT ( 'NONE',  ( 0.07619306301934503090, -1.974142829211253503, -0.6628502878266334664 ) ) ;
#22212=CARTESIAN_POINT ( 'NONE',  ( 0.3397077535880359545, -1.654685348432989089, -0.3858274525146626055 ) ) ;
#22220=CARTESIAN_POINT ( 'NONE',  ( 0.1986084012382124953, -2.036380768698693444, -0.7103514068621292754 ) ) ;
#22233=ORIENTED_EDGE ( 'NONE', *, *, #24326, .F. ) ;
#22235=ADVANCED_FACE ( 'NONE', ( #10382 ), #18495, .F. ) ;
#22247=CARTESIAN_POINT ( 'NONE',  ( 0.4667607702232405842, -1.076905671295661948, -0.4183295294279661403 ) ) ;
#22267=CARTESIAN_POINT ( 'NONE',  ( 0.2090306192065299884, -1.362070338884064258, -0.3027639479267801859 ) ) ;
#22272=CARTESIAN_POINT ( 'NONE',  ( 0.4527603377605404766, -1.144379813877050012, -0.3965114147629228980 ) ) ;
#22279=EDGE_CURVE ( 'NONE', #30753, #24795, #34204, .T. ) ;
#22282=CARTESIAN_POINT ( 'NONE',  ( 0.5299567605269758230, -1.673323247217261223, -0.5639626154930592605 ) ) ;
#22289=CARTESIAN_POINT ( 'NONE',  ( 0.1409906984825553267, -1.239706420848685875, -0.5155029497116575543 ) ) ;
#22291=CARTESIAN_POINT ( 'NONE',  ( 0.6404767502594985729, -1.465846671489676067, -0.6342850214802828734 ) ) ;
#22294=ORIENTED_EDGE ( 'NONE', *, *, #17180, .T. ) ;
#22298=FACE_OUTER_BOUND ( 'NONE', #37249, .T. ) ;
#22312=CARTESIAN_POINT ( 'NONE',  ( 0.2059273467974225835, -1.283046334493782359, -0.3904158619672754016 ) ) ;
#22314=B_SPLINE_CURVE_WITH_KNOTS ( 'NONE', 3,
 ( #9995, #178, #19661, #16575, #32197, #9594, #28517, #6490 ),
 .UNSPECIFIED., .F., .F.,
 ( 4, 2, 2, 4 ),
 ( 0.000000000000000000, 0.0002979882110954374698, 0.0005959764221908749396, 0.001191952844381744675 ),
 .UNSPECIFIED. ) ;
#22319=EDGE_CURVE ( 'NONE', #4341, #25189, #21735, .T. ) ;
#22331=CARTESIAN_POINT ( 'NONE',  ( 0.3371096829608895007, -1.701240623061720969, -0.6069842154957213465 ) ) ;
#22340=CARTESIAN_POINT ( 'NONE',  ( 0.3302290664199810100, -1.638364056477709996, -0.3722368618827794906 ) ) ;
#22346=CARTESIAN_POINT ( 'NONE',  ( 0.2597702376225676235, -1.565296447219295173, -0.3170323014659355287 ) ) ;
#22357=DIRECTION ( 'NONE',  ( -1.000000000000000000, -0.000000000000000000, -0.000000000000000000 ) ) ;
#22365=EDGE_CURVE ( 'NONE', #26020, #16545, #35521, .T. ) ;
#22370=CARTESIAN_POINT ( 'NONE',  ( 0.7059656540691128246, -1.571716619208481935, -0.5155029497116575543 ) ) ;
#22372=LINE ( 'NONE', #35493, #12561 ) ;
#22381=ORIENTED_EDGE ( 'NONE', *, *, #33623, .F. ) ;
#22386=ORIENTED_EDGE ( 'NONE', *, *, #29537, .F. ) ;
#22394=CARTESIAN_POINT ( 'NONE',  ( 0.06540210900078118061, -2.045735273566230639, -0.3096830216599801844 ) ) ;
#22396=AXIS2_PLACEMENT_3D ( 'NONE', #23890, #32914, #30453 ) ;
#22407=CARTESIAN_POINT ( 'NONE',  ( 0.6349199332347138514, -1.492121435015029585, -0.6355974108494197861 ) ) ;
#22412=CARTESIAN_POINT ( 'NONE',  ( 0.5826009915492634805, -1.549810527521380932, -0.4246621135213465847 ) ) ;
#22413=CARTESIAN_POINT ( 'NONE',  ( 0.1807987625579654534, -1.701547269739460022, -0.6830814722341453926 ) ) ;
#22416=VERTEX_POINT ( 'NONE', #12600 ) ;
#22423=CARTESIAN_POINT ( 'NONE',  ( 0.4559719632891929830, -1.698713290701216350, -0.5155029497116575543 ) ) ;
#22431=VERTEX_POINT ( 'NONE', #28851 ) ;
#22433=CARTESIAN_POINT ( 'NONE',  ( 0.5473076987003111515, -1.651760216406904513, -0.4929644493450987541 ) ) ;
#22439=EDGE_LOOP ( 'NONE', ( #24485, #18623, #38330, #5229 ) ) ;
#22441=CARTESIAN_POINT ( 'NONE',  ( 0.4602558791604159927, -1.075954481373732508, -0.4172575352404306881 ) ) ;
#22455=CIRCLE ( 'NONE', #25641, 0.1033070866141734129 ) ;
#22459=CARTESIAN_POINT ( 'NONE',  ( 0.1849042594950439655, -1.699762810001741453, -0.6534071581412237428 ) ) ;
#22461=CARTESIAN_POINT ( 'NONE',  ( 0.3634995547569259688, -1.769442106537615134, -0.6725227346654005789 ) ) ;
#22463=CARTESIAN_POINT ( 'NONE',  ( 0.6436302007692352722, -1.590381715263790463, -0.5770581850489380216 ) ) ;
#22467=ORIENTED_EDGE ( 'NONE', *, *, #15527, .T. ) ;
#22474=VERTEX_POINT ( 'NONE', #34620 ) ;
#22477=VECTOR ( 'NONE', #26179, 39.37007874015748143 ) ;
#22478=( BOUNDED_SURFACE ( )  B_SPLINE_SURFACE ( 3, 2, ( 
 ( #24368, #8930, #39988 ),
 ( #5419, #2366, #30740 ),
 ( #11412, #36512, #18190 ),
 ( #5824, #27655, #8324 ),
 ( #14905, #40188, #33415 ),
 ( #30332, #36906, #34022 ),
 ( #27266, #36707, #5637 ),
 ( #12023, #33608, #8516 ),
 ( #21081, #24580, #37117 ),
 ( #21507, #6032, #18599 ),
 ( #21687, #3734, #19760 ),
 ( #32297, #19970, #32110 ),
 ( #881, #35595, #1087 ),
 ( #31155, #16681, #4112 ),
 ( #35399, #22461, #15309 ),
 ( #25544, #25964, #22676 ),
 ( #32505, #28826, #38072 ),
 ( #24791, #37311, #7394 ),
 ( #10498, #40403, #12229 ),
 ( #34987, #10320, #3525 ),
 ( #16288, #6797, #9121 ),
 ( #13174, #9889, #38487 ),
 ( #34217, #12997, #31913 ),
 ( #3917, #684, #19379 ),
 ( #16475, #25744, #28628 ),
 ( #38270, #10103, #35208 ) ),
 .UNSPECIFIED., .F., .F., .T. ) 
 B_SPLINE_SURFACE_WITH_KNOTS ( ( 4, 2, 2, 2, 2, 2, 2, 2, 2, 2, 2, 2, 4 ),
 ( 3, 3 ),
 ( 0.03478970966414503263, 0.03529932688707621696, 0.03580894411000740130, 0.03682817855586976996, 0.03886664744759451423, 0.04090511633931925850, 0.04294358523104399583, 0.04498205412276874010, 0.04600128856863111571, 0.04702052301449348437, 0.04803975746035585304, 0.04905899190621822170, 0.05109746079794296597 ),
 ( 0.000000000000000000, 1.000000000000000000 ),
 .UNSPECIFIED. ) 
 GEOMETRIC_REPRESENTATION_ITEM ( )  RATIONAL_B_SPLINE_SURFACE ( (
 ( 1.000000000000000000, 0.7053326528219874270, 1.000000000000000000),
 ( 1.000000000000000000, 0.7069087193608284414, 1.000000000000000000),
 ( 1.000000000000000000, 0.7074454249098806047, 1.000000000000000000),
 ( 1.000000000000000000, 0.7079727039066888716, 1.000000000000000000),
 ( 1.000000000000000000, 0.7079140579849947379, 1.000000000000000000),
 ( 1.000000000000000000, 0.7072990859638439431, 1.000000000000000000),
 ( 1.000000000000000000, 0.7062992663257996462, 1.000000000000000000),
 ( 1.000000000000000000, 0.7026654075174075809, 1.000000000000000000),
 ( 1.000000000000000000, 0.6993568048661583658, 1.000000000000000000),
 ( 1.000000000000000000, 0.6923303540839972348, 1.000000000000000000),
 ( 1.000000000000000000, 0.6885467396574446175, 1.000000000000000000),
 ( 1.000000000000000000, 0.6809569680526225133, 1.000000000000000000),
 ( 1.000000000000000000, 0.6771650901613724960, 1.000000000000000000),
 ( 1.000000000000000000, 0.6704471956693288659, 1.000000000000000000),
 ( 1.000000000000000000, 0.6675067785250807795, 1.000000000000000000),
 ( 1.000000000000000000, 0.6649784099743590859, 1.000000000000000000),
 ( 1.000000000000000000, 0.6644567522668610726, 1.000000000000000000),
 ( 1.000000000000000000, 0.6643594168469727501, 1.000000000000000000),
 ( 1.000000000000000000, 0.6647836916442323441, 1.000000000000000000),
 ( 1.000000000000000000, 0.6667676599421886730, 1.000000000000000000),
 ( 1.000000000000000000, 0.6683270600134922912, 1.000000000000000000),
 ( 1.000000000000000000, 0.6727537477506539965, 1.000000000000000000),
 ( 1.000000000000000000, 0.6756357399901673499, 1.000000000000000000),
 ( 1.000000000000000000, 0.6860398255734453388, 1.000000000000000000),
 ( 1.000000000000000000, 0.6954024235273548182, 1.000000000000000000),
 ( 1.000000000000000000, 0.7067908011272799884, 1.000000000000000000) ) ) 
 REPRESENTATION_ITEM ( '' )  SURFACE ( )  );
#22488=CARTESIAN_POINT ( 'NONE',  ( 0.5835086506366403691, -1.603182442426240417, -0.5754264449309163254 ) ) ;
#22498=EDGE_CURVE ( 'NONE', #652, #2027, #19846, .T. ) ;
#22501=EDGE_CURVE ( 'NONE', #28743, #7643, #30637, .T. ) ;
#22508=AXIS2_PLACEMENT_3D ( 'NONE', #35395, #38871, #16676 ) ;
#22515=CARTESIAN_POINT ( 'NONE',  ( 0.2117001771772084040, -1.293046366063226538, -0.4065196447463829132 ) ) ;
#22525=CARTESIAN_POINT ( 'NONE',  ( 0.7009661026058806588, -1.563056106223300823, -0.5155029497116575543 ) ) ;
#22536=EDGE_CURVE ( 'NONE', #37901, #22853, #16416, .T. ) ;
#22537=CIRCLE ( 'NONE', #34348, 0.2200000000000000011 ) ;
#22541=CARTESIAN_POINT ( 'NONE',  ( 0.4513655011140282891, -1.638057308912242549, -0.4132293443021504697 ) ) ;
#22546=CARTESIAN_POINT ( 'NONE',  ( 0.4000000000034333314, -2.064900289389559607, -0.7181543511010001213 ) ) ;
#22554=FACE_BOUND ( 'NONE', #23849, .T. ) ;
#22571=EDGE_CURVE ( 'NONE', #18975, #25557, #8573, .T. ) ;
#22575=AXIS2_PLACEMENT_3D ( 'NONE', #21454, #27809, #40343 ) ;
#22581=CARTESIAN_POINT ( 'NONE',  ( 0.06666666666664561314, -2.107936428766273629, -0.7005084057759866090 ) ) ;
#22592=DIRECTION ( 'NONE',  ( 0.000000000000000000, 0.000000000000000000, -1.000000000000000000 ) ) ;
#22602=CARTESIAN_POINT ( 'NONE',  ( -0.004773644027431071801, -1.959412267866362356, -0.3319689416633392898 ) ) ;
#22610=DIRECTION ( 'NONE',  ( 0.5257402267398344486, 0.3034999571474336633, -0.7946602984917855439 ) ) ;
#22611=VECTOR ( 'NONE', #17983, 39.37007874015748854 ) ;
#22628=FACE_OUTER_BOUND ( 'NONE', #25047, .T. ) ;
#22629=EDGE_CURVE ( 'NONE', #22416, #12314, #32594, .T. ) ;
#22630=ORIENTED_EDGE ( 'NONE', *, *, #18289, .F. ) ;
#22633=TOROIDAL_SURFACE ( 'NONE', #35760, 0.08830708661417342731, 0.01499999999999999944 ) ;
#22636=CARTESIAN_POINT ( 'NONE',  ( 0.4234909963964843538, -1.082397635545747638, -0.5155029497116575543 ) ) ;
#22637=CARTESIAN_POINT ( 'NONE',  ( 0.3447453106071770579, -1.668772187017560915, -0.4515255377999706221 ) ) ;
#22642=EDGE_LOOP ( 'NONE', ( #3213, #39906 ) ) ;
#22647=CARTESIAN_POINT ( 'NONE',  ( 0.5271998568634933546, -1.674914755915226205, -0.4628290575799461348 ) ) ;
#22648=CARTESIAN_POINT ( 'NONE',  ( 0.1909286924077255032, -1.257064795538239022, -0.3194753470178354759 ) ) ;
#22651=CARTESIAN_POINT ( 'NONE',  ( 0.003300408388875467319, -1.849130736997417479, -0.3506394244204662503 ) ) ;
#22653=ORIENTED_EDGE ( 'NONE', *, *, #22279, .T. ) ;
#22661=EDGE_CURVE ( 'NONE', #19455, #33728, #25055, .T. ) ;
#22663=CIRCLE ( 'NONE', #333, 0.1033070866141732325 ) ;
#22666=DIRECTION ( 'NONE',  ( 0.8660512985181130219, 0.4999551463232377868, 0.000000000000000000 ) ) ;
#22676=CARTESIAN_POINT ( 'NONE',  ( 0.3710009529117821447, -1.739873908940936298, -0.4854938087489614196 ) ) ;
#22682=CARTESIAN_POINT ( 'NONE',  ( 0.4441836334028865796, -1.145505455753590418, -0.6481113851292223949 ) ) ;
#22686=EDGE_CURVE ( 'NONE', #29183, #37390, #20442, .T. ) ;
#22693=VECTOR ( 'NONE', #26861, 39.37007874015748143 ) ;
#22697=CARTESIAN_POINT ( 'NONE',  ( 0.6299594026003103586, -1.615593600444566569, -0.5387823540836409464 ) ) ;
#22699=VERTEX_POINT ( 'NONE', #36739 ) ;
#22705=CARTESIAN_POINT ( 'NONE',  ( 0.5895803812855957560, -1.594679580009012776, -0.5906415517346027544 ) ) ;
#22710=CARTESIAN_POINT ( 'NONE',  ( 0.5401403459456773914, -1.597711863851910996, -0.5730363334735802949 ) ) ;
#22716=CARTESIAN_POINT ( 'NONE',  ( 0.4278413765848551042, -1.120299553241070001, -0.3830631589809549431 ) ) ;
#22723=AXIS2_PLACEMENT_3D ( 'NONE', #13774, #17070, #26547 ) ;
#22730=ORIENTED_EDGE ( 'NONE', *, *, #32103, .F. ) ;
#22736=EDGE_CURVE ( 'NONE', #29150, #37623, #7078, .T. ) ;
#22738=CARTESIAN_POINT ( 'NONE',  ( 0.3590244010119321150, -1.770436742188270740, -0.4892477637902210019 ) ) ;
#22739=CARTESIAN_POINT ( 'NONE',  ( 0.3895266417130452408, -1.699103805033106651, -0.5245809722717744705 ) ) ;
#22750=CARTESIAN_POINT ( 'NONE',  ( 0.4747730085490121654, -1.591067186900658070, -0.4394709153640856125 ) ) ;
#22755=ORIENTED_EDGE ( 'NONE', *, *, #26886, .T. ) ;
#22759=CARTESIAN_POINT ( 'NONE',  ( 0.4352673078179172816, -1.693613930004312262, -0.5063126144843520526 ) ) ;
#22765=B_SPLINE_CURVE_WITH_KNOTS ( 'NONE', 3,
 ( #25915, #13553, #21858, #29391, #38436, #19715, #34385, #26122, #10274, #1235, #82, #22837 ),
 .UNSPECIFIED., .F., .F.,
 ( 4, 2, 2, 2, 2, 4 ),
 ( 1.163687884334659274E-17, 0.0008294755721960583124, 0.001244213358294084162, 0.001658951144392109686, 0.002488426716588164420, 0.003317902288784219372 ),
 .UNSPECIFIED. ) ;
#22767=ORIENTED_EDGE ( 'NONE', *, *, #34936, .F. ) ;
#22773=CARTESIAN_POINT ( 'NONE',  ( 0.5129993572544877534, -1.641037272694954474, -0.6170790168603458303 ) ) ;
#22780=CARTESIAN_POINT ( 'NONE',  ( 0.4792469954158677936, -1.117519082122008900, -0.6343516840475907914 ) ) ;
#22781=CARTESIAN_POINT ( 'NONE',  ( 0.3780067941418981392, -1.616348147715449768, -0.3643140746640379790 ) ) ;
#22791=CARTESIAN_POINT ( 'NONE',  ( 0.1999999999999789724, -2.107936428766273629, -0.7005084057759867200 ) ) ;
#22801=DIRECTION ( 'NONE',  ( 0.5147264766109145295, -0.8573544507820052285, 0.000000000000000000 ) ) ;
#22818=CARTESIAN_POINT ( 'NONE',  ( 0.6984663268742642428, -1.558725849730709934, -0.5155029497116575543 ) ) ;
#22819=CARTESIAN_POINT ( 'NONE',  ( 0.09999999999998167299, -1.869535141313860782, -0.3418892918993297059 ) ) ;
#22823=CARTESIAN_POINT ( 'NONE',  ( 0.1953801488688421129, -1.653727163013434920, -0.6877973177680917205 ) ) ;
#22828=DIRECTION ( 'NONE',  ( 0.8660512985181133550, 0.4999551463232372317, 0.000000000000000000 ) ) ;
#22837=CARTESIAN_POINT ( 'NONE',  ( 0.4751758298663427693, -1.652426242819087010, -0.6334442537810193175 ) ) ;
#22846=CARTESIAN_POINT ( 'NONE',  ( 0.3264244126186546802, -1.294301107126978767, -0.5166151207188711680 ) ) ;
#22847=EDGE_CURVE ( 'NONE', #38602, #22431, #37506, .T. ) ;
#22853=VERTEX_POINT ( 'NONE', #14255 ) ;
#22854=CARTESIAN_POINT ( 'NONE',  ( 0.5976280483195713922, -1.483999647174189862, -0.6415005453050633966 ) ) ;
#22860=ADVANCED_FACE ( 'NONE', ( #36060 ), #3481, .T. ) ;
#22861=CARTESIAN_POINT ( 'NONE',  ( 0.04930870543692147251, -1.485063399300671882, -0.3452542621255675348 ) ) ;
#22875=CYLINDRICAL_SURFACE ( 'NONE', #32411, 0.04330708661417322775 ) ;
#22881=CARTESIAN_POINT ( 'NONE',  ( 0.2161879510971927987, -1.277123080371499242, -0.7187326247832955817 ) ) ;
#22884=CARTESIAN_POINT ( 'NONE',  ( 0.3766954841305968360, -1.761798103149637029, -0.5753806683247417730 ) ) ;
#22896=CARTESIAN_POINT ( 'NONE',  ( 0.5172910145215950939, -1.680634944466891323, -0.5803635445188605191 ) ) ;
#22899=CARTESIAN_POINT ( 'NONE',  ( 0.6511295279640840761, -1.603372484741562687, -0.5770581850489380216 ) ) ;
#22912=CARTESIAN_POINT ( 'NONE',  ( 0.4181400076792504139, -1.624779815497015001, -0.6506891825583066558 ) ) ;
#22925=ORIENTED_EDGE ( 'NONE', *, *, #26502, .T. ) ;
#22932=EDGE_LOOP ( 'NONE', ( #30287, #33132, #16766, #38828 ) ) ;
#22937=PRODUCT_DEFINITION_SHAPE ( 'NONE', 'NONE',  #11907 ) ;
#22938=CARTESIAN_POINT ( 'NONE',  ( 0.3790029845727732605, -1.717173918479974803, -0.3392914156897724465 ) ) ;
#22945=CARTESIAN_POINT ( 'NONE',  ( 0.5010447282329528740, -1.606058451036832757, -0.4018775084353748972 ) ) ;
#22955=( BOUNDED_SURFACE ( )  B_SPLINE_SURFACE ( 3, 2, ( 
 ( #14871, #36672, #2118 ),
 ( #27432, #24150, #39756 ),
 ( #27009, #17943, #39956 ),
 ( #30500, #8480, #14652 ),
 ( #36471, #17735, #11588 ),
 ( #21041, #11776, #20855 ) ),
 .UNSPECIFIED., .F., .F., .T. ) 
 B_SPLINE_SURFACE_WITH_KNOTS ( ( 4, 2, 4 ),
 ( 3, 3 ),
 ( -7.708135345285693774E-16, 0.0003922111778123613546, 0.0007844223556254935770 ),
 ( 0.000000000000000000, 1.000000000000000000 ),
 .UNSPECIFIED. ) 
 GEOMETRIC_REPRESENTATION_ITEM ( )  RATIONAL_B_SPLINE_SURFACE ( (
 ( 1.000000000000000000, 0.8959137433787442983, 1.000000000000000000),
 ( 1.000000000000000000, 0.9145433835206386863, 1.000000000000000000),
 ( 1.000000000000000000, 0.9368263804283851748, 1.000000000000000000),
 ( 1.000000000000000000, 0.9787315261369833319, 1.000000000000000000),
 ( 1.000000000000000000, 0.9990824601813189654, 1.000000000000000000),
 ( 1.000000000000000000, 1.000000000000000000, 1.000000000000000000) ) ) 
 REPRESENTATION_ITEM ( '' )  SURFACE ( )  );
#22959=CARTESIAN_POINT ( 'NONE',  ( 0.5240124945691670977, -1.643385070224909095, -0.5720511728448423039 ) ) ;
#22964=DIRECTION ( 'NONE',  ( 1.000000000000000000, 0.000000000000000000, 0.000000000000000000 ) ) ;
#22966=CARTESIAN_POINT ( 'NONE',  ( 0.3643499753119555651, -1.728436088122397241, -0.4712977219643614268 ) ) ;
#22972=CARTESIAN_POINT ( 'NONE',  ( 0.3595715536228106801, -1.625401886829162423, -0.3696110269036073093 ) ) ;
#22975=CARTESIAN_POINT ( 'NONE',  ( 0.3969982963057278047, -1.750077671058422046, -0.4821875037442182599 ) ) ;
#22993=CARTESIAN_POINT ( 'NONE',  ( 0.3841185810962554070, -1.843835201582077810, -0.5188048874333898164 ) ) ;
#22995=EDGE_CURVE ( 'NONE', #18407, #25557, #4673, .T. ) ;
#23003=CARTESIAN_POINT ( 'NONE',  ( 0.3996906523120555832, -1.748698433108215822, -0.4855307030469387941 ) ) ;
#23004=CARTESIAN_POINT ( 'NONE',  ( 0.02999999999997886302, -2.107936428766274073, -0.7005084057759867200 ) ) ;
#23010=CARTESIAN_POINT ( 'NONE',  ( 0.6284438268168236474, -1.513958728249438668, -0.6343483574234501932 ) ) ;
#23016=B_SPLINE_CURVE_WITH_KNOTS ( 'NONE', 3,
 ( #14088, #5025, #29941, #20470, #26662, #8107, #4807, #17591, #39580, #20687, #11411, #7709, #38979, #1963, #20276, #32798, #29520, #23981, #33000, #1357, #1564, #17173, #26854, #39195 ),
 .UNSPECIFIED., .F., .F.,
 ( 4, 2, 2, 2, 2, 2, 2, 2, 2, 2, 2, 4 ),
 ( 0.000000000000000000, 0.001374078136085094080, 0.002061117204127640469, 0.002748156272170186858, 0.004122234408255279203, 0.005496312544340371115, 0.008244468816510554937, 0.01099262508868074049, 0.01374078136085092432, 0.01648893763302110640, 0.01923709390519129023, 0.02198525017736147058 ),
 .UNSPECIFIED. ) ;
#23018=CARTESIAN_POINT ( 'NONE',  ( 0.5939569629664056549, -1.553735267838222134, -0.5704756277538377551 ) ) ;
#23019=CARTESIAN_POINT ( 'NONE',  ( -2.134683096299215379E-14, -2.097675824466504135, -0.2588528740066096678 ) ) ;
#23020=DIRECTION ( 'NONE',  ( 0.8660512985181134660, 0.4999551463232372872, 0.000000000000000000 ) ) ;
#23021=CARTESIAN_POINT ( 'NONE',  ( 0.02999999999997886302, -2.097675824466503691, -0.2907077406111384099 ) ) ;
#23022=ORIENTED_EDGE ( 'NONE', *, *, #40637, .T. ) ;
#23023=ORIENTED_EDGE ( 'NONE', *, *, #26606, .F. ) ;
#23028=CARTESIAN_POINT ( 'NONE',  ( 0.4242133616548364183, -1.734366925052854391, -0.4397180493288433967 ) ) ;
#23034=CARTESIAN_POINT ( 'NONE',  ( 0.3451885137985100105, -1.726073941889417096, -0.5819068695184340667 ) ) ;
#23036=FACE_OUTER_BOUND ( 'NONE', #1745, .T. ) ;
#23051=CARTESIAN_POINT ( 'NONE',  ( 0.1590165108039097164, -1.390942544176572371, -0.5155029497116575543 ) ) ;
#23052=DIRECTION ( 'NONE',  ( 0.000000000000000000, 0.000000000000000000, -1.000000000000000000 ) ) ;
#23071=ORIENTED_EDGE ( 'NONE', *, *, #22661, .T. ) ;
#23073=EDGE_CURVE ( 'NONE', #6462, #29455, #38166, .T. ) ;
#23079=CARTESIAN_POINT ( 'NONE',  ( 0.4950886493683288037, -1.678532471121934044, -0.4215530961782456010 ) ) ;
#23081=EDGE_CURVE ( 'NONE', #16986, #2123, #11246, .T. ) ;
#23083=ORIENTED_EDGE ( 'NONE', *, *, #40605, .F. ) ;
#23099=VERTEX_POINT ( 'NONE', #22081 ) ;
#23102=AXIS2_PLACEMENT_3D ( 'NONE', #29132, #7515, #38994 ) ;
#23103=DIRECTION ( 'NONE',  ( 0.4999551463232372317, -0.8660512985181135770, 0.000000000000000000 ) ) ;
#23106=CARTESIAN_POINT ( 'NONE',  ( 0.3916862212415726519, -1.581131361642308608, -0.7187326247832954706 ) ) ;
#23112=( NAMED_UNIT ( * ) SI_UNIT ( $, .STERADIAN. ) SOLID_ANGLE_UNIT ( ) );
#23115=AXIS2_PLACEMENT_3D ( 'NONE', #29753, #20505, #33039 ) ;
#23116=CARTESIAN_POINT ( 'NONE',  ( 0.4667255516235201407, -1.094999438749613363, -0.3992978201560059559 ) ) ;
#23124=CIRCLE ( 'NONE', #26403, 0.2000000000000000666 ) ;
#23126=DIRECTION ( 'NONE',  ( -0.4999551463232372317, 0.8660512985181135770, -0.000000000000000000 ) ) ;
#23129=CARTESIAN_POINT ( 'NONE',  ( 0.6466186708443523168, -1.438673711944949307, -0.6250000000000000000 ) ) ;
#23134=ORIENTED_EDGE ( 'NONE', *, *, #23073, .F. ) ;
#23136=DIRECTION ( 'NONE',  ( 0.1109881770483700930, -0.4429139914152930846, -0.8896678148410526177 ) ) ;
#23137=VERTEX_POINT ( 'NONE', #4128 ) ;
#23139=CARTESIAN_POINT ( 'NONE',  ( 0.3809420377884416564, -1.709537094523409628, -0.3376603513304489157 ) ) ;
#23149=ORIENTED_EDGE ( 'NONE', *, *, #16842, .F. ) ;
#23166=CARTESIAN_POINT ( 'NONE',  ( 0.5534668029622461516, -1.624932764085767367, -0.5687721870468918084 ) ) ;
#23167=ORIENTED_EDGE ( 'NONE', *, *, #25584, .T. ) ;
#23171=B_SPLINE_CURVE_WITH_KNOTS ( 'NONE', 3,
 ( #686, #22884, #31917, #28828, #35212, #1091 ),
 .UNSPECIFIED., .F., .F.,
 ( 4, 2, 4 ),
 ( 0.000000000000000000, 0.0003405513792915484993, 0.0006811027585830969986 ),
 .UNSPECIFIED. ) ;
#23177=CARTESIAN_POINT ( 'NONE',  ( 0.2059273467974227778, -1.283046334493782359, -0.7137159211901564770 ) ) ;
#23204=VERTEX_POINT ( 'NONE', #32121 ) ;
#23205=CARTESIAN_POINT ( 'NONE',  ( 0.5089189524854907942, -1.641769820029543192, -0.4121086472089234842 ) ) ;
#23213=DIRECTION ( 'NONE',  ( 0.000000000000000000, -0.2513338844154411333, 0.9679004486746792812 ) ) ;
#23215=CIRCLE ( 'NONE', #14641, 0.1033070866141734129 ) ;
#23220=FACE_BOUND ( 'NONE', #15381, .T. ) ;
#23225=( GEOMETRIC_REPRESENTATION_CONTEXT ( 3 ) GLOBAL_UNCERTAINTY_ASSIGNED_CONTEXT ( ( #35466 ) ) GLOBAL_UNIT_ASSIGNED_CONTEXT ( ( #11616, #18377, #30925 ) ) REPRESENTATION_CONTEXT ( 'NONE', 'WORKASPACE' ) );
#23227=CARTESIAN_POINT ( 'NONE',  ( 0.5956979983064725204, -1.550072859360259070, -0.5756593981205863075 ) ) ;
#23236=CARTESIAN_POINT ( 'NONE',  ( 0.2059273467974225835, -1.283046334493782137, -0.6485234391946320676 ) ) ;
#23240=VERTEX_POINT ( 'NONE', #29029 ) ;
#23243=ORIENTED_EDGE ( 'NONE', *, *, #12837, .T. ) ;
#23244=CARTESIAN_POINT ( 'NONE',  ( 0.5910253966860438135, -1.487811233934940081, -0.6023409643032461291 ) ) ;
#23246=AXIS2_PLACEMENT_3D ( 'NONE', #36568, #3030, #8371 ) ;
#23253=CARTESIAN_POINT ( 'NONE',  ( 0.1183779203685188658, -1.376060927314119553, -0.3271212237852036409 ) ) ;
#23273=PRODUCT_DEFINITION_CONTEXT ( 'detailed design', #10342, 'design' ) ;
#23282=DIRECTION ( 'NONE',  ( 0.4999551463232372317, -0.8660512985181135770, 0.000000000000000000 ) ) ;
#23294=CARTESIAN_POINT ( 'NONE',  ( 0.5547152119369697099, -1.589750697506561616, -0.5166151207188711680 ) ) ;
#23302=ADVANCED_FACE ( 'NONE', ( #34999 ), #39035, .F. ) ;
#23304=ORIENTED_EDGE ( 'NONE', *, *, #34631, .F. ) ;
#23312=CARTESIAN_POINT ( 'NONE',  ( 0.2923286432308245808, -1.660243258845594649, -0.3370932271639339728 ) ) ;
#23319=CARTESIAN_POINT ( 'NONE',  ( 0.4906998715583268944, -1.589006395870980359, -0.5745131788651638427 ) ) ;
#23334=CARTESIAN_POINT ( 'NONE',  ( 0.3699999999999786793, -2.097675824466503691, -0.5196396315034578217 ) ) ;
#23336=B_SPLINE_CURVE_WITH_KNOTS ( 'NONE', 3,
 ( #10386, #16360, #20265, #7885, #20455, #28896, #32787, #14075, #7699, #32593, #13856, #29102, #19649, #3804 ),
 .UNSPECIFIED., .F., .F.,
 ( 4, 2, 2, 2, 2, 2, 4 ),
 ( 0.008198847749948421498, 0.008708900428346920755, 0.009218953106745421747, 0.009729005785143921003, 0.01023905846354242200, 0.01125916382033939796, 0.01227926917713637392 ),
 .UNSPECIFIED. ) ;
#23342=CARTESIAN_POINT ( 'NONE',  ( 0.2059273467974228333, -1.283046334493783247, -0.6445565283433527526 ) ) ;
#23348=VERTEX_POINT ( 'NONE', #3820 ) ;
#23349=CARTESIAN_POINT ( 'NONE',  ( 0.02650569172316860275, -1.591189904831632029, -0.6662411422194330912 ) ) ;
#23352=ORIENTED_EDGE ( 'NONE', *, *, #10704, .T. ) ;
#23353=CARTESIAN_POINT ( 'NONE',  ( 0.3573784231975513093, -1.820466169614756158, -0.5023318515619766833 ) ) ;
#23365=ORIENTED_EDGE ( 'NONE', *, *, #6675, .T. ) ;
#23374=LINE ( 'NONE', #32791, #6133 ) ;
#23375=ADVANCED_FACE ( 'NONE', ( #14890 ), #12473, .T. ) ;
#23377=CARTESIAN_POINT ( 'NONE',  ( 0.1909286924077255587, -1.257064795538239022, -0.6919843404141109433 ) ) ;
#23387=ORIENTED_EDGE ( 'NONE', *, *, #33344, .F. ) ;
#23391=VERTEX_POINT ( 'NONE', #37562 ) ;
#23394=CARTESIAN_POINT ( 'NONE',  ( 0.3601132046754574323, -1.751178885491700532, -0.4776197548361051370 ) ) ;
#23398=DIMENSIONAL_EXPONENTS ( 1.000000000000000000, 0.000000000000000000, 0.000000000000000000, 0.000000000000000000, 0.000000000000000000, 0.000000000000000000, 0.000000000000000000 ) ;
#23400=ORIENTED_EDGE ( 'NONE', *, *, #10337, .T. ) ;
#23407=EDGE_CURVE ( 'NONE', #394, #10240, #9299, .T. ) ;
#23414=CARTESIAN_POINT ( 'NONE',  ( 0.2209260011871197193, -1.309027873449325918, -0.4125659523519145666 ) ) ;
#23421=VERTEX_POINT ( 'NONE', #13088 ) ;
#23424=ORIENTED_EDGE ( 'NONE', *, *, #9032, .F. ) ;
#23427=CARTESIAN_POINT ( 'NONE',  ( 0.3959772125322972292, -1.738667461359298283, -0.4364921393681684414 ) ) ;
#23429=CARTESIAN_POINT ( 'NONE',  ( 0.4002945600007836169, -1.748174799945819924, -0.4981529668752289752 ) ) ;
#23436=CARTESIAN_POINT ( 'NONE',  ( 0.6119035909732429834, -1.554882900545723423, -0.6235685469894116650 ) ) ;
#23443=CARTESIAN_POINT ( 'NONE',  ( 0.5646341918047996788, -1.583084905584069224, -0.5428242601959012426 ) ) ;
#23447=ORIENTED_EDGE ( 'NONE', *, *, #2091, .T. ) ;
#23459=DIRECTION ( 'NONE',  ( 0.4999551463232373427, -0.8660512985181134660, 0.000000000000000000 ) ) ;
#23461=FACE_OUTER_BOUND ( 'NONE', #15594, .T. ) ;
#23465=DIRECTION ( 'NONE',  ( 0.8660512985181133550, 0.4999551463232372872, 0.000000000000000000 ) ) ;
#23468=CARTESIAN_POINT ( 'NONE',  ( 0.03824833094100624220, -1.739503649588687750, -0.3347792643966959747 ) ) ;
#23469=ORIENTED_EDGE ( 'NONE', *, *, #4199, .F. ) ;
#23471=CARTESIAN_POINT ( 'NONE',  ( 0.5033392876442730479, -1.584769073138426299, -0.5496476129754243045 ) ) ;
#23475=CARTESIAN_POINT ( 'NONE',  ( 0.4940945688342389119, -1.677685676440951790, -0.6095800757797251723 ) ) ;
#23481=CIRCLE ( 'NONE', #12952, 0.1033070866141734129 ) ;
#23484=FACE_OUTER_BOUND ( 'NONE', #11840, .T. ) ;
#23485=CARTESIAN_POINT ( 'NONE',  ( -2.112273405726188513E-14, -2.183180860297921466, -0.4937760292030871079 ) ) ;
#23490=ORIENTED_EDGE ( 'NONE', *, *, #22498, .T. ) ;
#23502=EDGE_CURVE ( 'NONE', #5888, #32180, #23771, .T. ) ;
#23504=DIRECTION ( 'NONE',  ( -0.9379438357983841401, -0.2431488234232593582, 0.2472650613323660318 ) ) ;
#23519=CARTESIAN_POINT ( 'NONE',  ( 0.4097635862714068544, -1.729374185699168232, -0.4282187442611350425 ) ) ;
#23537=EDGE_CURVE ( 'NONE', #25449, #2897, #763, .T. ) ;
#23540=CARTESIAN_POINT ( 'NONE',  ( 0.03333333333331219700, -2.097675824466503691, -0.7286991843995640483 ) ) ;
#23543=CARTESIAN_POINT ( 'NONE',  ( 0.3874305626238240263, -1.778265208088890104, -0.4824895240968558596 ) ) ;
#23548=EDGE_LOOP ( 'NONE', ( #10886, #29200, #14482, #3530 ) ) ;
#23549=CARTESIAN_POINT ( 'NONE',  ( 0.009515880660224757676, -1.737226041143324684, -0.6384574844869379540 ) ) ;
#23550=ORIENTED_EDGE ( 'NONE', *, *, #39431, .T. ) ;
#23551=CARTESIAN_POINT ( 'NONE',  ( 0.3568217579247562887, -1.837974685081549708, -0.5015348115105691118 ) ) ;
#23563=VERTEX_POINT ( 'NONE', #30494 ) ;
#23567=CARTESIAN_POINT ( 'NONE',  ( 0.4441836334028864686, -1.145505455753590196, -0.6481113851292223949 ) ) ;
#23568=( BOUNDED_SURFACE ( )  B_SPLINE_SURFACE ( 3, 2, ( 
 ( #31174, #12630, #34652 ),
 ( #24600, #30757, #36921 ),
 ( #31378, #37738, #2988 ),
 ( #40003, #15539, #28272 ),
 ( #11825, #34040, #27883 ),
 ( #18402, #9559, #21314 ),
 ( #40420, #34449, #24386 ),
 ( #8736, #28090, #15112 ),
 ( #15723, #6262, #21920 ),
 ( #2778, #33851, #40617 ),
 ( #12248, #2576, #6048 ),
 ( #22137, #18834, #37517 ),
 ( #18000, #30559, #3182 ),
 ( #40204, #24985, #37328 ),
 ( #37135, #18616, #9138 ),
 ( #137, #34238, #2382 ),
 ( #9339, #27478, #18208 ),
 ( #21704, #30954, #27672 ),
 ( #8949, #21523, #38549 ),
 ( #26217, #22938, #6652 ),
 ( #22739, #7255, #15928 ),
 ( #28476, #23139, #3791 ),
 ( #13650, #37945, #558 ),
 ( #31769, #952, #19026 ),
 ( #38739, #10564, #6455 ),
 ( #31556, #3373, #10171 ),
 ( #12852, #35055, #10375 ),
 ( #35453, #351, #25414 ) ),
 .UNSPECIFIED., .F., .F., .T. ) 
 B_SPLINE_SURFACE_WITH_KNOTS ( ( 4, 2, 2, 2, 2, 2, 2, 2, 2, 2, 2, 2, 2, 4 ),
 ( 3, 3 ),
 ( 0.03544507920328695411, 0.03595486840377590254, 0.03646465760426484404, 0.03748423600524272703, 0.03952339280719850689, 0.04156254960915428676, 0.04360170641111006662, 0.04462128481208795655, 0.04564086321306584648, 0.04768002001502162635, 0.04869959841599951628, 0.04971917681697740621, 0.05073875521795528920, 0.05175833361893317913 ),
 ( 0.000000000000000000, 1.000000000000000000 ),
 .UNSPECIFIED. ) 
 GEOMETRIC_REPRESENTATION_ITEM ( )  RATIONAL_B_SPLINE_SURFACE ( (
 ( 1.000000000000000000, 0.7061763356917282186, 1.000000000000000000),
 ( 1.000000000000000000, 0.7080421523057279787, 1.000000000000000000),
 ( 1.000000000000000000, 0.7088516299600189363, 1.000000000000000000),
 ( 1.000000000000000000, 0.7099244856010646920, 1.000000000000000000),
 ( 1.000000000000000000, 0.7101378557341009312, 1.000000000000000000),
 ( 1.000000000000000000, 0.7103445576143324613, 1.000000000000000000),
 ( 1.000000000000000000, 0.7098994762787453894, 1.000000000000000000),
 ( 1.000000000000000000, 0.7079279405282516979, 1.000000000000000000),
 ( 1.000000000000000000, 0.7057284653322816181, 1.000000000000000000),
 ( 1.000000000000000000, 0.7007157790497101635, 1.000000000000000000),
 ( 1.000000000000000000, 0.6978342510162478529, 1.000000000000000000),
 ( 1.000000000000000000, 0.6916754492645889041, 1.000000000000000000),
 ( 1.000000000000000000, 0.6883795134656507386, 1.000000000000000000),
 ( 1.000000000000000000, 0.6835032746938722870, 1.000000000000000000),
 ( 1.000000000000000000, 0.6818926907723115161, 1.000000000000000000),
 ( 1.000000000000000000, 0.6788412388327624836, 1.000000000000000000),
 ( 1.000000000000000000, 0.6773936298796268130, 1.000000000000000000),
 ( 1.000000000000000000, 0.6736810316134190790, 1.000000000000000000),
 ( 1.000000000000000000, 0.6720343155085293230, 1.000000000000000000),
 ( 1.000000000000000000, 0.6725111439841665595, 1.000000000000000000),
 ( 1.000000000000000000, 0.6731816333784381712, 1.000000000000000000),
 ( 1.000000000000000000, 0.6757599976966006672, 1.000000000000000000),
 ( 1.000000000000000000, 0.6776668555841935948, 1.000000000000000000),
 ( 1.000000000000000000, 0.6829223581646010066, 1.000000000000000000),
 ( 1.000000000000000000, 0.6862934035413943423, 1.000000000000000000),
 ( 1.000000000000000000, 0.6945721712650553270, 1.000000000000000000),
 ( 1.000000000000000000, 0.6994068901145207295, 1.000000000000000000),
 ( 1.000000000000000000, 0.7048795877316381686, 1.000000000000000000) ) ) 
 REPRESENTATION_ITEM ( '' )  SURFACE ( )  );
#23577=CARTESIAN_POINT ( 'NONE',  ( 0.4382015218937659884, -1.612541052972227940, -0.6615483979663951963 ) ) ;
#23590=CARTESIAN_POINT ( 'NONE',  ( 0.6603083091704677887, -1.500180305189478425, -0.4119820518570970758 ) ) ;
#23592=ADVANCED_FACE ( 'NONE', ( #35703 ), #14042, .F. ) ;
#23598=VERTEX_POINT ( 'NONE', #14866 ) ;
#23606=CARTESIAN_POINT ( 'NONE',  ( 0.4806378395295555772, -1.105637800341301880, -0.6194292131661299772 ) ) ;
#23608=ORIENTED_EDGE ( 'NONE', *, *, #14806, .T. ) ;
#23615=CARTESIAN_POINT ( 'NONE',  ( 0.3744966970941377982, -1.755388072428740065, -0.4336563827106933444 ) ) ;
#23618=CARTESIAN_POINT ( 'NONE',  ( 0.3895925628365914939, -1.758298928368249525, -0.4737392274988301288 ) ) ;
#23623=CARTESIAN_POINT ( 'NONE',  ( 0.6175558182517195682, -1.622344311396844097, -0.4976589326200486219 ) ) ;
#23630=CARTESIAN_POINT ( 'NONE',  ( 0.5852709255473115268, -1.480800356531663198, -0.6004500878436644928 ) ) ;
#23635=ORIENTED_EDGE ( 'NONE', *, *, #34653, .T. ) ;
#23642=B_SPLINE_CURVE_WITH_KNOTS ( 'NONE', 3,
 ( #38725, #32155, #13828, #23334 ),
 .UNSPECIFIED., .F., .F.,
 ( 4, 4 ),
 ( 0.000000000000000000, 0.001818400350217978930 ),
 .UNSPECIFIED. ) ;
#23644=ORIENTED_EDGE ( 'NONE', *, *, #4525, .T. ) ;
#23646=DIRECTION ( 'NONE',  ( -0.8660512985181135770, -0.4999551463232371207, 0.000000000000000000 ) ) ;
#23656=CARTESIAN_POINT ( 'NONE',  ( 0.6984663268742642428, -1.558725849730709934, -0.5155029497116575543 ) ) ;
#23659=CARTESIAN_POINT ( 'NONE',  ( 0.1832580928828051736, -1.261492888555858505, -0.3231111295750616619 ) ) ;
#23660=CARTESIAN_POINT ( 'NONE',  ( 0.4867251962510119045, -1.680960026995096612, -0.6125153944539966089 ) ) ;
#23670=DIRECTION ( 'NONE',  ( -0.5963781153887844910, -0.3442778833694402074, -0.7251247358268644305 ) ) ;
#23671=CARTESIAN_POINT ( 'NONE',  ( 0.3655440060901842259, -1.768235641947720094, -0.5860794697665872022 ) ) ;
#23680=CARTESIAN_POINT ( 'NONE',  ( 0.4768848212686893073, -1.682051206446435465, -0.4156371400837834407 ) ) ;
#23690=CARTESIAN_POINT ( 'NONE',  ( 0.4356662251172991329, -1.610775558009423847, -0.3686272921855576756 ) ) ;
#23691=CARTESIAN_POINT ( 'NONE',  ( 0.6379434534673991131, -1.610984557855128951, -0.4725373547503501359 ) ) ;
#23703=CARTESIAN_POINT ( 'NONE',  ( 0.3786975293126830788, -1.707670322493268111, -0.4135462521370839029 ) ) ;
#23705=CARTESIAN_POINT ( 'NONE',  ( 0.3830059406587226767, -1.662912566754132015, -0.6203890335291190050 ) ) ;
#23707=CIRCLE ( 'NONE', #9211, 0.2200000000000000566 ) ;
#23720=ORIENTED_EDGE ( 'NONE', *, *, #28489, .F. ) ;
#23725=CARTESIAN_POINT ( 'NONE',  ( 0.3842204440267534826, -1.812485869991422804, -0.5233031296161457790 ) ) ;
#23732=CARTESIAN_POINT ( 'NONE',  ( 0.05254288559145195436, -1.595463313323315369, -0.6695117733422313311 ) ) ;
#23736=CARTESIAN_POINT ( 'NONE',  ( 0.6576035064516577711, -1.449376941801497454, -0.4138723806928110704 ) ) ;
#23751=VERTEX_POINT ( 'NONE', #6201 ) ;
#23763=CARTESIAN_POINT ( 'NONE',  ( 0.3950375043453270285, -1.756612718480099034, -0.7128469446588594494 ) ) ;
#23768=DIRECTION ( 'NONE',  ( 0.000000000000000000, 0.000000000000000000, -1.000000000000000000 ) ) ;
#23771=CIRCLE ( 'NONE', #27722, 0.04330708661417322775 ) ;
#23776=CARTESIAN_POINT ( 'NONE',  ( 0.2456699162554547011, -1.579418306085378143, -0.3207381830095928921 ) ) ;
#23777=ORIENTED_EDGE ( 'NONE', *, *, #11400, .T. ) ;
#23779=LINE ( 'NONE', #36297, #37049 ) ;
#23784=CARTESIAN_POINT ( 'NONE',  ( 0.4110399549994251389, -1.609958759213365953, -0.3626335216686736862 ) ) ;
#23806=AXIS2_PLACEMENT_3D ( 'NONE', #1579, #8527, #35918 ) ;
#23813=DIRECTION ( 'NONE',  ( 0.4999551463232372317, -0.8660512985181135770, 0.000000000000000000 ) ) ;
#23815=CARTESIAN_POINT ( 'NONE',  ( 0.3694954200858134863, -1.765954564873332355, -0.4302357760272142451 ) ) ;
#23818=CARTESIAN_POINT ( 'NONE',  ( 0.3939846702892026986, -1.751817380748406539, -0.4710255994886535236 ) ) ;
#23824=CARTESIAN_POINT ( 'NONE',  ( 0.6115442966349228238, -1.578889019291040530, -0.5746358093662063959 ) ) ;
#23832=CARTESIAN_POINT ( 'NONE',  ( 0.5726340570884991266, -1.543972946347143882, -0.4961447500887076201 ) ) ;
#23836=B_SPLINE_SURFACE_WITH_KNOTS ( 'NONE', 3, 3, ( 
 ( #546, #338, #7241, #19817 ),
 ( #12842, #32351, #29290, #1138 ),
 ( #26205, #14649, #4381, #1741 ),
 ( #38936, #36056, #29480, #36467 ),
 ( #5178, #36249, #20641, #8282 ),
 ( #32566, #16939, #2113, #23540 ),
 ( #8067, #13831, #29683, #20426 ) ),
 .UNSPECIFIED., .F., .F., .F.,
 ( 4, 1, 1, 1, 4 ),
 ( 4, 4 ),
 ( 0.000000000000000000, 0.2500000000000000000, 0.5000000000000000000, 0.7500000000000000000, 1.000000000000000000 ),
 ( 0.000000000000000000, 1.000000000000000000 ),
 .UNSPECIFIED. ) ;
#23838=CARTESIAN_POINT ( 'NONE',  ( 0.4733616728321626832, -1.077395945196840010, -0.6087806452432535931 ) ) ;
#23846=CARTESIAN_POINT ( 'NONE',  ( 0.005339406051279861967, -1.804346059958628068, -0.3571184395977468062 ) ) ;
#23849=EDGE_LOOP ( 'NONE', ( #35173, #15920 ) ) ;
#23858=VERTEX_POINT ( 'NONE', #32302 ) ;
#23859=CARTESIAN_POINT ( 'NONE',  ( -1.651713865843977279E-05, -2.061678968352038233, -0.6852225792402809601 ) ) ;
#23862=CIRCLE ( 'NONE', #33021, 0.05330708661417321581 ) ;
#23867=B_SPLINE_CURVE_WITH_KNOTS ( 'NONE', 3,
 ( #15185, #30827, #17860, #33700 ),
 .UNSPECIFIED., .F., .F.,
 ( 4, 4 ),
 ( 1.734723475976807094E-18, 0.0003603784013037980918 ),
 .UNSPECIFIED. ) ;
#23871=CARTESIAN_POINT ( 'NONE',  ( 0.7215184893803678889, -1.528098279142000804, -0.6250000000000000000 ) ) ;
#23881=CARTESIAN_POINT ( 'NONE',  ( 0.3999999999999787059, -2.097675824466503691, -0.5196396315034578217 ) ) ;
#23883=CARTESIAN_POINT ( 'NONE',  ( 0.2284923717121198627, -1.304659949875474068, -0.5155029497116575543 ) ) ;
#23890=CARTESIAN_POINT ( 'NONE',  ( 0.4822598830809305959, -1.683537768409984592, -0.5984293649392239400 ) ) ;
#23898=AXIS2_PLACEMENT_3D ( 'NONE', #38970, #13859, #26436 ) ;
#23902=CARTESIAN_POINT ( 'NONE',  ( 0.3999999999999786504, -1.973385418564556293, -0.6834611762463905782 ) ) ;
#23912=CARTESIAN_POINT ( 'NONE',  ( -2.119743302583864240E-14, -2.097675824466504135, -0.7286991843995639373 ) ) ;
#23915=CARTESIAN_POINT ( 'NONE',  ( 0.4634712904840411762, -1.711704060178987241, -0.5155029497116575543 ) ) ;
#23916=CARTESIAN_POINT ( 'NONE',  ( 0.4189043378923988925, -1.737431724743732753, -0.5872665585884508932 ) ) ;
#23917=CARTESIAN_POINT ( 'NONE',  ( 0.3782552467915779593, -1.656602296218481207, -0.6321311662414380583 ) ) ;
#23923=CARTESIAN_POINT ( 'NONE',  ( 0.3832670810558529984, -1.653853153454119873, -0.3970663464927791098 ) ) ;
#23931=ORIENTED_EDGE ( 'NONE', *, *, #16568, .T. ) ;
#23933=CARTESIAN_POINT ( 'NONE',  ( 0.3822380469604623743, -1.608340248901213965, -0.6174813857019513241 ) ) ;
#23945=CARTESIAN_POINT ( 'NONE',  ( 0.03990608087475910198, -1.702714339505654095, -0.6675373308980625531 ) ) ;
#23961=AXIS2_PLACEMENT_3D ( 'NONE', #35993, #1079, #13589 ) ;
#23965=ORIENTED_EDGE ( 'NONE', *, *, #11155, .T. ) ;
#23970=CARTESIAN_POINT ( 'NONE',  ( 0.3699999999999786793, -2.097675824466503691, -0.4856910779487875196 ) ) ;
#23972=DIRECTION ( 'NONE',  ( 0.4999551463232377313, -0.8660512985181132439, 0.000000000000000000 ) ) ;
#23973=CARTESIAN_POINT ( 'NONE',  ( 0.4125827319849673658, -1.718883513293331555, -0.4950489522355766003 ) ) ;
#23981=CARTESIAN_POINT ( 'NONE',  ( 0.03396956254496814182, -1.810633036012876618, -0.3262169007243910235 ) ) ;
#23998=CARTESIAN_POINT ( 'NONE',  ( 0.3731443575968244608, -1.763008880570848147, -0.4358735606183953837 ) ) ;
#23999=CARTESIAN_POINT ( 'NONE',  ( 0.1890666733121571796, -1.695896060689630946, -0.3290518381478249599 ) ) ;
#24018=VERTEX_POINT ( 'NONE', #17883 ) ;
#24020=CARTESIAN_POINT ( 'NONE',  ( 0.3878952717463541866, -1.820239213664927691, -0.5225022260212327518 ) ) ;
#24023=CARTESIAN_POINT ( 'NONE',  ( 0.3853411735687863326, -1.756807109041631509, -0.4499573014711771846 ) ) ;
#24027=DIRECTION ( 'NONE',  ( 0.4999551463232372317, -0.8660512985181133550, 0.000000000000000000 ) ) ;
#24028=CARTESIAN_POINT ( 'NONE',  ( 0.3900349134625270553, -1.754097501170372775, -0.4603090518067394221 ) ) ;
#24030=DIRECTION ( 'NONE',  ( 0.4999551463232373427, -0.8660512985181134660, 0.000000000000000000 ) ) ;
#24033=CARTESIAN_POINT ( 'NONE',  ( 0.5748241391253147148, -1.612671306764259072, -0.5249618373864313181 ) ) ;
#24042=CARTESIAN_POINT ( 'NONE',  ( 0.3807174028472657956, -1.746516858961833396, -0.5732035964501958070 ) ) ;
#24044=CARTESIAN_POINT ( 'NONE',  ( 0.4382015218937534429, -1.612541052972219724, -0.6615483979664105174 ) ) ;
#24069=AXIS2_PLACEMENT_3D ( 'NONE', #17122, #7845, #35640 ) ;
#24071=CARTESIAN_POINT ( 'NONE',  ( -2.112273405726188513E-14, -2.097675824466503691, -0.6968677163258658602 ) ) ;
#24077=AXIS2_PLACEMENT_3D ( 'NONE', #40289, #31257, #6342 ) ;
#24108=ORIENTED_EDGE ( 'NONE', *, *, #16498, .T. ) ;
#24112=CARTESIAN_POINT ( 'NONE',  ( 0.4634203168357881597, -1.610090559957644274, -0.3776084174194705989 ) ) ;
#24117=VERTEX_POINT ( 'NONE', #242 ) ;
#24135=CARTESIAN_POINT ( 'NONE',  ( 0.1992679972018663592, -1.286890268402110182, -0.7430135000225476238 ) ) ;
#24147=CARTESIAN_POINT ( 'NONE',  ( 0.4540174329365269656, -1.143689243732040728, -0.6344893339101922436 ) ) ;
#24150=CARTESIAN_POINT ( 'NONE',  ( 0.3797463714376327348, -1.760601621700183639, -0.4487751144967741523 ) ) ;
#24152=ORIENTED_EDGE ( 'NONE', *, *, #5851, .F. ) ;
#24154=ORIENTED_EDGE ( 'NONE', *, *, #18726, .T. ) ;
#24155=ORIENTED_EDGE ( 'NONE', *, *, #39929, .F. ) ;
#24156=CARTESIAN_POINT ( 'NONE',  ( 0.09591312667570967010, -1.362172318102457202, -0.6980176222590579460 ) ) ;
#24158=CARTESIAN_POINT ( 'NONE',  ( 0.3591498995103418190, -1.737620376665806932, -0.5147966178037273188 ) ) ;
#24177=CARTESIAN_POINT ( 'NONE',  ( 0.4197981397002149007, -1.708404881074925274, -0.5025783929700992081 ) ) ;
#24188=CARTESIAN_POINT ( 'NONE',  ( 0.1734973056165642902, -1.209394307038482719, -0.5155029497116575543 ) ) ;
#24190=B_SPLINE_CURVE_WITH_KNOTS ( 'NONE', 3,
 ( #25052, #34513, #6323, #32031, #6516, #25261, #25471, #9814, #38199, #13310 ),
 .UNSPECIFIED., .F., .F.,
 ( 4, 2, 2, 2, 4 ),
 ( 0.000000000000000000, 0.0002543125689965293913, 0.0005086251379930587825, 0.0007629377069895881738, 0.001017250275986117565 ),
 .UNSPECIFIED. ) ;
#24202=EDGE_LOOP ( 'NONE', ( #9710, #10514, #2429, #23083 ) ) ;
#24211=ORIENTED_EDGE ( 'NONE', *, *, #34137, .T. ) ;
#24213=CARTESIAN_POINT ( 'NONE',  ( 0.3926986855850684854, -1.778818435110647522, -0.3125573702649511731 ) ) ;
#24215=AXIS2_PLACEMENT_3D ( 'NONE', #6719, #19293, #611 ) ;
#24216=CARTESIAN_POINT ( 'NONE',  ( 0.3939841861132012957, -1.751817660254116893, -0.4710238052775803652 ) ) ;
#24219=DIRECTION ( 'NONE',  ( -0.000000000000000000, -0.9450610163799286756, -0.3268939817722809615 ) ) ;
#24224=CARTESIAN_POINT ( 'NONE',  ( 0.6213544394143908356, -1.618324384172695529, -0.5525161381485133028 ) ) ;
#24225=CARTESIAN_POINT ( 'NONE',  ( 0.1511697332786464953, -1.326440298964499886, -0.7191902533801515229 ) ) ;
#24229=VERTEX_POINT ( 'NONE', #16249 ) ;
#24232=CARTESIAN_POINT ( 'NONE',  ( 0.3630296588320852114, -1.750092887594260960, -0.5972373629894556224 ) ) ;
#24233=CARTESIAN_POINT ( 'NONE',  ( 0.4212767629397370373, -1.592273061960515435, -0.6162690127139324181 ) ) ;
#24239=CARTESIAN_POINT ( 'NONE',  ( 0.6400160853294423191, -1.459529829645036081, -0.3976988710621562895 ) ) ;
#24241=LINE ( 'NONE', #2829, #40306 ) ;
#24245=CARTESIAN_POINT ( 'NONE',  ( 0.1036077641498115154, -1.348975793691512992, -0.3541914004549143180 ) ) ;
#24248=ORIENTED_EDGE ( 'NONE', *, *, #40139, .F. ) ;
#24264=CARTESIAN_POINT ( 'NONE',  ( 0.5010929404620397820, -1.674525211673266956, -0.6058220862217358338 ) ) ;
#24265=ADVANCED_FACE ( 'NONE', ( #28588 ), #4063, .F. ) ;
#24266=EDGE_CURVE ( 'NONE', #9810, #1239, #5908, .T. ) ;
#24267=B_SPLINE_CURVE_WITH_KNOTS ( 'NONE', 1,
 ( #13026, #5814, #25163, #3152 ),
 .UNSPECIFIED., .F., .F.,
 ( 2, 1, 1, 2 ),
 ( -0.0007619999999999863211, 2.168404344971008868E-18, 0.0007619999999999993315, 0.001523999999999991074 ),
 .UNSPECIFIED. ) ;
#24277=CARTESIAN_POINT ( 'NONE',  ( 0.5838486772476066955, -1.549002738031555637, -0.6085822719328981556 ) ) ;
#24280=CARTESIAN_POINT ( 'NONE',  ( 0.4428525721104821233, -1.108557561101682909, -0.3966740480326817475 ) ) ;
#24282=CARTESIAN_POINT ( 'NONE',  ( 0.2747286271120374934, -1.554764607944815635, -0.7171264253415187140 ) ) ;
#24283=CARTESIAN_POINT ( 'NONE',  ( 0.3811173169455821519, -1.749731223830197191, -0.5852530064128164122 ) ) ;
#24284=ORIENTED_EDGE ( 'NONE', *, *, #2167, .F. ) ;
#24287=ORIENTED_EDGE ( 'NONE', *, *, #7196, .F. ) ;
#24288=CARTESIAN_POINT ( 'NONE',  ( 0.4498803379890206067, -1.659323614875797936, -0.3947173143921381411 ) ) ;
#24298=CARTESIAN_POINT ( 'NONE',  ( 0.2469141422421070875, -1.581573626495411444, -0.3511777555542848206 ) ) ;
#24305=EDGE_CURVE ( 'NONE', #2027, #18407, #28261, .T. ) ;
#24309=DIRECTION ( 'NONE',  ( 0.8660512985181133550, 0.4999551463232371207, 0.000000000000000000 ) ) ;
#24311=CARTESIAN_POINT ( 'NONE',  ( 0.3907225962692674193, -1.711934981260601063, -0.4322588514322361908 ) ) ;
#24317=CARTESIAN_POINT ( 'NONE',  ( 0.3907430023610570791, -1.657027545734215179, -0.4094362587932089403 ) ) ;
#24326=EDGE_CURVE ( 'NONE', #34358, #34037, #3946, .T. ) ;
#24334=CARTESIAN_POINT ( 'NONE',  ( 0.3984413745674345031, -1.753413336483850893, -0.5068292923117084792 ) ) ;
#24337=ORIENTED_EDGE ( 'NONE', *, *, #8501, .F. ) ;
#24360=DIRECTION ( 'NONE',  ( -1.000000000000000000, -0.000000000000000000, -0.000000000000000000 ) ) ;
#24362=CARTESIAN_POINT ( 'NONE',  ( 0.3599681117411700493, -1.738096220096565725, -0.5053368274672028759 ) ) ;
#24365=CYLINDRICAL_SURFACE ( 'NONE', #7629, 0.1033070866141734129 ) ;
#24368=CARTESIAN_POINT ( 'NONE',  ( 0.1991480113865250756, -2.054949600705706203, -0.6841806413415671972 ) ) ;
#24371=CARTESIAN_POINT ( 'NONE',  ( 0.4428400309745523233, -1.146281092196613338, -0.3830631589809550541 ) ) ;
#24372=EDGE_LOOP ( 'NONE', ( #37192, #39702, #20059, #23304 ) ) ;
#24377=EDGE_LOOP ( 'NONE', ( #3876, #25887, #23387, #22025 ) ) ;
#24386=CARTESIAN_POINT ( 'NONE',  ( 0.1953882094510071277, -1.994676107002966381, -0.3200132981238684726 ) ) ;
#24388=DIRECTION ( 'NONE',  ( 0.8660512985181133550, 0.4999551463232372872, 0.000000000000000000 ) ) ;
#24393=CARTESIAN_POINT ( 'NONE',  ( 0.3999999999999787059, -2.183180860297921466, -0.5437760292030870968 ) ) ;
#24400=ORIENTED_EDGE ( 'NONE', *, *, #9835, .F. ) ;
#24405=CARTESIAN_POINT ( 'NONE',  ( 0.3831941804535738405, -1.607788291067505870, -0.3198167766998259998 ) ) ;
#24407=CARTESIAN_POINT ( 'NONE',  ( 0.2010877066827159720, -1.651987922488803440, -0.3292090611533607936 ) ) ;
#24411=CARTESIAN_POINT ( 'NONE',  ( 0.3999999999999787059, -2.166079853131637645, -0.4467913981637915422 ) ) ;
#24422=CARTESIAN_POINT ( 'NONE',  ( 0.6169029553321203618, -1.567646591109399523, -0.4433873813970327094 ) ) ;
#24423=CARTESIAN_POINT ( 'NONE',  ( 0.04765665840200696002, -1.630838948795847010, -0.6681089085276715744 ) ) ;
#24433=CARTESIAN_POINT ( 'NONE',  ( 0.4621279655515690976, -1.664766036179415432, -0.6170834442379143914 ) ) ;
#24435=CARTESIAN_POINT ( 'NONE',  ( 0.4685175142989152497, -1.068920175619711976, -0.6082962044498383403 ) ) ;
#24458=ORIENTED_EDGE ( 'NONE', *, *, #22995, .F. ) ;
#24464=CARTESIAN_POINT ( 'NONE',  ( 0.3999999999999787059, -2.143627883852845528, -0.5325888117242426611 ) ) ;
#24469=CARTESIAN_POINT ( 'NONE',  ( 0.2400364630114684983, -2.004548383824730884, -0.6718252909726382116 ) ) ;
#24481=EDGE_LOOP ( 'NONE', ( #9307, #21511, #14828, #35331 ) ) ;
#24485=ORIENTED_EDGE ( 'NONE', *, *, #15935, .F. ) ;
#24493=VERTEX_POINT ( 'NONE', #35492 ) ;
#24505=EDGE_LOOP ( 'NONE', ( #12154, #29397, #25264, #20391 ) ) ;
#24507=CARTESIAN_POINT ( 'NONE',  ( 0.1772434461258276250, -1.460886006248064639, -0.3542314186169536749 ) ) ;
#24513=EDGE_CURVE ( 'NONE', #617, #30709, #7992, .T. ) ;
#24514=CARTESIAN_POINT ( 'NONE',  ( -2.128119112016648632E-14, -2.087870288139423103, -0.7252158372584678325 ) ) ;
#24524=CARTESIAN_POINT ( 'NONE',  ( 0.3428182734493427919, -1.642767540764730416, -0.3789368674292417083 ) ) ;
#24526=AXIS2_PLACEMENT_3D ( 'NONE', #13725, #29381, #4270 ) ;
#24527=CARTESIAN_POINT ( 'NONE',  ( 0.2161879510971927987, -1.277123080371499242, -0.7187326247832955817 ) ) ;
#24539=CARTESIAN_POINT ( 'NONE',  ( 0.3395458163374477922, -1.664374608384261878, -0.3921577936940786602 ) ) ;
#24543=EDGE_CURVE ( 'NONE', #4931, #21660, #2618, .T. ) ;
#24550=ORIENTED_EDGE ( 'NONE', *, *, #6683, .F. ) ;
#24551=CARTESIAN_POINT ( 'NONE',  ( 0.1734973056165642902, -1.209394307038482497, -0.5155029497116575543 ) ) ;
#24553=LINE ( 'NONE', #28047, #8825 ) ;
#24571=DIRECTION ( 'NONE',  ( 0.4999551463232372317, -0.8660512985181134660, 0.000000000000000000 ) ) ;
#24580=CARTESIAN_POINT ( 'NONE',  ( 0.3594221198575611176, -1.931599736257602284, -0.6668497031992260959 ) ) ;
#24587=DIRECTION ( 'NONE',  ( 0.4999551463232373427, -0.8660512985181134660, 0.000000000000000000 ) ) ;
#24600=CARTESIAN_POINT ( 'NONE',  ( 0.3699999999999789013, -2.087706782572656738, -0.4706861924077629378 ) ) ;
#24601=CARTESIAN_POINT ( 'NONE',  ( 0.3644626074408009453, -1.765287842794585726, -0.5889622461435645162 ) ) ;
#24614=LINE ( 'NONE', #32881, #31000 ) ;
#24615=EDGE_CURVE ( 'NONE', #556, #7985, #16469, .T. ) ;
#24620=CARTESIAN_POINT ( 'NONE',  ( 0.3871477414013556606, -1.840016465421978165, -0.5197212197501380748 ) ) ;
#24631=CARTESIAN_POINT ( 'NONE',  ( 0.6260846371513943964, -1.362782225785380996, -0.6250000000000000000 ) ) ;
#24632=CARTESIAN_POINT ( 'NONE',  ( 0.4184753273149497965, -1.633759443312357007, -0.5155029497116575543 ) ) ;
#24633=TOROIDAL_SURFACE ( 'NONE', #18713, 0.2200000000000000566, 0.02999999999999999889 ) ;
#24637=CARTESIAN_POINT ( 'NONE',  ( 0.6626821769541543228, -1.455497439629167777, -0.4141230538711661580 ) ) ;
#24643=CARTESIAN_POINT ( 'NONE',  ( 0.3596447502321097334, -1.738446402475701591, -0.5125164628055072225 ) ) ;
#24644=CARTESIAN_POINT ( 'NONE',  ( 0.4034397895666202993, -1.737305379259379334, -0.5960298613879961849 ) ) ;
#24652=CARTESIAN_POINT ( 'NONE',  ( 0.5137479461421968763, -1.668697091725908521, -0.5969086590007808280 ) ) ;
#24659=CARTESIAN_POINT ( 'NONE',  ( 0.5269601233575494925, -1.601707680730814598, -0.5991548076442045900 ) ) ;
#24661=ORIENTED_EDGE ( 'NONE', *, *, #2147, .T. ) ;
#24667=B_SPLINE_CURVE_WITH_KNOTS ( 'NONE', 3,
 ( #29718, #8105, #4805, #17590 ),
 .UNSPECIFIED., .F., .F.,
 ( 4, 4 ),
 ( 0.4469892262121280546, 0.5550469413684232522 ),
 .UNSPECIFIED. ) ;
#24680=CARTESIAN_POINT ( 'NONE',  ( 0.5875120920308054551, -1.532572385145595684, -0.4099296195555359179 ) ) ;
#24681=CARTESIAN_POINT ( 'NONE',  ( 0.4409062655693438137, -1.690090444797295977, -0.2869361388274795921 ) ) ;
#24686=CARTESIAN_POINT ( 'NONE',  ( 0.2219773688075763474, -1.468623658325240333, -0.6797324060620716368 ) ) ;
#24717=CARTESIAN_POINT ( 'NONE',  ( 0.4167269056019572426, -1.703721376542429722, -0.4188292666922682761 ) ) ;
#24719=EDGE_LOOP ( 'NONE', ( #11383, #39045, #23022, #30359 ) ) ;
#24720=CARTESIAN_POINT ( 'NONE',  ( 0.4795819664771983071, -1.106247336020415917, -0.4111404562665418871 ) ) ;
#24729=CARTESIAN_POINT ( 'NONE',  ( 0.4611095784274710785, -1.074565241972302410, -0.4179763115151196029 ) ) ;
#24746=CARTESIAN_POINT ( 'NONE',  ( 0.3439082139226234403, -1.634872185475882533, -0.4352343451533515206 ) ) ;
#24752=CARTESIAN_POINT ( 'NONE',  ( 0.2134937173224229212, -1.278678410919930730, -0.5155029497116575543 ) ) ;
#24758=CARTESIAN_POINT ( 'NONE',  ( 0.3543612153453276070, -1.726706594326277822, -0.5324466127738753940 ) ) ;
#24765=CARTESIAN_POINT ( 'NONE',  ( 0.2211959769661342168, -1.309495541150525799, -0.4400554600884077350 ) ) ;
#24776=CIRCLE ( 'NONE', #28062, 0.1033070866141734129 ) ;
#24784=CARTESIAN_POINT ( 'NONE',  ( 0.02319709399062810581, -1.613360830953564973, -0.6353126625343105127 ) ) ;
#24789=FACE_OUTER_BOUND ( 'NONE', #6930, .T. ) ;
#24790=AXIS2_PLACEMENT_3D ( 'NONE', #5588, #12378, #24933 ) ;
#24791=CARTESIAN_POINT ( 'NONE',  ( 0.1959911413068460284, -1.662491970225822735, -0.6568654529857578250 ) ) ;
#24795=VERTEX_POINT ( 'NONE', #16152 ) ;
#24799=CARTESIAN_POINT ( 'NONE',  ( 0.1999999999999789724, -2.183180860297921466, -0.4937760292030871079 ) ) ;
#24808=CARTESIAN_POINT ( 'NONE',  ( 0.2764337282391428618, -1.207704344519209938, -0.5166151207188711680 ) ) ;
#24812=ORIENTED_EDGE ( 'NONE', *, *, #13480, .F. ) ;
#24820=CARTESIAN_POINT ( 'NONE',  ( 0.3234194364778873454, -1.642295127928019793, -0.6168578883319564277 ) ) ;
#24822=CARTESIAN_POINT ( 'NONE',  ( 0.1963639982240613369, -1.999069888237751780, -0.2881341410394136493 ) ) ;
#24827=ORIENTED_EDGE ( 'NONE', *, *, #29544, .T. ) ;
#24837=CARTESIAN_POINT ( 'NONE',  ( 0.6355919355275447824, -1.485218526194229005, -0.3957663088022824738 ) ) ;
#24841=CARTESIAN_POINT ( 'NONE',  ( 0.1909286924077255032, -1.257064795538239022, -0.3194753470178354759 ) ) ;
#24845=CARTESIAN_POINT ( 'NONE',  ( 0.4089074357954356476, -1.710833460744737078, -0.6076181741210081588 ) ) ;
#24846=ADVANCED_FACE ( 'NONE', ( #28689 ), #10553, .T. ) ;
#24848=CARTESIAN_POINT ( 'NONE',  ( 0.5542431180310618544, -1.624464136724068419, -0.4644229827488332574 ) ) ;
#24849=CARTESIAN_POINT ( 'NONE',  ( 0.3992403239432265050, -1.683235622436123125, -0.6263438071736147084 ) ) ;
#24850=EDGE_CURVE ( 'NONE', #3583, #394, #2025, .T. ) ;
#24851=ORIENTED_EDGE ( 'NONE', *, *, #34825, .T. ) ;
#24852=CARTESIAN_POINT ( 'NONE',  ( 0.4867251962510779073, -1.680960026995275802, -0.6125153944540090434 ) ) ;
#24858=CARTESIAN_POINT ( 'NONE',  ( 0.4517786694993131680, -1.612323574982035712, -0.6578841968208716251 ) ) ;
#24860=VERTEX_POINT ( 'NONE', #6046 ) ;
#24862=AXIS2_PLACEMENT_3D ( 'NONE', #36172, #39268, #23465 ) ;
#24875=CARTESIAN_POINT ( 'NONE',  ( 0.2049227550019952493, -1.874964159105817485, -0.3434029161829166843 ) ) ;
#24876=CARTESIAN_POINT ( 'NONE',  ( 0.4409062655693438137, -1.690090444797295977, -0.7462941026102624109 ) ) ;
#24878=EDGE_CURVE ( 'NONE', #8354, #3740, #732, .T. ) ;
#24880=ADVANCED_FACE ( 'NONE', ( #19634 ), #37967, .F. ) ;
#24882=DIRECTION ( 'NONE',  ( -0.2681551574199820265, -0.1548009352265700411, -0.9508572353419014744 ) ) ;
#24893=CARTESIAN_POINT ( 'NONE',  ( 0.2198247498919005116, -1.608236751325475167, -0.6963561265924880228 ) ) ;
#24894=CARTESIAN_POINT ( 'NONE',  ( 0.1909286924077256420, -1.257064795538239244, -0.2869361388274796476 ) ) ;
#24901=CARTESIAN_POINT ( 'NONE',  ( 0.1999999999999794720, -2.107936428766273629, -0.2870436526301871627 ) ) ;
#24922=CARTESIAN_POINT ( 'NONE',  ( 0.4650292090997563133, -1.068238633521630732, -0.4213092890091242881 ) ) ;
#24927=DIRECTION ( 'NONE',  ( 0.000000000000000000, -0.3420201433256721546, 0.9396926207859070956 ) ) ;
#24933=DIRECTION ( 'NONE',  ( 0.8660512985181134660, 0.4999551463232372317, 0.000000000000000000 ) ) ;
#24957=VERTEX_POINT ( 'NONE', #13842 ) ;
#24961=CARTESIAN_POINT ( 'NONE',  ( 0.4093192649698301211, -1.477391824278449395, -0.4706793243405929528 ) ) ;
#24977=EDGE_CURVE ( 'NONE', #12681, #38249, #25645, .T. ) ;
#24985=CARTESIAN_POINT ( 'NONE',  ( 0.3625773210575073957, -1.777458267349059540, -0.3444665025425360239 ) ) ;
#25001=ORIENTED_EDGE ( 'NONE', *, *, #28244, .F. ) ;
#25018=AXIS2_PLACEMENT_3D ( 'NONE', #36732, #21715, #6273 ) ;
#25019=CARTESIAN_POINT ( 'NONE',  ( 0.6213533671482026621, -1.618071575169615306, -0.4781682850753038450 ) ) ;
#25023=DIRECTION ( 'NONE',  ( 0.8660512985181130219, 0.4999551463232378978, 0.000000000000000000 ) ) ;
#25027=CARTESIAN_POINT ( 'NONE',  ( 0.3623340787431935106, -1.967984212679734446, -0.5065714937396946782 ) ) ;
#25035=EDGE_CURVE ( 'NONE', #2123, #13011, #15164, .T. ) ;
#25045=CARTESIAN_POINT ( 'NONE',  ( 0.09473499835993481888, -1.365368924775509196, -0.3575598482871295558 ) ) ;
#25046=VERTEX_POINT ( 'NONE', #2339 ) ;
#25047=EDGE_LOOP ( 'NONE', ( #19232, #17450, #31600, #3384, #5591, #40517, #11725, #5402, #37594 ) ) ;
#25052=CARTESIAN_POINT ( 'NONE',  ( 0.3595715536228106801, -1.625401886829162423, -0.3696110269036073093 ) ) ;
#25055=CIRCLE ( 'NONE', #14528, 0.2500000000000000000 ) ;
#25056=ORIENTED_EDGE ( 'NONE', *, *, #24266, .T. ) ;
#25062=CARTESIAN_POINT ( 'NONE',  ( 0.7059656540691128246, -1.571716619208481935, -0.5155029497116575543 ) ) ;
#25063=CARTESIAN_POINT ( 'NONE',  ( 0.6089330441038812713, -1.477473485466218150, -0.6250000000000000000 ) ) ;
#25071=CARTESIAN_POINT ( 'NONE',  ( 0.1708500036367240627, -1.718699357903690439, -0.6511465918194946356 ) ) ;
#25072=CARTESIAN_POINT ( 'NONE',  ( 0.3533584531583440214, -1.730880459003149907, -0.4486410610578602243 ) ) ;
#25078=CARTESIAN_POINT ( 'NONE',  ( 0.5114126470110640366, -1.614748454822723556, -0.5166151207188711680 ) ) ;
#25085=CARTESIAN_POINT ( 'NONE',  ( 0.3771763907541850758, -1.752869764700489830, -0.5848310859449704635 ) ) ;
#25087=VERTEX_POINT ( 'NONE', #11784 ) ;
#25101=DIRECTION ( 'NONE',  ( -0.9877995450870419303, -0.03415031169247099291, 0.1519401689387651910 ) ) ;
#25102=EDGE_CURVE ( 'NONE', #35001, #4931, #34965, .T. ) ;
#25103=CARTESIAN_POINT ( 'NONE',  ( 0.3956641542645719656, -1.754140676906325469, -0.4988858376329875499 ) ) ;
#25105=AXIS2_PLACEMENT_3D ( 'NONE', #10435, #19899, #1214 ) ;
#25107=ORIENTED_EDGE ( 'NONE', *, *, #21504, .T. ) ;
#25109=CARTESIAN_POINT ( 'NONE',  ( 0.4661081799873099119, -1.093130792299548570, -0.4039132814442666364 ) ) ;
#25114=( BOUNDED_SURFACE ( )  B_SPLINE_SURFACE ( 3, 2, ( 
 ( #30579, #5253, #21117 ),
 ( #12265, #5673, #2197 ),
 ( #21721, #30371, #21332 ),
 ( #36737, #12059, #15345 ),
 ( #27901, #40224, #34059 ),
 ( #27303, #28105, #24822 ),
 ( #15557, #8356, #27690 ),
 ( #18416, #18017, #11843 ),
 ( #33647, #40442, #40633 ),
 ( #20925, #2403, #17809 ),
 ( #2592, #33869, #3009 ),
 ( #24620, #37345, #39832 ),
 ( #24020, #37155, #36544 ),
 ( #11653, #24213, #8966 ),
 ( #9156, #30775, #18228 ),
 ( #21540, #34253, #8546 ),
 ( #5859, #2797, #6067 ),
 ( #40020, #5457, #18634 ),
 ( #14942, #27494, #24407 ),
 ( #36942, #34863, #154 ),
 ( #3805, #13268, #32183 ),
 ( #3607, #34465, #16361 ),
 ( #16174, #3197, #21939 ),
 ( #9773, #9359, #19650 ),
 ( #6476, #37963, #22346 ),
 ( #22759, #370, #3995 ),
 ( #16557, #6281, #25211 ),
 ( #9978, #37756, #19250 ) ),
 .UNSPECIFIED., .F., .F., .F. ) 
 B_SPLINE_SURFACE_WITH_KNOTS ( ( 4, 2, 2, 2, 2, 2, 2, 2, 2, 2, 2, 2, 2, 4 ),
 ( 3, 3 ),
 ( 0.03544507920328695411, 0.03595486840377590254, 0.03646465760426484404, 0.03748423600524272703, 0.03952339280719850689, 0.04156254960915428676, 0.04360170641111006662, 0.04462128481208795655, 0.04564086321306584648, 0.04768002001502162635, 0.04869959841599951628, 0.04971917681697740621, 0.05073875521795528920, 0.05175833361893317913 ),
 ( 0.000000000000000000, 1.000000000000000000 ),
 .UNSPECIFIED. ) 
 GEOMETRIC_REPRESENTATION_ITEM ( )  RATIONAL_B_SPLINE_SURFACE ( (
 ( 1.000000000000000000, 0.7061763356917282186, 1.000000000000000000),
 ( 1.000000000000000000, 0.7080421523057206512, 1.000000000000000000),
 ( 1.000000000000000000, 0.7088516299600281512, 1.000000000000000000),
 ( 1.000000000000000000, 0.7099244856010550331, 1.000000000000000000),
 ( 1.000000000000000000, 0.7101378557341009312, 1.000000000000000000),
 ( 1.000000000000000000, 0.7103445576143324613, 1.000000000000000000),
 ( 1.000000000000000000, 0.7098994762787452784, 1.000000000000000000),
 ( 1.000000000000000000, 0.7079279405282515869, 1.000000000000000000),
 ( 1.000000000000000000, 0.7057284653323193657, 1.000000000000000000),
 ( 1.000000000000000000, 0.7007157790496724159, 1.000000000000000000),
 ( 1.000000000000000000, 0.6978342510162854895, 1.000000000000000000),
 ( 1.000000000000000000, 0.6916754492645512675, 1.000000000000000000),
 ( 1.000000000000000000, 0.6883795134656507386, 1.000000000000000000),
 ( 1.000000000000000000, 0.6835032746938722870, 1.000000000000000000),
 ( 1.000000000000000000, 0.6818926907722926423, 1.000000000000000000),
 ( 1.000000000000000000, 0.6788412388327813574, 1.000000000000000000),
 ( 1.000000000000000000, 0.6773936298796078281, 1.000000000000000000),
 ( 1.000000000000000000, 0.6736810316134569376, 1.000000000000000000),
 ( 1.000000000000000000, 0.6720343155085293230, 1.000000000000000000),
 ( 1.000000000000000000, 0.6725111439841665595, 1.000000000000000000),
 ( 1.000000000000000000, 0.6731816333784569339, 1.000000000000000000),
 ( 1.000000000000000000, 0.6757599976965816824, 1.000000000000000000),
 ( 1.000000000000000000, 0.6776668555842312314, 1.000000000000000000),
 ( 1.000000000000000000, 0.6829223581645637031, 1.000000000000000000),
 ( 1.000000000000000000, 0.6862934035413942313, 1.000000000000000000),
 ( 1.000000000000000000, 0.6945721712650552160, 1.000000000000000000),
 ( 1.000000000000000000, 0.6994068901145212847, 1.000000000000000000),
 ( 1.000000000000000000, 0.7048795877316381686, 1.000000000000000000) ) ) 
 REPRESENTATION_ITEM ( '' )  SURFACE ( )  );
#25115=AXIS2_PLACEMENT_3D ( 'NONE', #12170, #28013, #34584 ) ;
#25119=AXIS2_PLACEMENT_3D ( 'NONE', #18831, #31375, #36918 ) ;
#25123=CARTESIAN_POINT ( 'NONE',  ( 0.4159916692016358830, -1.069406866067976081, -0.5155029497116575543 ) ) ;
#25134=DIRECTION ( 'NONE',  ( -0.4999551463232372317, 0.8660512985181135770, -0.000000000000000000 ) ) ;
#25148=VERTEX_POINT ( 'NONE', #11378 ) ;
#25150=CARTESIAN_POINT ( 'NONE',  ( 0.3330378571917648745, -1.679292210583121170, -0.6251523164888654893 ) ) ;
#25151=TOROIDAL_SURFACE ( 'NONE', #39610, 0.08830708661417323302, 0.01499999999999999944 ) ;
#25155=ORIENTED_EDGE ( 'NONE', *, *, #33932, .T. ) ;
#25163=CARTESIAN_POINT ( 'NONE',  ( 0.1909286924077255032, -1.257064795538239022, -0.6184399470714002645 ) ) ;
#25177=CARTESIAN_POINT ( 'NONE',  ( 0.6409058204046232943, -1.459016202299332710, -0.5155029497116575543 ) ) ;
#25189=VERTEX_POINT ( 'NONE', #30296 ) ;
#25190=ORIENTED_EDGE ( 'NONE', *, *, #31331, .F. ) ;
#25194=ORIENTED_EDGE ( 'NONE', *, *, #26247, .F. ) ;
#25206=CARTESIAN_POINT ( 'NONE',  ( 0.5058599984363494340, -1.583313914148366752, -0.4933326546058601214 ) ) ;
#25211=CARTESIAN_POINT ( 'NONE',  ( 0.2831656786010217641, -1.548301601687314788, -0.3099957012843251869 ) ) ;
#25218=ADVANCED_FACE ( 'NONE', ( #27232 ), #40354, .F. ) ;
#25225=EDGE_CURVE ( 'NONE', #34108, #37380, #790, .T. ) ;
#25226=CARTESIAN_POINT ( 'NONE',  ( 0.6448693075501473748, -1.567563692131277220, -0.4251249543968058653 ) ) ;
#25227=CARTESIAN_POINT ( 'NONE',  ( 0.3993946999846398893, -2.070215760155117213, -0.4742227968861380538 ) ) ;
#25234=ORIENTED_EDGE ( 'NONE', *, *, #18289, .T. ) ;
#25237=FACE_OUTER_BOUND ( 'NONE', #13806, .T. ) ;
#25238=DIRECTION ( 'NONE',  ( 0.4999551463232373427, -0.8660512985181134660, 0.000000000000000000 ) ) ;
#25241=CARTESIAN_POINT ( 'NONE',  ( 0.3639089045978470272, -1.623236563750744876, -0.6630443531552572267 ) ) ;
#25242=ADVANCED_FACE ( 'NONE', ( #15493 ), #1058, .T. ) ;
#25256=CIRCLE ( 'NONE', #7493, 0.2200000000000001121 ) ;
#25261=CARTESIAN_POINT ( 'NONE',  ( 0.3439881215215967458, -1.640653147150704871, -0.3778432901105419073 ) ) ;
#25263=ORIENTED_EDGE ( 'NONE', *, *, #16957, .T. ) ;
#25264=ORIENTED_EDGE ( 'NONE', *, *, #14263, .F. ) ;
#25271=CARTESIAN_POINT ( 'NONE',  ( 0.1094055670226265625, -1.326767981663566243, -0.3565224830446982462 ) ) ;
#25274=CARTESIAN_POINT ( 'NONE',  ( 0.4334739817046469601, -1.659740982267900566, -0.5155029497116575543 ) ) ;
#25276=CARTESIAN_POINT ( 'NONE',  ( 0.5949938736933503280, -1.485520306704343207, -0.4218885508374648485 ) ) ;
#25280=FACE_OUTER_BOUND ( 'NONE', #13453, .T. ) ;
#25282=CARTESIAN_POINT ( 'NONE',  ( 0.1630182088513137673, -1.785047172228910517, -0.6488655176575248706 ) ) ;
#25299=CARTESIAN_POINT ( 'NONE',  ( 0.1937395639937359026, -1.657857108843001193, -0.6872458559241637621 ) ) ;
#25321=CARTESIAN_POINT ( 'NONE',  ( -2.112273405726188513E-14, -1.837418632672298768, -0.6339733133327630776 ) ) ;
#25324=TOROIDAL_SURFACE ( 'NONE', #8207, 0.1333070866141734256, 0.02999999999999999889 ) ;
#25325=CARTESIAN_POINT ( 'NONE',  ( 0.1960722456818423942, -1.288731303253011218, -0.2917126172454974631 ) ) ;
#25344=ADVANCED_FACE ( 'NONE', ( #38841 ), #1645, .T. ) ;
#25353=ORIENTED_EDGE ( 'NONE', *, *, #15426, .T. ) ;
#25363=ADVANCED_FACE ( 'NONE', ( #20155 ), #36218, .T. ) ;
#25367=CARTESIAN_POINT ( 'NONE',  ( 0.4093192649698303431, -1.477391824278450061, -0.4706793243405929528 ) ) ;
#25368=( BOUNDED_SURFACE ( )  B_SPLINE_SURFACE ( 3, 2, ( 
 ( #36652, #5162, #1719 ),
 ( #17715, #14236, #2310 ),
 ( #14629, #4965, #33544 ),
 ( #27200, #2092, #2511 ) ),
 .UNSPECIFIED., .F., .F., .T. ) 
 B_SPLINE_SURFACE_WITH_KNOTS ( ( 4, 4 ),
 ( 3, 3 ),
 ( -2.862293735361731706E-17, 0.001825051142017923740 ),
 ( 0.000000000000000000, 1.000000000000000000 ),
 .UNSPECIFIED. ) 
 GEOMETRIC_REPRESENTATION_ITEM ( )  RATIONAL_B_SPLINE_SURFACE ( (
 ( 1.000000000000000000, 0.7061763356917307721, 1.000000000000000000),
 ( 1.000000000000000000, 0.7067362331337545545, 1.000000000000000000),
 ( 1.000000000000000000, 0.7071034392571972083, 1.000000000000000000),
 ( 1.000000000000000000, 0.7071067811865461294, 1.000000000000000000) ) ) 
 REPRESENTATION_ITEM ( '' )  SURFACE ( )  );
#25371=CARTESIAN_POINT ( 'NONE',  ( 0.6277577389591226797, -1.601617165483917971, -0.5786592524461142695 ) ) ;
#25376=CARTESIAN_POINT ( 'NONE',  ( 0.4358024118727818474, -1.610872297623142879, -0.3687891571712654804 ) ) ;
#25393=EDGE_CURVE ( 'NONE', #8912, #5500, #2104, .T. ) ;
#25414=CARTESIAN_POINT ( 'NONE',  ( 0.2988334432509203720, -1.539938620923237300, -0.3360421071361874845 ) ) ;
#25416=CARTESIAN_POINT ( 'NONE',  ( 0.6413879784614744395, -1.405912376546664122, -0.6250000000000000000 ) ) ;
#25428=CARTESIAN_POINT ( 'NONE',  ( 0.4625514705274676452, -1.592010743194695932, -0.4306025673467906434 ) ) ;
#25432=CARTESIAN_POINT ( 'NONE',  ( 0.3999999999999785949, -2.097675824466503247, -0.7286991843995642704 ) ) ;
#25445=CARTESIAN_POINT ( 'NONE',  ( 0.4780249079440049287, -1.118244978643492260, -0.3962549247049245715 ) ) ;
#25449=VERTEX_POINT ( 'NONE', #14780 ) ;
#25456=CARTESIAN_POINT ( 'NONE',  ( 0.5350387257620740078, -1.658384496898128724, -0.5719998859210704278 ) ) ;
#25470=DIRECTION ( 'NONE',  ( 0.4999551463232377313, -0.8660512985181132439, -0.000000000000000000 ) ) ;
#25471=CARTESIAN_POINT ( 'NONE',  ( 0.3425551896464547053, -1.643320776792971616, -0.3792307086401233152 ) ) ;
#25478=CARTESIAN_POINT ( 'NONE',  ( 0.1619657438594586940, -1.395601528504655020, -0.3525121130699213623 ) ) ;
#25480=CARTESIAN_POINT ( 'NONE',  ( 0.3513236816452379729, -1.665692895111267058, -0.7210133640968660051 ) ) ;
#25485=CARTESIAN_POINT ( 'NONE',  ( 0.1974703294706521284, -2.027200055516245047, -0.7082635437208197882 ) ) ;
#25498=FACE_OUTER_BOUND ( 'NONE', #21868, .T. ) ;
#25500=AXIS2_PLACEMENT_3D ( 'NONE', #10236, #29361, #20109 ) ;
#25501=ORIENTED_EDGE ( 'NONE', *, *, #11146, .T. ) ;
#25522=EDGE_CURVE ( 'NONE', #3740, #29449, #38825, .T. ) ;
#25535=DIRECTION ( 'NONE',  ( 0.4999551463232372317, -0.8660512985181135770, 0.000000000000000000 ) ) ;
#25544=CARTESIAN_POINT ( 'NONE',  ( 0.1856681452801951515, -1.696504954290812606, -0.6536319978138861453 ) ) ;
#25550=VERTEX_POINT ( 'NONE', #21574 ) ;
#25557=VERTEX_POINT ( 'NONE', #9013 ) ;
#25574=FACE_OUTER_BOUND ( 'NONE', #13410, .T. ) ;
#25584=EDGE_CURVE ( 'NONE', #9058, #33739, #5306, .T. ) ;
#25592=B_SPLINE_CURVE_WITH_KNOTS ( 'NONE', 3,
 ( #11346, #14848, #11753, #40124, #17914, #23916 ),
 .UNSPECIFIED., .F., .F.,
 ( 4, 2, 4 ),
 ( 0.0001712049647610483895, 0.0007981265351246958793, 0.001425048105488343261 ),
 .UNSPECIFIED. ) ;
#25595=CARTESIAN_POINT ( 'NONE',  ( 0.2511799810870077310, -1.337738304023724512, -0.3144976166544468099 ) ) ;
#25616=CARTESIAN_POINT ( 'NONE',  ( 0.4243666725459965261, -1.591076223527387423, -0.4156371400837811647 ) ) ;
#25618=CARTESIAN_POINT ( 'NONE',  ( 0.3139698647411150456, -1.647750188186495768, -0.3722908259404185127 ) ) ;
#25621=CARTESIAN_POINT ( 'NONE',  ( 0.1989976604547400996, -2.047409678865566018, -0.7132172901365276818 ) ) ;
#25631=EDGE_CURVE ( 'NONE', #28758, #40101, #29142, .T. ) ;
#25636=CARTESIAN_POINT ( 'NONE',  ( 0.1999999999999789724, -2.183180860297921466, -0.4937760292030871079 ) ) ;
#25639=B_SPLINE_CURVE_WITH_KNOTS ( 'NONE', 3,
 ( #36743, #6287, #30587, #33879, #24631, #37162 ),
 .UNSPECIFIED., .F., .F.,
 ( 4, 2, 4 ),
 ( 0.004447844280125260071, 0.005140701078120121607, 0.005833557876114983144 ),
 .UNSPECIFIED. ) ;
#25641=AXIS2_PLACEMENT_3D ( 'NONE', #23883, #23282, #35804 ) ;
#25645=B_SPLINE_CURVE_WITH_KNOTS ( 'NONE', 3,
 ( #20251, #20439, #38950, #35452 ),
 .UNSPECIFIED., .F., .F.,
 ( 4, 4 ),
 ( 0.000000000000000000, 0.001408481125205278926 ),
 .UNSPECIFIED. ) ;
#25652=CARTESIAN_POINT ( 'NONE',  ( 0.3991893380402145586, -1.748812823822652129, -0.5227832640171824474 ) ) ;
#25661=ORIENTED_EDGE ( 'NONE', *, *, #39, .F. ) ;
#25668=ORIENTED_EDGE ( 'NONE', *, *, #8817, .T. ) ;
#25672=EDGE_LOOP ( 'NONE', ( #6659, #24287, #40252, #30822 ) ) ;
#25673=CARTESIAN_POINT ( 'NONE',  ( 0.3838614819971074565, -1.826137710545491899, -0.5214446907161387479 ) ) ;
#25674=DIRECTION ( 'NONE',  ( 1.000000000000000000, 0.000000000000000000, 0.000000000000000000 ) ) ;
#25680=CARTESIAN_POINT ( 'NONE',  ( 0.03333333333331219700, -2.097675824466503691, -0.2588528740066097233 ) ) ;
#25683=DIRECTION ( 'NONE',  ( 0.4999551463232372317, -0.8660512985181133550, 0.000000000000000000 ) ) ;
#25685=CARTESIAN_POINT ( 'NONE',  ( 0.3391087009220875581, -1.665264393586757485, -0.3926146152733260286 ) ) ;
#25694=CARTESIAN_POINT ( 'NONE',  ( 0.4208428299034849274, -1.590742573860040920, -0.4148732612168254397 ) ) ;
#25699=CARTESIAN_POINT ( 'NONE',  ( 0.3760351885562676078, -1.762179279381405061, -0.5696997652324907735 ) ) ;
#25703=AXIS2_PLACEMENT_3D ( 'NONE', #15132, #17944, #26628 ) ;
#25706=VERTEX_POINT ( 'NONE', #35928 ) ;
#25708=CARTESIAN_POINT ( 'NONE',  ( 0.4149386519513223459, -1.589462803974980076, -0.6474370376047597908 ) ) ;
#25715=CARTESIAN_POINT ( 'NONE',  ( 0.03069864901531152435, -1.915872880763735742, -0.3084851516908380664 ) ) ;
#25719=CARTESIAN_POINT ( 'NONE',  ( 0.5399038930177495477, -1.667580954481910904, -0.5371941175943450997 ) ) ;
#25721=B_SPLINE_CURVE_WITH_KNOTS ( 'NONE', 3,
 ( #8405, #17665, #30030, #21172, #10906, #1663, #26749, #24264, #23475, #23660 ),
 .UNSPECIFIED., .F., .F.,
 ( 4, 2, 2, 2, 4 ),
 ( 0.000000000000000000, 0.0006458916093408944735, 0.001291783218681788947, 0.001937674828022683312, 0.002583566437363577894 ),
 .UNSPECIFIED. ) ;
#25728=VECTOR ( 'NONE', #8401, 39.37007874015748143 ) ;
#25744=CARTESIAN_POINT ( 'NONE',  ( 0.3740582401036630644, -1.700298052928095549, -0.6903158886021862894 ) ) ;
#25745=EDGE_CURVE ( 'NONE', #3583, #16852, #20696, .T. ) ;
#25748=CARTESIAN_POINT ( 'NONE',  ( 0.1424029337235096226, -1.400533250147911746, -0.3244367222852112542 ) ) ;
#25762=DIRECTION ( 'NONE',  ( 0.4999551463232377313, -0.8660512985181132439, -0.000000000000000000 ) ) ;
#25763=AXIS2_PLACEMENT_3D ( 'NONE', #30771, #18414, #4901 ) ;
#25765=CIRCLE ( 'NONE', #39532, 0.1699999999999999845 ) ;
#25779=CARTESIAN_POINT ( 'NONE',  ( 0.6379434532176896377, -1.610984557999281419, -0.4725373545200265979 ) ) ;
#25784=CARTESIAN_POINT ( 'NONE',  ( 0.4738838377074015562, -1.632444973519838971, -0.6081242360855458884 ) ) ;
#25790=CARTESIAN_POINT ( 'NONE',  ( 0.4631130424841433668, -1.102114521487385757, -0.3875800985506998031 ) ) ;
#25805=CARTESIAN_POINT ( 'NONE',  ( 0.1796683189498666788, -1.379020643267101498, -0.3452591383903352851 ) ) ;
#25812=ORIENTED_EDGE ( 'NONE', *, *, #17128, .F. ) ;
#25827=CARTESIAN_POINT ( 'NONE',  ( 0.4390726440607947700, -1.640987763579620617, -0.4103404039523522728 ) ) ;
#25850=ORIENTED_EDGE ( 'NONE', *, *, #23073, .T. ) ;
#25857=EDGE_CURVE ( 'NONE', #24860, #4952, #20490, .T. ) ;
#25858=CARTESIAN_POINT ( 'NONE',  ( -2.112273405726188513E-14, -2.183180860297921466, -0.4937760292030871079 ) ) ;
#25859=CARTESIAN_POINT ( 'NONE',  ( 0.4099162622095676722, -1.645682601181238436, -0.3971641022030795165 ) ) ;
#25887=ORIENTED_EDGE ( 'NONE', *, *, #38868, .T. ) ;
#25889=B_SPLINE_CURVE_WITH_KNOTS ( 'NONE', 3,
 ( #30595, #14955, #27509, #39635, #36563, #40033 ),
 .UNSPECIFIED., .F., .F.,
 ( 4, 2, 4 ),
 ( 0.000000000000000000, 0.0008310496493514948207, 0.001662099298702989641 ),
 .UNSPECIFIED. ) ;
#25892=CIRCLE ( 'NONE', #12102, 0.1333070866141734534 ) ;
#25893=CARTESIAN_POINT ( 'NONE',  ( 0.3031943397128461504, -1.538683866714745996, -0.7284286296668287530 ) ) ;
#25897=AXIS2_PLACEMENT_3D ( 'NONE', #27706, #40239, #37551 ) ;
#25899=CARTESIAN_POINT ( 'NONE',  ( 0.1049118822781112403, -1.346279903101843534, -0.6713530932235223236 ) ) ;
#25905=CARTESIAN_POINT ( 'NONE',  ( 0.6376027386425543453, -1.480971300301067384, -0.6353011510804285056 ) ) ;
#25910=PLANE ( 'NONE',  #21238 ) ;
#25913=AXIS2_PLACEMENT_3D ( 'NONE', #7300, #6913, #10223 ) ;
#25914=CARTESIAN_POINT ( 'NONE',  ( 0.02999923155047439643, -2.091072551548296854, -0.2612331489864342937 ) ) ;
#25915=CARTESIAN_POINT ( 'NONE',  ( 0.5605867575437351036, -1.621001144914625991, -0.5473203437262892379 ) ) ;
#25924=CARTESIAN_POINT ( 'NONE',  ( 0.5887170121326058547, -1.595259432128637966, -0.4420053674003829314 ) ) ;
#25930=CARTESIAN_POINT ( 'NONE',  ( 0.3365096318212707494, -1.698808709566205444, -0.6091315585829111257 ) ) ;
#25931=EDGE_LOOP ( 'NONE', ( #40244, #8309 ) ) ;
#25932=CARTESIAN_POINT ( 'NONE',  ( 0.5947987396514448077, -1.485632953921246946, -0.6449812926602518370 ) ) ;
#25933=ORIENTED_EDGE ( 'NONE', *, *, #21227, .T. ) ;
#25939=CARTESIAN_POINT ( 'NONE',  ( 0.4952038534613475429, -1.196867906360179257, -0.6186948529734399571 ) ) ;
#25962=CARTESIAN_POINT ( 'NONE',  ( 0.2564068258101134812, -1.570482518261666183, -0.6784006763467468337 ) ) ;
#25964=CARTESIAN_POINT ( 'NONE',  ( 0.3665277588547195542, -1.753889016291175773, -0.6758757405868985879 ) ) ;
#25974=ORIENTED_EDGE ( 'NONE', *, *, #1723, .F. ) ;
#25978=CARTESIAN_POINT ( 'NONE',  ( 0.5383772456381804572, -1.668462259336880305, -0.5443662320918334352 ) ) ;
#25981=DIRECTION ( 'NONE',  ( -0.4999551463232372317, 0.8660512985181135770, -0.000000000000000000 ) ) ;
#25983=CARTESIAN_POINT ( 'NONE',  ( 0.6181169081387583031, -1.622430050042262817, -0.5225751115788848100 ) ) ;
#25986=ORIENTED_EDGE ( 'NONE', *, *, #16955, .T. ) ;
#25988=VECTOR ( 'NONE', #36786, 39.37007874015748854 ) ;
#25995=EDGE_CURVE ( 'NONE', #27529, #2123, #12580, .T. ) ;
#25997=CARTESIAN_POINT ( 'NONE',  ( 0.3974995447111917546, -1.636701680056106056, -0.6413756779823100995 ) ) ;
#26012=B_SPLINE_CURVE_WITH_KNOTS ( 'NONE', 3,
 ( #25932, #22854, #34559, #35373, #32263, #4082, #4683, #23244, #26523, #32472 ),
 .UNSPECIFIED., .F., .F.,
 ( 4, 2, 2, 2, 4 ),
 ( 0.000000000000000000, 0.0003584082070478624717, 0.0007168164140957249434, 0.001075224621143587361, 0.001433632828191449887 ),
 .UNSPECIFIED. ) ;
#26020=VERTEX_POINT ( 'NONE', #24393 ) ;
#26027=CARTESIAN_POINT ( 'NONE',  ( 0.3624061103390761596, -1.968824918581871808, -0.4968426515054794046 ) ) ;
#26043=EDGE_CURVE ( 'NONE', #38511, #5281, #8430, .T. ) ;
#26044=DIRECTION ( 'NONE',  ( 0.8660512985181135770, 0.4999551463232371207, -3.316523347579165317E-14 ) ) ;
#26046=EDGE_CURVE ( 'NONE', #29847, #7589, #1454, .T. ) ;
#26057=CARTESIAN_POINT ( 'NONE',  ( 0.4721942231302789228, -1.661553490448593351, -0.6136790096869797484 ) ) ;
#26072=CARTESIAN_POINT ( 'NONE',  ( 0.6496884796976931664, -1.552103590352501339, -0.4192475089069890859 ) ) ;
#26074=CARTESIAN_POINT ( 'NONE',  ( 0.1977770593140153743, -1.253111361966154469, -0.7170389795550398127 ) ) ;
#26079=ORIENTED_EDGE ( 'NONE', *, *, #29825, .T. ) ;
#26083=ADVANCED_FACE ( 'NONE', ( #33341 ), #21014, .F. ) ;
#26087=CARTESIAN_POINT ( 'NONE',  ( 0.1854014988492357074, -1.730386108846895921, -0.3576835534809157946 ) ) ;
#26090=ORIENTED_EDGE ( 'NONE', *, *, #5739, .F. ) ;
#26097=CARTESIAN_POINT ( 'NONE',  ( 0.06540210900077661482, -2.107936428766288728, -0.2870436526301870517 ) ) ;
#26098=( BOUNDED_SURFACE ( )  B_SPLINE_SURFACE ( 3, 2, ( 
 ( #11059, #11249, #11463 ),
 ( #23618, #36134, #23818 ),
 ( #27093, #39627, #24028 ),
 ( #33454, #5260, #29376 ) ),
 .UNSPECIFIED., .F., .F., .F. ) 
 B_SPLINE_SURFACE_WITH_KNOTS ( ( 4, 4 ),
 ( 3, 3 ),
 ( 1.279358563532895232E-17, 0.0008871692367534844822 ),
 ( 0.000000000000000000, 1.000000000000000000 ),
 .UNSPECIFIED. ) 
 GEOMETRIC_REPRESENTATION_ITEM ( )  RATIONAL_B_SPLINE_SURFACE ( (
 ( 1.000000000000000000, 0.9159177456829746822, 1.000000000000000000),
 ( 1.000000000000000000, 0.9105746466534058170, 1.000000000000000000),
 ( 1.000000000000000000, 0.9036974575934779708, 1.000000000000000000),
 ( 1.000000000000000000, 0.8959137433814483575, 1.000000000000000000) ) ) 
 REPRESENTATION_ITEM ( '' )  SURFACE ( )  );
#26100=CARTESIAN_POINT ( 'NONE',  ( 0.4079901106498464158, -1.633071172328754983, -0.7462941026102626330 ) ) ;
#26101=VERTEX_POINT ( 'NONE', #25325 ) ;
#26106=CARTESIAN_POINT ( 'NONE',  ( 0.2842326993136328195, -1.549395603922531617, -0.7208999815284821144 ) ) ;
#26107=CARTESIAN_POINT ( 'NONE',  ( 0.4016461280392738531, -1.742774929250199945, -0.4866300481184575033 ) ) ;
#26108=EDGE_CURVE ( 'NONE', #12314, #13200, #19737, .T. ) ;
#26113=ADVANCED_FACE ( 'NONE', ( #6379 ), #10940, .T. ) ;
#26114=CARTESIAN_POINT ( 'NONE',  ( 0.6615513487989460595, -1.426771801028701825, -0.6132045830072060388 ) ) ;
#26117=CARTESIAN_POINT ( 'NONE',  ( 0.4162711365034791888, -1.591899382515264305, -0.6171341197600156425 ) ) ;
#26121=CARTESIAN_POINT ( 'NONE',  ( 0.6057880463341017707, -1.521544944963801882, -0.4306026127826089178 ) ) ;
#26122=CARTESIAN_POINT ( 'NONE',  ( 0.5222653935518027923, -1.637842191745487730, -0.6100709635252473673 ) ) ;
#26123=CARTESIAN_POINT ( 'NONE',  ( 0.2059267202968889376, -1.283046696160772271, -0.2869364497861741636 ) ) ;
#26124=ORIENTED_EDGE ( 'NONE', *, *, #37167, .F. ) ;
#26128=DIRECTION ( 'NONE',  ( 0.4999551463232373427, -0.8660512985181134660, 0.000000000000000000 ) ) ;
#26134=CARTESIAN_POINT ( 'NONE',  ( 0.3614155096298604097, -1.733227469354456263, -0.5467282445978081107 ) ) ;
#26136=DIRECTION ( 'NONE',  ( 0.9823715787225890672, 0.000000000000000000, 0.1869387100578369376 ) ) ;
#26142=CARTESIAN_POINT ( 'NONE',  ( -2.051109323440559901E-05, -2.028068521879886177, -0.3128692020079770209 ) ) ;
#26143=ORIENTED_EDGE ( 'NONE', *, *, #34676, .T. ) ;
#26153=CARTESIAN_POINT ( 'NONE',  ( 0.1999999999999789169, -2.097675824466503247, -0.7286991843995637153 ) ) ;
#26161=CARTESIAN_POINT ( 'NONE',  ( 0.4038347882556602153, -1.728811102479167472, -0.5994564538101174733 ) ) ;
#26169=VERTEX_POINT ( 'NONE', #19357 ) ;
#26171=ORIENTED_EDGE ( 'NONE', *, *, #23502, .T. ) ;
#26172=CARTESIAN_POINT ( 'NONE',  ( 0.5360939586754306374, -1.669780358010149568, -0.5511600881468147195 ) ) ;
#26174=CARTESIAN_POINT ( 'NONE',  ( 0.2059273467974225835, -1.283046334493782137, -0.6485234391946320676 ) ) ;
#26176=CARTESIAN_POINT ( 'NONE',  ( 0.6505092258670857053, -1.603730573490116162, -0.4546931408925022899 ) ) ;
#26179=DIRECTION ( 'NONE',  ( -1.000000000000000000, -0.000000000000000000, -0.000000000000000000 ) ) ;
#26186=CARTESIAN_POINT ( 'NONE',  ( 0.4812560861399013401, -1.590261200983826173, -0.4454942134426254086 ) ) ;
#26195=( NAMED_UNIT ( * ) PLANE_ANGLE_UNIT ( ) SI_UNIT ( $, .RADIAN. ) );
#26197=CARTESIAN_POINT ( 'NONE',  ( 0.4469283285619459201, -1.099869350908816878, -0.4033480720695140631 ) ) ;
#26201=ADVANCED_FACE ( 'NONE', ( #12764 ), #3505, .T. ) ;
#26205=CARTESIAN_POINT ( 'NONE',  ( 0.3784118722789395206, -1.581834032482531738, -0.7462941026102631881 ) ) ;
#26207=CARTESIAN_POINT ( 'NONE',  ( 0.2059273467974225835, -1.283046334493782137, -0.6485234391946320676 ) ) ;
#26217=CARTESIAN_POINT ( 'NONE',  ( 0.3864136346424311141, -1.704101823309675190, -0.5257935635300878818 ) ) ;
#26228=ORIENTED_EDGE ( 'NONE', *, *, #36357, .F. ) ;
#26229=CARTESIAN_POINT ( 'NONE',  ( 0.2059273467974226113, -1.283046334493782803, -0.3194715457588298557 ) ) ;
#26237=DIRECTION ( 'NONE',  ( -0.9654310062341997511, 0.000000000000000000, -0.2606587274610626670 ) ) ;
#26240=CARTESIAN_POINT ( 'NONE',  ( 0.5214666498663128591, -1.638124173219856150, -0.6107250905094568916 ) ) ;
#26245=ADVANCED_FACE ( 'NONE', ( #7372 ), #29413, .F. ) ;
#26247=EDGE_CURVE ( 'NONE', #7589, #14915, #16659, .T. ) ;
#26248=ORIENTED_EDGE ( 'NONE', *, *, #17968, .T. ) ;
#26250=VERTEX_POINT ( 'NONE', #25719 ) ;
#26255=DIMENSIONAL_EXPONENTS ( 1.000000000000000000, 0.000000000000000000, 0.000000000000000000, 0.000000000000000000, 0.000000000000000000, 0.000000000000000000, 0.000000000000000000 ) ;
#26256=EDGE_CURVE ( 'NONE', #6802, #26020, #28361, .T. ) ;
#26258=EDGE_LOOP ( 'NONE', ( #784, #23777, #11006, #39315, #25056, #24248, #27177, #13902 ) ) ;
#26260=CARTESIAN_POINT ( 'NONE',  ( 0.6583424475134876941, -1.513463612852635087, -0.4125214496082464932 ) ) ;
#26266=CARTESIAN_POINT ( 'NONE',  ( 0.5832016030513088589, -1.507466846285616890, -0.4433012690765181230 ) ) ;
#26275=CARTESIAN_POINT ( 'NONE',  ( 0.1813268067401742623, -1.770784169840084354, -0.3550387660845038540 ) ) ;
#26278=CARTESIAN_POINT ( 'NONE',  ( 0.3834850620676270583, -1.099718979878179237, -0.5155029497116575543 ) ) ;
#26298=CARTESIAN_POINT ( 'NONE',  ( 0.5716435301310013317, -1.574655833597282228, -0.5703388428348806771 ) ) ;
#26300=FACE_OUTER_BOUND ( 'NONE', #39352, .T. ) ;
#26303=EDGE_CURVE ( 'NONE', #19986, #15269, #34448, .T. ) ;
#26305=B_SPLINE_CURVE_WITH_KNOTS ( 'NONE', 3,
 ( #11809, #17775, #21292, #39581, #20894, #14700 ),
 .UNSPECIFIED., .F., .F.,
 ( 4, 2, 4 ),
 ( 0.000000000000000000, 0.0009816776391258473251, 0.001963355278251694650 ),
 .UNSPECIFIED. ) ;
#26307=CARTESIAN_POINT ( 'NONE',  ( 0.4264202721361136650, -1.467519734074643756, -0.5166151207188711680 ) ) ;
#26317=CARTESIAN_POINT ( 'NONE',  ( 0.4768848212686895849, -1.682051206446435243, -0.4156371400837835517 ) ) ;
#26321=CARTESIAN_POINT ( 'NONE',  ( 0.5493166376341016566, -1.662147153828273050, -0.4937231952609894003 ) ) ;
#26325=CARTESIAN_POINT ( 'NONE',  ( 0.07404520294109505352, -1.411154561580794331, -0.3648634245470773196 ) ) ;
#26329=CARTESIAN_POINT ( 'NONE',  ( 0.04420884470503230745, -1.503720994967077784, -0.6465903430088162374 ) ) ;
#26330=CARTESIAN_POINT ( 'NONE',  ( 0.3639979711723335121, -1.990389627807109152, -0.5000272939307007780 ) ) ;
#26332=CARTESIAN_POINT ( 'NONE',  ( 0.4839231165671814550, -1.681532706550865397, -0.6135084623096023204 ) ) ;
#26343=DIRECTION ( 'NONE',  ( 0.9823715787225887341, 0.000000000000000000, 0.1869387100578391581 ) ) ;
#26362=ORIENTED_EDGE ( 'NONE', *, *, #24513, .F. ) ;
#26365=DIRECTION ( 'NONE',  ( 0.8660512985181135770, 0.4999551463232370652, 2.644395542647567230E-15 ) ) ;
#26371=ORIENTED_EDGE ( 'NONE', *, *, #16515, .F. ) ;
#26386=DIRECTION ( 'NONE',  ( 0.000000000000000000, 0.000000000000000000, -1.000000000000000000 ) ) ;
#26393=CARTESIAN_POINT ( 'NONE',  ( 0.6106560647436484190, -1.615133038819531741, -0.5295971823914620291 ) ) ;
#26399=EDGE_CURVE ( 'NONE', #24957, #15024, #13264, .T. ) ;
#26403=AXIS2_PLACEMENT_3D ( 'NONE', #31515, #19185, #3325 ) ;
#26414=CARTESIAN_POINT ( 'NONE',  ( 0.07285041588532994994, -1.413036571972506428, -0.6863200093549134406 ) ) ;
#26415=ORIENTED_EDGE ( 'NONE', *, *, #35073, .F. ) ;
#26436=DIRECTION ( 'NONE',  ( -1.000000000000000000, 0.000000000000000000, 0.000000000000000000 ) ) ;
#26444=CARTESIAN_POINT ( 'NONE',  ( 0.5576601260976730146, -1.622690634273228349, -0.5586186950843531340 ) ) ;
#26455=ORIENTED_EDGE ( 'NONE', *, *, #8977, .T. ) ;
#26458=AXIS2_PLACEMENT_3D ( 'NONE', #5076, #21352, #14143 ) ;
#26459=CARTESIAN_POINT ( 'NONE',  ( 0.6420950953327444477, -1.575825456952314685, -0.4289601232232088113 ) ) ;
#26473=CARTESIAN_POINT ( 'NONE',  ( 0.4806321272675940781, -1.111925921944065809, -0.6264081341737259834 ) ) ;
#26476=DIRECTION ( 'NONE',  ( 0.4999551463232373427, -0.8660512985181134660, 0.000000000000000000 ) ) ;
#26477=ADVANCED_FACE ( 'NONE', ( #36648 ), #10611, .T. ) ;
#26479=ORIENTED_EDGE ( 'NONE', *, *, #9835, .T. ) ;
#26480=CARTESIAN_POINT ( 'NONE',  ( 0.3969982963057278047, -1.750077671058422046, -0.4821875037442182599 ) ) ;
#26485=CARTESIAN_POINT ( 'NONE',  ( 0.3926032618788913298, -1.756026311479878421, -0.5284552501752952658 ) ) ;
#26495=CARTESIAN_POINT ( 'NONE',  ( 0.6482135835996580830, -1.415164486681432798, -0.6155586712855226628 ) ) ;
#26501=AXIS2_PLACEMENT_3D ( 'NONE', #11196, #36281, #1956 ) ;
#26502=EDGE_CURVE ( 'NONE', #24229, #3740, #11856, .T. ) ;
#26505=CARTESIAN_POINT ( 'NONE',  ( 0.5749393492916552439, -1.540325544240326083, -0.4818059086064602203 ) ) ;
#26506=CARTESIAN_POINT ( 'NONE',  ( 0.02999778723028644414, -2.087755359801441557, -0.2623954751430960797 ) ) ;
#26512=CARTESIAN_POINT ( 'NONE',  ( 0.3718671178488404672, -1.764871997527151848, -0.5765770349210319612 ) ) ;
#26515=CARTESIAN_POINT ( 'NONE',  ( 0.3492852788876838477, -1.696550652582485830, -0.4668076899784869283 ) ) ;
#26523=CARTESIAN_POINT ( 'NONE',  ( 0.5881066016147241671, -1.489496199501605611, -0.5990371943001994159 ) ) ;
#26527=DIRECTION ( 'NONE',  ( 0.8660512985181126888, 0.4999551463232385085, 0.000000000000000000 ) ) ;
#26529=FACE_OUTER_BOUND ( 'NONE', #27879, .T. ) ;
#26534=TOROIDAL_SURFACE ( 'NONE', #25897, 0.09088067974298029428, 0.01499999999999999944 ) ;
#26535=CARTESIAN_POINT ( 'NONE',  ( 0.003464874609604914023, -1.839213656041257527, -0.6448626447465779510 ) ) ;
#26538=AXIS2_PLACEMENT_3D ( 'NONE', #29007, #870, #31907 ) ;
#26545=DIRECTION ( 'NONE',  ( -1.000000000000000000, 8.195543980992782950E-15, 4.097771990496391475E-15 ) ) ;
#26546=DIRECTION ( 'NONE',  ( 0.000000000000000000, 0.000000000000000000, -1.000000000000000000 ) ) ;
#26547=DIRECTION ( 'NONE',  ( 0.000000000000000000, 0.000000000000000000, -1.000000000000000000 ) ) ;
#26550=CIRCLE ( 'NONE', #8792, 0.2200000000000000011 ) ;
#26561=DIRECTION ( 'NONE',  ( -0.4999551463232372317, 0.8660512985181135770, -0.000000000000000000 ) ) ;
#26578=CARTESIAN_POINT ( 'NONE',  ( 0.6186566136881834765, -1.609114265322737269, -0.4705007761744832706 ) ) ;
#26597=CARTESIAN_POINT ( 'NONE',  ( 0.3123258297132953665, -1.533408232077866362, -0.7003322928082994503 ) ) ;
#26602=CARTESIAN_POINT ( 'NONE',  ( 0.4000000000004778067, -2.061712828828752730, -0.2709148305154810421 ) ) ;
#26605=FACE_OUTER_BOUND ( 'NONE', #24202, .T. ) ;
#26606=EDGE_CURVE ( 'NONE', #10778, #23598, #40271, .T. ) ;
#26608=CARTESIAN_POINT ( 'NONE',  ( 0.6100534684184480971, -1.615500477088944065, -0.5228428417932495798 ) ) ;
#26615=AXIS2_PLACEMENT_3D ( 'NONE', #30765, #18625, #9350 ) ;
#26618=DIRECTION ( 'NONE',  ( 0.000000000000000000, 0.000000000000000000, 1.000000000000000000 ) ) ;
#26628=DIRECTION ( 'NONE',  ( -1.000000000000000000, 0.000000000000000000, 0.000000000000000000 ) ) ;
#26631=CIRCLE ( 'NONE', #1020, 0.08830708661417320526 ) ;
#26633=ORIENTED_EDGE ( 'NONE', *, *, #26909, .F. ) ;
#26635=CARTESIAN_POINT ( 'NONE',  ( 0.06788540646851175253, -1.426487579412121898, -0.6578865797971491514 ) ) ;
#26636=EDGE_LOOP ( 'NONE', ( #22100, #8842, #23023, #22630, #20301 ) ) ;
#26647=CYLINDRICAL_SURFACE ( 'NONE', #14327, 0.03000000000000003358 ) ;
#26659=DIRECTION ( 'NONE',  ( -0.4999551463232377313, 0.8660512985181132439, 0.000000000000000000 ) ) ;
#26662=CARTESIAN_POINT ( 'NONE',  ( 0.1457829054851000339, -1.333675122505752375, -0.3151394128761840774 ) ) ;
#26663=CARTESIAN_POINT ( 'NONE',  ( 0.4317743168343897153, -1.612353136874114634, -0.6636800572944283605 ) ) ;
#26665=CARTESIAN_POINT ( 'NONE',  ( 0.1359911470193229943, -1.231045907863504763, -0.5155029497116575543 ) ) ;
#26666=CARTESIAN_POINT ( 'NONE',  ( 0.3984114568195520345, -1.599003643269838904, -0.5155029497116575543 ) ) ;
#26679=CARTESIAN_POINT ( 'NONE',  ( 0.3992403239432529283, -1.683235622436187073, -0.6263438071736542323 ) ) ;
#26683=CARTESIAN_POINT ( 'NONE',  ( 0.5789220659479127340, -1.645056496184873929, -0.5155029497116575543 ) ) ;
#26689=( BOUNDED_SURFACE ( )  B_SPLINE_SURFACE ( 3, 2, ( 
 ( #4747, #30477, #14847 ),
 ( #39936, #17320, #20621 ),
 ( #33758, #11345, #2089 ),
 ( #11752, #2306, #26797 ),
 ( #29876, #8045, #33157 ),
 ( #20829, #1715, #23703 ),
 ( #10958, #24311, #2506 ),
 ( #23519, #36834, #8651 ),
 ( #14626, #8453, #4962 ),
 ( #15046, #21222, #14417 ),
 ( #36034, #27196, #33350 ),
 ( #5572, #39730, #14232 ) ),
 .UNSPECIFIED., .F., .F., .T. ) 
 B_SPLINE_SURFACE_WITH_KNOTS ( ( 4, 2, 2, 2, 2, 4 ),
 ( 3, 3 ),
 ( 0.000000000000000000, 0.0002157422512141129838, 0.0004314845024282259675, 0.0008629690048564519350, 0.001294453507284677903, 0.001725938009712903870 ),
 ( 0.000000000000000000, 1.000000000000000000 ),
 .UNSPECIFIED. ) 
 GEOMETRIC_REPRESENTATION_ITEM ( )  RATIONAL_B_SPLINE_SURFACE ( (
 ( 1.000000000000000000, 0.8660688067375535981, 1.000000000000000000),
 ( 1.000000000000000000, 0.8654212037204194186, 1.000000000000000000),
 ( 1.000000000000000000, 0.8620557401133326358, 1.000000000000000000),
 ( 1.000000000000000000, 0.8506860164930378776, 1.000000000000000000),
 ( 1.000000000000000000, 0.8429438875099044548, 1.000000000000000000),
 ( 1.000000000000000000, 0.8190090774808674867, 1.000000000000000000),
 ( 1.000000000000000000, 0.8018511170037568858, 1.000000000000000000),
 ( 1.000000000000000000, 0.7696825608641452154, 1.000000000000000000),
 ( 1.000000000000000000, 0.7540990922196469937, 1.000000000000000000),
 ( 1.000000000000000000, 0.7234792338946504087, 1.000000000000000000),
 ( 1.000000000000000000, 0.7084058450330773526, 1.000000000000000000),
 ( 1.000000000000000000, 0.6936380329425325675, 1.000000000000000000) ) ) 
 REPRESENTATION_ITEM ( '' )  SURFACE ( )  );
#26694=CARTESIAN_POINT ( 'NONE',  ( 0.1806790351422245811, -1.790997932741038801, -0.3531985826763806569 ) ) ;
#26708=CARTESIAN_POINT ( 'NONE',  ( 0.3625960434667531151, -1.762758894398492204, -0.5926935080085831142 ) ) ;
#26711=CARTESIAN_POINT ( 'NONE',  ( 0.6069444678199540366, -1.586721832627447037, -0.5605626994862983326 ) ) ;
#26718=CARTESIAN_POINT ( 'NONE',  ( 0.5769685703849426472, -1.564106961903302784, -0.4421163036608469765 ) ) ;
#26719=CARTESIAN_POINT ( 'NONE',  ( -1.545739608871925730E-14, -2.094379624154600883, -0.2600525927961437334 ) ) ;
#26722=B_SPLINE_CURVE_WITH_KNOTS ( 'NONE', 3,
 ( #12525, #34330, #36799, #18301, #5532, #6141, #33943, #24277, #9224, #9436, #2472, #34126 ),
 .UNSPECIFIED., .F., .F.,
 ( 4, 2, 2, 2, 2, 4 ),
 ( 0.004565700224486055406, 0.005703496875624043498, 0.006272395201193034509, 0.006841293526762026386, 0.007979090177900018815, 0.009116886829038009510 ),
 .UNSPECIFIED. ) ;
#26724=ORIENTED_EDGE ( 'NONE', *, *, #7152, .T. ) ;
#26741=CARTESIAN_POINT ( 'NONE',  ( 0.1690117501680792333, -1.307634958409015669, -0.3044763796399118094 ) ) ;
#26742=ORIENTED_EDGE ( 'NONE', *, *, #33898, .T. ) ;
#26744=CARTESIAN_POINT ( 'NONE',  ( 0.07228386787129255364, -1.414757321928298950, -0.6600343213859931613 ) ) ;
#26747=CARTESIAN_POINT ( 'NONE',  ( 0.1909286924077255032, -1.257064795538239022, -0.3194753470178354759 ) ) ;
#26749=CARTESIAN_POINT ( 'NONE',  ( 0.5140855864883536741, -1.668539606441037826, -0.5966333239037243663 ) ) ;
#26764=CARTESIAN_POINT ( 'NONE',  ( 0.3681929541678355400, -1.759371874277346537, -0.5873187883762895911 ) ) ;
#26766=CYLINDRICAL_SURFACE ( 'NONE', #9859, 0.2200000000000000289 ) ;
#26772=EDGE_CURVE ( 'NONE', #22699, #30555, #22167, .T. ) ;
#26780=ORIENTED_EDGE ( 'NONE', *, *, #25102, .F. ) ;
#26786=CARTESIAN_POINT ( 'NONE',  ( 0.6438069108991687495, -1.607599694021685899, -0.4632284051550286108 ) ) ;
#26797=CARTESIAN_POINT ( 'NONE',  ( 0.3883097432465577592, -1.693085907158164538, -0.4088198505623931722 ) ) ;
#26801=FACE_OUTER_BOUND ( 'NONE', #33178, .T. ) ;
#26804=CARTESIAN_POINT ( 'NONE',  ( 0.3443170205183039845, -1.640114790049758353, -0.3775635453920966333 ) ) ;
#26806=CARTESIAN_POINT ( 'NONE',  ( 0.6275005400096769215, -1.601790509832649922, -0.5777336405445359091 ) ) ;
#26811=CARTESIAN_POINT ( 'NONE',  ( 0.3672875303838389338, -1.616970901354834789, -0.6123576500872190964 ) ) ;
#26814=ORIENTED_EDGE ( 'NONE', *, *, #25857, .F. ) ;
#26815=DIRECTION ( 'NONE',  ( 0.8660512985181134660, 0.4999551463232372872, 0.000000000000000000 ) ) ;
#26827=CARTESIAN_POINT ( 'NONE',  ( 0.01266905423176017606, -1.700475420996584885, -0.6376096380771161254 ) ) ;
#26829=CARTESIAN_POINT ( 'NONE',  ( 0.6457670174492194937, -1.456209924560479152, -0.4058631681734992669 ) ) ;
#26843=EDGE_LOOP ( 'NONE', ( #13284, #457, #12931, #15290 ) ) ;
#26850=CARTESIAN_POINT ( 'NONE',  ( 0.3944272916047369404, -1.765189661685290901, -0.7095092544234420373 ) ) ;
#26851=DIRECTION ( 'NONE',  ( -0.4999551463232373427, 0.8660512985181134660, -0.000000000000000000 ) ) ;
#26854=CARTESIAN_POINT ( 'NONE',  ( 0.02998309779899579336, -2.054017904330772470, -0.2742168981856276666 ) ) ;
#26861=DIRECTION ( 'NONE',  ( -0.000000000000000000, -0.000000000000000000, 1.000000000000000000 ) ) ;
#26863=B_SPLINE_CURVE_WITH_KNOTS ( 'NONE', 3,
 ( #1870, #17675, #24280, #14196 ),
 .UNSPECIFIED., .F., .F.,
 ( 4, 4 ),
 ( 0.000000000000000000, 0.0008899773499878894933 ),
 .UNSPECIFIED. ) ;
#26864=CARTESIAN_POINT ( 'NONE',  ( 0.3925301276612754298, -1.756377271995033684, -0.4843757382520948451 ) ) ;
#26886=EDGE_CURVE ( 'NONE', #5500, #32636, #36845, .T. ) ;
#26887=DIRECTION ( 'NONE',  ( 1.000000000000000000, 0.000000000000000000, 0.000000000000000000 ) ) ;
#26893=FACE_OUTER_BOUND ( 'NONE', #38945, .T. ) ;
#26901=CARTESIAN_POINT ( 'NONE',  ( 0.5896330274811124594, -1.594592002126501429, -0.5907196032396619945 ) ) ;
#26907=CARTESIAN_POINT ( 'NONE',  ( 0.5857434439472278820, -1.570035424762864285, -0.5212337988449284865 ) ) ;
#26909=EDGE_CURVE ( 'NONE', #9760, #4182, #21644, .T. ) ;
#26914=( BOUNDED_SURFACE ( )  B_SPLINE_SURFACE ( 3, 2, ( 
 ( #33370, #14249, #26811 ),
 ( #5174, #7853, #17726 ),
 ( #8276, #8063, #23933 ),
 ( #36463, #39150, #33174 ),
 ( #1918, #17548, #4559 ),
 ( #30276, #14435, #17932 ),
 ( #29894, #4764, #29678 ),
 ( #36052, #39948, #1736 ) ),
 .UNSPECIFIED., .F., .F., .T. ) 
 B_SPLINE_SURFACE_WITH_KNOTS ( ( 4, 2, 2, 4 ),
 ( 3, 3 ),
 ( 0.003138011302842199680, 0.004009802660711201706, 0.004445698339645702719, 0.004881594018580203732 ),
 ( 0.000000000000000000, 1.000000000000000000 ),
 .UNSPECIFIED. ) 
 GEOMETRIC_REPRESENTATION_ITEM ( )  RATIONAL_B_SPLINE_SURFACE ( (
 ( 1.000000000000000000, 0.5504785946861689983, 1.000000000000000000),
 ( 1.000000000000000000, 0.5522673118645705648, 1.000000000000000000),
 ( 1.000000000000000000, 0.5426696336924615727, 1.000000000000000000),
 ( 1.000000000000000000, 0.5149554968636153029, 1.000000000000000000),
 ( 1.000000000000000000, 0.5037106103022731540, 1.000000000000000000),
 ( 1.000000000000000000, 0.4776838670538872678, 1.000000000000000000),
 ( 1.000000000000000000, 0.4627352203515152085, 1.000000000000000000),
 ( 1.000000000000000000, 0.4461867090254074131, 1.000000000000000000) ) ) 
 REPRESENTATION_ITEM ( '' )  SURFACE ( )  );
#26922=DIRECTION ( 'NONE',  ( 0.8660512985181133550, 0.4999551463232372317, 0.000000000000000000 ) ) ;
#26924=CARTESIAN_POINT ( 'NONE',  ( 0.1999999999999789724, -2.183180860297921466, -0.4937760292030871079 ) ) ;
#26932=CARTESIAN_POINT ( 'NONE',  ( 0.01034223579727351801, -1.726934810087732641, -0.6381276386021752511 ) ) ;
#26933=DIRECTION ( 'NONE',  ( 0.4999551463232373427, -0.8660512985181134660, 0.000000000000000000 ) ) ;
#26955=CIRCLE ( 'NONE', #7968, 0.2200000000000000566 ) ;
#26958=CARTESIAN_POINT ( 'NONE',  ( 0.4114050106974946330, -1.724440955265992947, -0.5872665585884049300 ) ) ;
#26961=ORIENTED_EDGE ( 'NONE', *, *, #29775, .F. ) ;
#26970=CARTESIAN_POINT ( 'NONE',  ( 0.2034277765170372787, -1.278716433895728422, -0.7137157339815681789 ) ) ;
#26971=VERTEX_POINT ( 'NONE', #34523 ) ;
#26985=EDGE_CURVE ( 'NONE', #31373, #24117, #37804, .T. ) ;
#26990=CARTESIAN_POINT ( 'NONE',  ( 0.3499942944112305887, -1.632920710989241408, -0.3738306617559248868 ) ) ;
#26994=CARTESIAN_POINT ( 'NONE',  ( 0.6099423129193194404, -1.615565191381619137, -0.5028438385245220799 ) ) ;
#27003=ADVANCED_FACE ( 'NONE', ( #5730 ), #18258, .T. ) ;
#27005=DIRECTION ( 'NONE',  ( 0.8660512985181135770, 0.4999551463232370652, -9.916483284928376127E-15 ) ) ;
#27009=CARTESIAN_POINT ( 'NONE',  ( 0.3771340144105596592, -1.765187147855314498, -0.4446665289696524748 ) ) ;
#27010=CARTESIAN_POINT ( 'NONE',  ( 0.3934443868333699634, -1.753172285594142066, -0.5285261949624394662 ) ) ;
#27016=CARTESIAN_POINT ( 'NONE',  ( 0.1177554796393661674, -1.375324152023213564, -0.7018171977754862345 ) ) ;
#27024=ORIENTED_EDGE ( 'NONE', *, *, #12176, .F. ) ;
#27033=ORIENTED_EDGE ( 'NONE', *, *, #28027, .T. ) ;
#27038=CARTESIAN_POINT ( 'NONE',  ( 0.3699999999999786793, -2.080216821995567233, -0.4859795201926049302 ) ) ;
#27040=EDGE_CURVE ( 'NONE', #31364, #23204, #13287, .T. ) ;
#27041=AXIS2_PLACEMENT_3D ( 'NONE', #33532, #11338, #36223 ) ;
#27043=CARTESIAN_POINT ( 'NONE',  ( 0.1790649681787556680, -1.895405488977804254, -0.6873613951464528915 ) ) ;
#27056=ADVANCED_FACE ( 'NONE', ( #3454 ), #7322, .F. ) ;
#27059=DIRECTION ( 'NONE',  ( -0.4999551463232372317, 0.8660512985181135770, -0.000000000000000000 ) ) ;
#27069=CARTESIAN_POINT ( 'NONE',  ( 0.4030327056921976792, -1.680968334469209680, -0.4031266960524464982 ) ) ;
#27081=EDGE_LOOP ( 'NONE', ( #14388, #20145, #21699 ) ) ;
#27082=AXIS2_PLACEMENT_3D ( 'NONE', #20044, #23136, #35662 ) ;
#27088=EDGE_CURVE ( 'NONE', #14602, #15639, #36923, .T. ) ;
#27092=CARTESIAN_POINT ( 'NONE',  ( 0.3945466357887226772, -1.754957878890512024, -0.4915690588065673161 ) ) ;
#27093=CARTESIAN_POINT ( 'NONE',  ( 0.3857519400669835452, -1.760804991660537722, -0.4635226585062726667 ) ) ;
#27098=B_SPLINE_CURVE_WITH_KNOTS ( 'NONE', 3,
 ( #833, #26123, #35359, #3687, #38634, #7346, #28373 ),
 .UNSPECIFIED., .F., .F.,
 ( 4, 3, 4 ),
 ( -6.000000000402129679E-08, 0.000000000000000000, 0.0003133564821238285308 ),
 .UNSPECIFIED. ) ;
#27100=CARTESIAN_POINT ( 'NONE',  ( 0.6042279486826958035, -1.591103445072521438, -0.5492199064561998911 ) ) ;
#27101=CARTESIAN_POINT ( 'NONE',  ( 0.02992969784436203332, -1.949504067775972294, -0.6897318246428794097 ) ) ;
#27103=CARTESIAN_POINT ( 'NONE',  ( 0.3720469278356866027, -1.757009016027275550, -0.4316954512420498880 ) ) ;
#27105=CIRCLE ( 'NONE', #22508, 0.03000000000000001971 ) ;
#27108=CARTESIAN_POINT ( 'NONE',  ( 0.5717479371661525755, -1.545029730964961434, -0.5259570771718768967 ) ) ;
#27110=AXIS2_PLACEMENT_3D ( 'NONE', #25367, #31932, #18977 ) ;
#27127=CARTESIAN_POINT ( 'NONE',  ( 0.02299189108461704989, -1.617841354202916859, -0.3728701932220275794 ) ) ;
#27129=CARTESIAN_POINT ( 'NONE',  ( 0.3330041777007136661, -1.680901281163226457, -0.6241177864389138019 ) ) ;
#27137=ORIENTED_EDGE ( 'NONE', *, *, #37717, .T. ) ;
#27144=CARTESIAN_POINT ( 'NONE',  ( 0.1424771846812046827, -1.296107695835423401, -0.3417999629372251436 ) ) ;
#27152=LINE ( 'NONE', #23871, #12194 ) ;
#27161=CARTESIAN_POINT ( 'NONE',  ( 0.3649134372921009062, -1.761483993094715705, -0.5896594712253142578 ) ) ;
#27164=CARTESIAN_POINT ( 'NONE',  ( 0.5324045658229008549, -1.654590185004139125, -0.5371941175943450997 ) ) ;
#27166=CIRCLE ( 'NONE', #36994, 0.03000000000000002318 ) ;
#27171=CARTESIAN_POINT ( 'NONE',  ( 0.4376587549789876519, -1.692075737177143768, -0.4124806547340321705 ) ) ;
#27174=ORIENTED_EDGE ( 'NONE', *, *, #34825, .F. ) ;
#27177=ORIENTED_EDGE ( 'NONE', *, *, #39, .T. ) ;
#27179=VERTEX_POINT ( 'NONE', #35733 ) ;
#27187=ORIENTED_EDGE ( 'NONE', *, *, #37284, .T. ) ;
#27196=CARTESIAN_POINT ( 'NONE',  ( 0.3857818729960305060, -1.743806986988165386, -0.4496613049301777520 ) ) ;
#27197=CARTESIAN_POINT ( 'NONE',  ( 0.2160030156770379184, -1.196403219198641565, -0.5155029497116575543 ) ) ;
#27200=CARTESIAN_POINT ( 'NONE',  ( 0.1999999999999791112, -2.107936428766273629, -0.2870436526301869407 ) ) ;
#27204=CARTESIAN_POINT ( 'NONE',  ( 0.3405956938547828883, -1.648484147626967378, -0.3820619200265555904 ) ) ;
#27205=CARTESIAN_POINT ( 'NONE',  ( 0.6597989824866907771, -1.598367771496736367, -0.5155029497116575543 ) ) ;
#27228=CARTESIAN_POINT ( 'NONE',  ( 0.1359808222933183708, -1.346136899214501526, -0.7113549742108937757 ) ) ;
#27232=FACE_OUTER_BOUND ( 'NONE', #22932, .T. ) ;
#27238=ORIENTED_EDGE ( 'NONE', *, *, #703, .F. ) ;
#27249=ORIENTED_EDGE ( 'NONE', *, *, #6855, .F. ) ;
#27259=CARTESIAN_POINT ( 'NONE',  ( 0.1621979957779212944, -1.277097269517335931, -0.6997590581617950667 ) ) ;
#27264=AXIS2_PLACEMENT_3D ( 'NONE', #10943, #23504, #11548 ) ;
#27266=CARTESIAN_POINT ( 'NONE',  ( 0.1939472947763713484, -2.001291656381384954, -0.6721680726779954984 ) ) ;
#27277=ADVANCED_FACE ( 'NONE', ( #26893 ), #6703, .T. ) ;
#27294=CIRCLE ( 'NONE', #22050, 0.02999999999999997113 ) ;
#27298=CARTESIAN_POINT ( 'NONE',  ( 0.4370059147932298105, -1.114236431796985949, -0.6414654485229357439 ) ) ;
#27303=CARTESIAN_POINT ( 'NONE',  ( 0.3972786276333574174, -2.032124455670578200, -0.4826101713713118468 ) ) ;
#27309=CARTESIAN_POINT ( 'NONE',  ( 0.2923286432308245808, -1.660243258845594649, -0.3694143330441917450 ) ) ;
#27311=CARTESIAN_POINT ( 'NONE',  ( 0.3933751395322774291, -1.752169251404669392, -0.4834917239368269337 ) ) ;
#27312=CARTESIAN_POINT ( 'NONE',  ( 0.5616682974235900350, -1.585511599874633193, -0.5166151207188732775 ) ) ;
#27316=B_SPLINE_CURVE_WITH_KNOTS ( 'NONE', 3,
 ( #24298, #18120, #21007, #40108, #34148, #15032 ),
 .UNSPECIFIED., .F., .F.,
 ( 4, 2, 4 ),
 ( 0.000000000000000000, 0.001177402821458509207, 0.002354805642917018414 ),
 .UNSPECIFIED. ) ;
#27317=CARTESIAN_POINT ( 'NONE',  ( 0.5763042886240972162, -1.611411870786366940, -0.5437224079586429060 ) ) ;
#27326=CARTESIAN_POINT ( 'NONE',  ( 0.4296077269088024453, -1.643823256665882582, -0.6213498245139347231 ) ) ;
#27329=VERTEX_POINT ( 'NONE', #27309 ) ;
#27331=CARTESIAN_POINT ( 'NONE',  ( 0.4697623592636160361, -1.061459377010899541, -0.6056023639864148711 ) ) ;
#27337=CARTESIAN_POINT ( 'NONE',  ( 0.3699999999999786793, -2.166079853131637645, -0.4467913981637915422 ) ) ;
#27342=CARTESIAN_POINT ( 'NONE',  ( 0.1756948879565448929, -1.266804977652423725, -0.3255180435861027011 ) ) ;
#27343=EDGE_LOOP ( 'NONE', ( #29254, #19497, #14356, #1101 ) ) ;
#27350=CIRCLE ( 'NONE', #10252, 0.03000000000000002318 ) ;
#27364=AXIS2_PLACEMENT_3D ( 'NONE', #25177, #35032, #34824 ) ;
#27374=VERTEX_POINT ( 'NONE', #21339 ) ;
#27379=CARTESIAN_POINT ( 'NONE',  ( 0.3655107245187978471, -1.761138529012605369, -0.5889844493690715721 ) ) ;
#27380=EDGE_LOOP ( 'NONE', ( #7370, #19991, #2847, #39952 ) ) ;
#27381=ORIENTED_EDGE ( 'NONE', *, *, #18232, .F. ) ;
#27385=CARTESIAN_POINT ( 'NONE',  ( 0.4030327056921978457, -1.680968334469209680, -0.4031266960524464427 ) ) ;
#27397=CARTESIAN_POINT ( 'NONE',  ( 0.2011892967074957184, -1.251141541415955682, -0.3144976166544468099 ) ) ;
#27403=ORIENTED_EDGE ( 'NONE', *, *, #12014, .F. ) ;
#27404=CARTESIAN_POINT ( 'NONE',  ( 0.1424029337235096226, -1.400533250147911746, -0.3552704771134632677 ) ) ;
#27409=CARTESIAN_POINT ( 'NONE',  ( 0.1997816917901940881, -2.061179784062637133, -0.2712838347678763196 ) ) ;
#27410=FACE_OUTER_BOUND ( 'NONE', #3445, .T. ) ;
#27412=VECTOR ( 'NONE', #8325, 39.37007874015748854 ) ;
#27414=CARTESIAN_POINT ( 'NONE',  ( 0.3854140029834414172, -1.662020764902374381, -0.6188351660075884775 ) ) ;
#27416=CARTESIAN_POINT ( 'NONE',  ( 0.2284923717121199460, -1.304659949875474068, -0.5155029497116575543 ) ) ;
#27418=CARTESIAN_POINT ( 'NONE',  ( 0.3824171657898973176, -1.655877295464978527, -0.3991060487093113784 ) ) ;
#27432=CARTESIAN_POINT ( 'NONE',  ( 0.3791949009533828741, -1.765055094326592577, -0.4492776787058168630 ) ) ;
#27444=CARTESIAN_POINT ( 'NONE',  ( 0.2059273467974226113, -1.283046334493782359, -0.5931747813493345456 ) ) ;
#27470=ORIENTED_EDGE ( 'NONE', *, *, #14287, .F. ) ;
#27478=CARTESIAN_POINT ( 'NONE',  ( 0.3682365755625819914, -1.750444406184286761, -0.3437022085564034879 ) ) ;
#27486=ORIENTED_EDGE ( 'NONE', *, *, #3868, .F. ) ;
#27488=CARTESIAN_POINT ( 'NONE',  ( 0.5114126470110641476, -1.614748454822723556, -0.5166151207188711680 ) ) ;
#27494=CARTESIAN_POINT ( 'NONE',  ( 0.4032509867765149414, -1.739306358580214429, -0.3080928060649947287 ) ) ;
#27500=DIRECTION ( 'NONE',  ( -0.4999551463232373427, 0.8660512985181134660, -0.000000000000000000 ) ) ;
#27508=CARTESIAN_POINT ( 'NONE',  ( 0.6027970226300880530, -1.572625850366509148, -0.6129179047768924526 ) ) ;
#27509=CARTESIAN_POINT ( 'NONE',  ( 0.4358762597388673998, -1.693470429196241911, -0.6183159457888328658 ) ) ;
#27513=CARTESIAN_POINT ( 'NONE',  ( 0.1909286924077255587, -1.257064795538239022, -0.3614800891584005194 ) ) ;
#27519=DIRECTION ( 'NONE',  ( 1.000000000000000000, 0.000000000000000000, 0.000000000000000000 ) ) ;
#27521=CARTESIAN_POINT ( 'NONE',  ( 0.4535876148589958468, -1.088427983879621586, -0.6204185223330352938 ) ) ;
#27528=DIRECTION ( 'NONE',  ( 0.8660512985181133550, 0.4999551463232371207, 0.000000000000000000 ) ) ;
#27529=VERTEX_POINT ( 'NONE', #36039 ) ;
#27533=CARTESIAN_POINT ( 'NONE',  ( 0.1544872190154600589, -1.284018304476169714, -0.3339841533942207730 ) ) ;
#27546=CARTESIAN_POINT ( 'NONE',  ( 0.1403991652838525728, -1.774344845793157655, -0.3580071914498583752 ) ) ;
#27549=CARTESIAN_POINT ( 'NONE',  ( 0.5664866863181922119, -1.581107300538653782, -0.4800253713849400583 ) ) ;
#27555=DIRECTION ( 'NONE',  ( 0.8660512985181130219, 0.4999551463232377868, 0.000000000000000000 ) ) ;
#27562=FACE_OUTER_BOUND ( 'NONE', #37647, .T. ) ;
#27565=CARTESIAN_POINT ( 'NONE',  ( 0.2656972267752780725, -1.560961775696012355, -0.7135955925061087113 ) ) ;
#27578=ORIENTED_EDGE ( 'NONE', *, *, #39112, .F. ) ;
#27584=CARTESIAN_POINT ( 'NONE',  ( 0.1909288978607520115, -1.257065151435887040, -0.7137147910394006090 ) ) ;
#27587=CARTESIAN_POINT ( 'NONE',  ( 0.1734973056165642902, -1.209394307038482719, -0.5155029497116575543 ) ) ;
#27592=CARTESIAN_POINT ( 'NONE',  ( -2.196333431559634599E-13, -2.094416301789170820, -0.7275128151819897360 ) ) ;
#27601=CARTESIAN_POINT ( 'NONE',  ( 0.3518531909964315307, -1.625880855532917169, -0.4272450907526114117 ) ) ;
#27610=AXIS2_PLACEMENT_3D ( 'NONE', #23021, #9654, #15820 ) ;
#27614=CARTESIAN_POINT ( 'NONE',  ( 0.3431621118303436191, -1.692997266099296461, -0.4130752873103220035 ) ) ;
#27615=ORIENTED_EDGE ( 'NONE', *, *, #36924, .F. ) ;
#27626=CARTESIAN_POINT ( 'NONE',  ( 0.1690930997617906550, -1.307384335399499831, -0.7282839042959697862 ) ) ;
#27627=CARTESIAN_POINT ( 'NONE',  ( 0.3633532330403487776, -1.743361738801966210, -0.5306750697200927069 ) ) ;
#27632=EDGE_LOOP ( 'NONE', ( #13244, #14261, #17140 ) ) ;
#27639=ORIENTED_EDGE ( 'NONE', *, *, #8501, .T. ) ;
#27644=CARTESIAN_POINT ( 'NONE',  ( 0.4042628496030684637, -1.723800573128688507, -0.6015185938071440086 ) ) ;
#27646=EDGE_CURVE ( 'NONE', #29368, #20774, #16579, .T. ) ;
#27647=CARTESIAN_POINT ( 'NONE',  ( 0.3744125517984470131, -1.759357067434767607, -0.4355489755031470289 ) ) ;
#27650=CARTESIAN_POINT ( 'NONE',  ( 0.3593346688482154661, -1.735925422213635549, -0.5010936962835144115 ) ) ;
#27655=CARTESIAN_POINT ( 'NONE',  ( 0.3671187914973310096, -2.025419988125670034, -0.6786350348123257881 ) ) ;
#27668=ORIENTED_EDGE ( 'NONE', *, *, #16565, .T. ) ;
#27672=CARTESIAN_POINT ( 'NONE',  ( 0.1966547502198365549, -1.674282070017420576, -0.3593914745891567675 ) ) ;
#27675=CARTESIAN_POINT ( 'NONE',  ( 0.2059273467974226113, -1.283046334493782359, -0.5931747813493345456 ) ) ;
#27685=CARTESIAN_POINT ( 'NONE',  ( 0.1999999999735330158, -2.091146487246815955, -0.6943973668278335953 ) ) ;
#27688=AXIS2_PLACEMENT_3D ( 'NONE', #31123, #3140, #29197 ) ;
#27689=CARTESIAN_POINT ( 'NONE',  ( 0.4703191885827326946, -1.592420631535068187, -0.5958679092299303814 ) ) ;
#27690=CARTESIAN_POINT ( 'NONE',  ( 0.1951391704723344500, -1.987894887562734469, -0.2907895905339114018 ) ) ;
#27698=CARTESIAN_POINT ( 'NONE',  ( 0.2059273467974224725, -1.283046334493782137, -0.3824824602286829855 ) ) ;
#27699=AXIS2_PLACEMENT_3D ( 'NONE', #14872, #39957, #36861 ) ;
#27705=CARTESIAN_POINT ( 'NONE',  ( 0.6067827457248362588, -1.586506025082006444, -0.4704708140563562679 ) ) ;
#27706=CARTESIAN_POINT ( 'NONE',  ( 0.4559719632891930385, -1.698713290701216350, -0.5155029497116575543 ) ) ;
#27709=CARTESIAN_POINT ( 'NONE',  ( 0.1909286924077255310, -1.257064795538239022, -0.3824824602286830411 ) ) ;
#27711=CARTESIAN_POINT ( 'NONE',  ( 0.3658297366832103936, -1.745592370396175541, -0.4954708084374070953 ) ) ;
#27712=CARTESIAN_POINT ( 'NONE',  ( 0.3951778266041646170, -1.698641715122608087, -0.6047022095078790072 ) ) ;
#27713=CARTESIAN_POINT ( 'NONE',  ( 0.4112193008909713066, -1.591609915476099868, -0.6177460231409267477 ) ) ;
#27714=CARTESIAN_POINT ( 'NONE',  ( 0.3624061103390691096, -1.968824918581854932, -0.4968426515055719972 ) ) ;
#27716=CARTESIAN_POINT ( 'NONE',  ( 0.5172910145744592514, -1.680634944436373512, -0.5803635445752998168 ) ) ;
#27722=AXIS2_PLACEMENT_3D ( 'NONE', #35101, #6904, #19479 ) ;
#27729=CARTESIAN_POINT ( 'NONE',  ( 0.1612877650847679423, -1.277903580349897039, -0.3312613801211721221 ) ) ;
#27733=FACE_OUTER_BOUND ( 'NONE', #19764, .T. ) ;
#27735=ADVANCED_FACE ( 'NONE', ( #26801 ), #25368, .F. ) ;
#27742=CARTESIAN_POINT ( 'NONE',  ( 0.2447871629624292500, -1.421848713596993496, -0.3349537587709216502 ) ) ;
#27744=CARTESIAN_POINT ( 'NONE',  ( 0.04430295985701804273, -1.505275273055644902, -0.3761050495259261606 ) ) ;
#27750=( BOUNDED_SURFACE ( )  B_SPLINE_SURFACE ( 3, 2, ( 
 ( #22899, #31724, #9514 ),
 ( #3540, #12808, #25371 ),
 ( #10120, #10335, #37902 ),
 ( #9714, #34799, #13012 ),
 ( #22697, #19399, #6601 ),
 ( #19183, #35228, #19595 ),
 ( #907, #25983, #38508 ),
 ( #16110, #35416, #7212 ),
 ( #19777, #4137, #12591 ),
 ( #7416, #4347, #19994 ),
 ( #33336, #32529, #7826 ),
 ( #4949, #29452, #26578 ),
 ( #23691, #1105, #36021 ),
 ( #26786, #17514, #38900 ),
 ( #30063, #5145, #17305 ),
 ( #26176, #39312, #20203 ) ),
 .UNSPECIFIED., .F., .F., .T. ) 
 B_SPLINE_SURFACE_WITH_KNOTS ( ( 4, 2, 2, 2, 2, 2, 2, 4 ),
 ( 3, 3 ),
 ( 0.000000000000000000, 0.0008688684136184839351, 0.001303302620427725794, 0.001737736827236967870, 0.002172171034046209946, 0.002606605240855451588, 0.003041039447664693664, 0.003475473654473935740 ),
 ( 0.000000000000000000, 1.000000000000000000 ),
 .UNSPECIFIED. ) 
 GEOMETRIC_REPRESENTATION_ITEM ( )  RATIONAL_B_SPLINE_SURFACE ( (
 ( 1.000000000000000000, 0.7071067811865511255, 1.000000000000000000),
 ( 1.000000000000000000, 0.7497868472460812450, 1.000000000000000000),
 ( 1.000000000000000000, 0.7816256484933949977, 1.000000000000000000),
 ( 1.000000000000000000, 0.8066966545080302975, 1.000000000000000000),
 ( 1.000000000000000000, 0.8110625487245798348, 1.000000000000000000),
 ( 1.000000000000000000, 0.8155049440654144055, 1.000000000000000000),
 ( 1.000000000000000000, 0.8158287745906235289, 1.000000000000000000),
 ( 1.000000000000000000, 0.8158343461500251470, 1.000000000000000000),
 ( 1.000000000000000000, 0.8155513814744629331, 1.000000000000000000),
 ( 1.000000000000000000, 0.8111133430346705309, 1.000000000000000000),
 ( 1.000000000000000000, 0.8067191351272415822, 1.000000000000000000),
 ( 1.000000000000000000, 0.7903519271076608899, 1.000000000000000000),
 ( 1.000000000000000000, 0.7782561128466314315, 1.000000000000000000),
 ( 1.000000000000000000, 0.7472427613862036022, 1.000000000000000000),
 ( 1.000000000000000000, 0.7284546171351224952, 1.000000000000000000),
 ( 1.000000000000000000, 0.7071067811866026398, 1.000000000000000000) ) ) 
 REPRESENTATION_ITEM ( '' )  SURFACE ( )  );
#27754=CARTESIAN_POINT ( 'NONE',  ( 0.2847549724830318874, -1.551417661949121118, -0.6853099816877789019 ) ) ;
#27758=AXIS2_PLACEMENT_3D ( 'NONE', #24551, #21472, #37080 ) ;
#27765=CARTESIAN_POINT ( 'NONE',  ( 0.1876560278723298503, -1.258954043299216119, -0.2885605078359608222 ) ) ;
#27767=ORIENTED_EDGE ( 'NONE', *, *, #5390, .T. ) ;
#27778=EDGE_CURVE ( 'NONE', #4952, #10331, #219, .T. ) ;
#27779=AXIS2_PLACEMENT_3D ( 'NONE', #30043, #33316, #36001 ) ;
#27781=VECTOR ( 'NONE', #33223, 39.37007874015748854 ) ;
#27786=AXIS2_PLACEMENT_3D ( 'NONE', #26924, #39455, #11087 ) ;
#27794=CARTESIAN_POINT ( 'NONE',  ( 0.4242133616548364183, -1.734366925052854391, -0.4397180493288433967 ) ) ;
#27798=CARTESIAN_POINT ( 'NONE',  ( 0.02999999999851975241, -2.094416301510383605, -0.7275128150656288151 ) ) ;
#27799=CARTESIAN_POINT ( 'NONE',  ( 0.5403448000457758971, -1.667326427136834432, -0.4959994330086618941 ) ) ;
#27808=B_SPLINE_CURVE_WITH_KNOTS ( 'NONE', 3,
 ( #10866, #13929, #26117, #19914 ),
 .UNSPECIFIED., .F., .F.,
 ( 4, 4 ),
 ( 1.734723475976807094E-18, 0.0003881528371572850154 ),
 .UNSPECIFIED. ) ;
#27809=DIRECTION ( 'NONE',  ( -0.4999551463232373427, 0.8660512985181134660, -0.000000000000000000 ) ) ;
#27819=AXIS2_PLACEMENT_3D ( 'NONE', #8920, #2961, #8315 ) ;
#27835=EDGE_CURVE ( 'NONE', #2400, #16986, #7368, .T. ) ;
#27838=EDGE_CURVE ( 'NONE', #15019, #26971, #14698, .T. ) ;
#27842=CIRCLE ( 'NONE', #16040, 0.1999999999999999278 ) ;
#27851=DIRECTION ( 'NONE',  ( 0.4999551463232372317, -0.8660512985181135770, 0.000000000000000000 ) ) ;
#27858=CARTESIAN_POINT ( 'NONE',  ( 0.04510596909177587432, -1.502102959356099277, -0.6428203672274495073 ) ) ;
#27863=CIRCLE ( 'NONE', #25913, 0.2200000000000000844 ) ;
#27867=AXIS2_PLACEMENT_3D ( 'NONE', #24799, #14914, #17784 ) ;
#27870=LINE ( 'NONE', #30940, #35157 ) ;
#27878=ORIENTED_EDGE ( 'NONE', *, *, #2465, .T. ) ;
#27879=EDGE_LOOP ( 'NONE', ( #26724, #92, #14736, #4605 ) ) ;
#27883=CARTESIAN_POINT ( 'NONE',  ( 0.1980544885252993881, -2.023080723334441888, -0.3130069968383289991 ) ) ;
#27901=CARTESIAN_POINT ( 'NONE',  ( 0.3986242379676584457, -2.054315208824561090, -0.4776734711709474945 ) ) ;
#27905=DIRECTION ( 'NONE',  ( 0.8660512985181134660, 0.4999551463232373427, 0.000000000000000000 ) ) ;
#27916=CARTESIAN_POINT ( 'NONE',  ( 0.5894785928677049869, -1.594119400354429672, -0.4403033262486665267 ) ) ;
#27921=B_SPLINE_CURVE_WITH_KNOTS ( 'NONE', 3,
 ( #25063, #37597, #21998, #9418, #20, #3849, #34522, #28558, #3663, #22203 ),
 .UNSPECIFIED., .F., .F.,
 ( 4, 2, 2, 2, 4 ),
 ( 0.002185774412332532404, 0.002876031867927643197, 0.003566289323522753556, 0.004256546779117863916, 0.004946804234712974709 ),
 .UNSPECIFIED. ) ;
#27923=CARTESIAN_POINT ( 'NONE',  ( 0.3626713113217782114, -1.760022178122295777, -0.5161757929854556837 ) ) ;
#27924=DIRECTION ( 'NONE',  ( 0.4999551463232372317, -0.8660512985181135770, 0.000000000000000000 ) ) ;
#27930=CARTESIAN_POINT ( 'NONE',  ( 0.5122377809615301647, -1.683552081278821833, -0.5849915291001885898 ) ) ;
#27944=ORIENTED_EDGE ( 'NONE', *, *, #25995, .T. ) ;
#27947=DIRECTION ( 'NONE',  ( 1.000000000000000000, 0.000000000000000000, 0.000000000000000000 ) ) ;
#27955=CARTESIAN_POINT ( 'NONE',  ( 0.2065475242433257030, -1.810140062844285413, -0.3513024119729122874 ) ) ;
#27957=CARTESIAN_POINT ( 'NONE',  ( 0.5648676111026831315, -1.582764309389034896, -0.4871114102051288253 ) ) ;
#27960=CIRCLE ( 'NONE', #30594, 0.02999999999999997113 ) ;
#27961=CARTESIAN_POINT ( 'NONE',  ( 0.3999999999999787059, -2.120797187169804143, -0.5256435360466945594 ) ) ;
#27975=CARTESIAN_POINT ( 'NONE',  ( 0.1786812025795815329, -1.892228462347241624, -0.6870626404130494302 ) ) ;
#27980=ORIENTED_EDGE ( 'NONE', *, *, #12873, .T. ) ;
#27987=CIRCLE ( 'NONE', #3668, 0.2200000000000000566 ) ;
#27992=CARTESIAN_POINT ( 'NONE',  ( 0.4974655663051580357, -1.692079803311779873, -0.4360563182030788854 ) ) ;
#27997=CARTESIAN_POINT ( 'NONE',  ( 0.4183807527607137922, -1.702160111122825059, -0.4180178025648325080 ) ) ;
#28002=CARTESIAN_POINT ( 'NONE',  ( 0.4022495603007555931, -1.747046214996282432, -0.4499298451809822796 ) ) ;
#28013=DIRECTION ( 'NONE',  ( 0.4999551463232373427, -0.8660512985181134660, 0.000000000000000000 ) ) ;
#28027=EDGE_CURVE ( 'NONE', #36736, #17902, #39625, .T. ) ;
#28041=ORIENTED_EDGE ( 'NONE', *, *, #24305, .F. ) ;
#28044=CARTESIAN_POINT ( 'NONE',  ( 0.3396305973613506501, -1.637478036087311350, -0.5914524579777636903 ) ) ;
#28047=CARTESIAN_POINT ( 'NONE',  ( 0.4588468109159730135, -1.044667397767246708, -0.4248180574663139586 ) ) ;
#28050=B_SPLINE_CURVE_WITH_KNOTS ( 'NONE', 3,
 ( #25595, #15917, #25805, #10364 ),
 .UNSPECIFIED., .F., .F.,
 ( 4, 4 ),
 ( 5.485677294651091042E-18, 0.003354154147083482796 ),
 .UNSPECIFIED. ) ;
#28051=ORIENTED_EDGE ( 'NONE', *, *, #19064, .T. ) ;
#28053=CARTESIAN_POINT ( 'NONE',  ( 0.1909286924077255032, -1.257064795538239022, -0.5931747813493344346 ) ) ;
#28062=AXIS2_PLACEMENT_3D ( 'NONE', #20308, #17417, #39417 ) ;
#28063=CARTESIAN_POINT ( 'NONE',  ( 0.3784855106043947814, -1.091058466892998347, -0.5155029497116575543 ) ) ;
#28071=CARTESIAN_POINT ( 'NONE',  ( 0.4704749616853449168, -1.069673565160275341, -0.4234913399341371787 ) ) ;
#28075=EDGE_CURVE ( 'NONE', #25550, #14915, #17283, .T. ) ;
#28079=DIRECTION ( 'NONE',  ( 1.000000000000000000, 0.000000000000000000, 0.000000000000000000 ) ) ;
#28080=B_SPLINE_CURVE_WITH_KNOTS ( 'NONE', 3,
 ( #17635, #30182, #39636, #2419 ),
 .UNSPECIFIED., .F., .F.,
 ( 4, 4 ),
 ( 0.000000000000000000, 0.0002675641918131738258 ),
 .UNSPECIFIED. ) ;
#28090=CARTESIAN_POINT ( 'NONE',  ( 0.3607657536367212536, -1.946668260980969345, -0.3283241642772302127 ) ) ;
#28098=FACE_OUTER_BOUND ( 'NONE', #40415, .T. ) ;
#28102=CARTESIAN_POINT ( 'NONE',  ( 0.3969700875656382300, -1.750093955434189663, -0.5306525527942058673 ) ) ;
#28103=PLANE ( 'NONE',  #25763 ) ;
#28105=CARTESIAN_POINT ( 'NONE',  ( 0.3940832238624992767, -1.985670795305536140, -0.2899752743292205448 ) ) ;
#28111=CARTESIAN_POINT ( 'NONE',  ( 0.1784968570797965948, -1.218054820023663831, -0.5155029497116575543 ) ) ;
#28117=CARTESIAN_POINT ( 'NONE',  ( 0.6618556493260480122, -1.443346534042697638, -0.4155153992717031675 ) ) ;
#28118=CARTESIAN_POINT ( 'NONE',  ( 0.3903407250317349475, -1.765467622026976491, -0.4499573014716374830 ) ) ;
#28119=DIRECTION ( 'NONE',  ( 0.8660512985181135770, 0.4999551463232370652, -1.983296656985675225E-15 ) ) ;
#28128=CARTESIAN_POINT ( 'NONE',  ( 0.5368080558625972776, -1.632053713898605984, -0.4360733739357021133 ) ) ;
#28131=CARTESIAN_POINT ( 'NONE',  ( 0.5360939587443181997, -1.669780357970381601, -0.5511600881812523944 ) ) ;
#28144=ORIENTED_EDGE ( 'NONE', *, *, #26043, .F. ) ;
#28155=CARTESIAN_POINT ( 'NONE',  ( 0.1357105165892663889, -2.107936428766272741, -0.2870436526301869407 ) ) ;
#28157=CARTESIAN_POINT ( 'NONE',  ( 0.5810193296476801050, -1.554241992011831996, -0.4294310414331839465 ) ) ;
#28163=CARTESIAN_POINT ( 'NONE',  ( 0.2569741121304622844, -1.653347272235380361, -0.6637523221072149093 ) ) ;
#28175=VERTEX_POINT ( 'NONE', #2463 ) ;
#28176=ORIENTED_EDGE ( 'NONE', *, *, #33145, .F. ) ;
#28188=CARTESIAN_POINT ( 'NONE',  ( 0.5136163779962517051, -1.682756243106886318, -0.4473473194278146936 ) ) ;
#28195=B_SPLINE_CURVE_WITH_KNOTS ( 'NONE', 3,
 ( #17897, #39500, #11331, #33335, #5335, #33138, #30464, #15031, #33526, #8030, #8241, #24112, #17304, #23690 ),
 .UNSPECIFIED., .F., .F.,
 ( 4, 2, 2, 2, 2, 2, 4 ),
 ( 0.000000000000000000, 0.001093382690672758516, 0.001640074036009137558, 0.002186765381345516599, 0.002733456726681895640, 0.003280148072018274682, 0.004373530762691031464 ),
 .UNSPECIFIED. ) ;
#28197=CARTESIAN_POINT ( 'NONE',  ( 0.3984114568195522010, -1.599003643269838904, -0.5155029497116575543 ) ) ;
#28203=DIRECTION ( 'NONE',  ( 0.000000000000000000, 1.000000000000000000, -1.224646799147353207E-16 ) ) ;
#28206=DIRECTION ( 'NONE',  ( 0.000000000000000000, 0.2751755752258863152, 0.9613939893712164508 ) ) ;
#28218=CARTESIAN_POINT ( 'NONE',  ( 0.4623247243936773332, -1.147348113996353502, -0.6255478604071451620 ) ) ;
#28233=B_SPLINE_CURVE_WITH_KNOTS ( 'NONE', 3,
 ( #1306, #10956, #1114, #13621, #29660, #36032, #20007, #26186, #14018, #38710, #10530, #13811, #35626, #7836 ),
 .UNSPECIFIED., .F., .F.,
 ( 4, 2, 2, 2, 2, 2, 4 ),
 ( 0.000000000000000000, 0.0007668932026506553078, 0.001150339803975984100, 0.001533786405301312784, 0.001917233006626641468, 0.002300679607951969935, 0.003067572810602619930 ),
 .UNSPECIFIED. ) ;
#28237=CARTESIAN_POINT ( 'NONE',  ( 0.2059273467974225835, -1.283046334493782359, -0.4400554600884078460 ) ) ;
#28244=EDGE_CURVE ( 'NONE', #16545, #357, #22090, .T. ) ;
#28245=CARTESIAN_POINT ( 'NONE',  ( 0.4634712904840416758, -1.711704060178988129, -0.5155029497116575543 ) ) ;
#28248=CARTESIAN_POINT ( 'NONE',  ( 0.2059273467974226945, -1.283046334493782803, -0.2869361388274795921 ) ) ;
#28252=CARTESIAN_POINT ( 'NONE',  ( 0.3571225321066454073, -1.899149384614340130, -0.5066234194226268972 ) ) ;
#28258=VERTEX_POINT ( 'NONE', #36999 ) ;
#28261=CIRCLE ( 'NONE', #34168, 0.2000000000000000111 ) ;
#28272=CARTESIAN_POINT ( 'NONE',  ( 0.1984983582844195016, -2.028698869828995388, -0.3115429933617774316 ) ) ;
#28275=CARTESIAN_POINT ( 'NONE',  ( -0.002218965743620939825, -1.368565310413371705, -0.3828039145932563558 ) ) ;
#28282=CARTESIAN_POINT ( 'NONE',  ( 0.4833924548366955731, -1.608298341119788422, -0.3888178814765106406 ) ) ;
#28302=CIRCLE ( 'NONE', #29629, 0.1875727115490685715 ) ;
#28303=CARTESIAN_POINT ( 'NONE',  ( 0.6033996618073826923, -1.480667803124354531, -0.5155029497116575543 ) ) ;
#28311=CARTESIAN_POINT ( 'NONE',  ( 0.3853365039963215222, -1.652093682163140453, -0.3956870249903657322 ) ) ;
#28315=EDGE_LOOP ( 'NONE', ( #33531, #5901, #39228, #13982 ) ) ;
#28316=CARTESIAN_POINT ( 'NONE',  ( 0.3544525855956190963, -1.628498139902242681, -0.6593841416022943047 ) ) ;
#28325=EDGE_LOOP ( 'NONE', ( #5183, #8009, #30137, #37323, #8741, #27187, #14781 ) ) ;
#28341=CARTESIAN_POINT ( 'NONE',  ( 0.1734973056165642902, -1.209394307038482497, -0.5155029497116575543 ) ) ;
#28346=CARTESIAN_POINT ( 'NONE',  ( 0.07420452683010890504, -1.738585387657813675, -0.3647249226900559083 ) ) ;
#28348=CARTESIAN_POINT ( 'NONE',  ( 0.6572879434354249595, -1.449559110403086049, -0.6172981636778317460 ) ) ;
#28351=CARTESIAN_POINT ( 'NONE',  ( 0.3436484202359983975, -1.636297845364965697, -0.6542514959024295917 ) ) ;
#28354=CARTESIAN_POINT ( 'NONE',  ( 0.4264202721361137760, -1.467519734074644200, -0.5166151207188711680 ) ) ;
#28357=CARTESIAN_POINT ( 'NONE',  ( 0.3005522690096895100, -1.423263844426111868, -0.7187326247832939163 ) ) ;
#28361=CIRCLE ( 'NONE', #30996, 0.05000000000000000971 ) ;
#28366=DIRECTION ( 'NONE',  ( 0.8660512985181131329, 0.4999551463232376758, 0.000000000000000000 ) ) ;
#28368=CIRCLE ( 'NONE', #6087, 0.1033070866141732880 ) ;
#28373=CARTESIAN_POINT ( 'NONE',  ( 0.1960722456818423942, -1.288731303253011218, -0.2917126172454974631 ) ) ;
#28388=CARTESIAN_POINT ( 'NONE',  ( 0.5026806121458677890, -1.673566903547699436, -0.4262783769486948593 ) ) ;
#28395=CARTESIAN_POINT ( 'NONE',  ( 0.1909286924077255032, -1.257064795538239022, -0.7462941026102624109 ) ) ;
#28397=ORIENTED_EDGE ( 'NONE', *, *, #9477, .F. ) ;
#28440=CARTESIAN_POINT ( 'NONE',  ( 0.5749953953004710572, -1.612551028885189863, -0.5288418706057514962 ) ) ;
#28449=DIRECTION ( 'NONE',  ( 0.4999551463232372317, -0.8660512985181135770, 0.000000000000000000 ) ) ;
#28468=CARTESIAN_POINT ( 'NONE',  ( 0.1999999999999789724, -2.183180860297921466, -0.4937760292030871079 ) ) ;
#28471=VERTEX_POINT ( 'NONE', #26106 ) ;
#28474=ORIENTED_EDGE ( 'NONE', *, *, #16068, .T. ) ;
#28476=CARTESIAN_POINT ( 'NONE',  ( 0.3959837544953576094, -1.690093441653652162, -0.5214913642057524834 ) ) ;
#28480=ORIENTED_EDGE ( 'NONE', *, *, #11146, .F. ) ;
#28484=EDGE_LOOP ( 'NONE', ( #2195, #13641, #23550, #32537 ) ) ;
#28485=AXIS2_PLACEMENT_3D ( 'NONE', #28118, #37885, #21955 ) ;
#28489=EDGE_CURVE ( 'NONE', #357, #31608, #20585, .T. ) ;
#28490=CARTESIAN_POINT ( 'NONE',  ( 0.4501395481517306285, -1.610781249451892716, -0.3723713353267660287 ) ) ;
#28517=CARTESIAN_POINT ( 'NONE',  ( 0.1909286924077254755, -1.257064795538238577, -0.6405900374560394850 ) ) ;
#28518=EDGE_CURVE ( 'NONE', #29909, #37390, #10707, .T. ) ;
#28521=CARTESIAN_POINT ( 'NONE',  ( 0.4102377630207764692, -1.609602033329217141, -0.3618696079564429624 ) ) ;
#28529=CARTESIAN_POINT ( 'NONE',  ( 0.5240088150632713493, -1.676756884404518200, -0.5894117387006844178 ) ) ;
#28538=EDGE_LOOP ( 'NONE', ( #17004, #36466 ) ) ;
#28548=LINE ( 'NONE', #422, #20456 ) ;
#28557=CARTESIAN_POINT ( 'NONE',  ( 0.1367339749541140737, -1.455102376090395389, -0.3611272873345107159 ) ) ;
#28558=CARTESIAN_POINT ( 'NONE',  ( 0.6006288095222466206, -1.388058312517433057, -0.6250000000000001110 ) ) ;
#28559=CIRCLE ( 'NONE', #22575, 0.04330708661417343591 ) ;
#28560=DIRECTION ( 'NONE',  ( 0.8660512985181130219, 0.4999551463232377868, 0.000000000000000000 ) ) ;
#28567=CARTESIAN_POINT ( 'NONE',  ( -0.002385887202282944899, -1.874416880861737633, -0.6477095634347505015 ) ) ;
#28578=AXIS2_PLACEMENT_3D ( 'NONE', #14720, #33432, #40207 ) ;
#28581=CARTESIAN_POINT ( 'NONE',  ( 0.6147843586992604026, -1.475607795738035577, -0.4128325507852580456 ) ) ;
#28582=EDGE_CURVE ( 'NONE', #22431, #22474, #19262, .T. ) ;
#28585=ADVANCED_FACE ( 'NONE', ( #23220, #3676 ), #1412, .F. ) ;
#28587=ORIENTED_EDGE ( 'NONE', *, *, #37119, .F. ) ;
#28588=FACE_OUTER_BOUND ( 'NONE', #2140, .T. ) ;
#28589=ORIENTED_EDGE ( 'NONE', *, *, #6864, .T. ) ;
#28606=VERTEX_POINT ( 'NONE', #16415 ) ;
#28610=CARTESIAN_POINT ( 'NONE',  ( 0.3923243630925510872, -1.966611948492501316, -0.4968729097670202544 ) ) ;
#28618=CIRCLE ( 'NONE', #31905, 0.1700000000000000400 ) ;
#28622=CARTESIAN_POINT ( 'NONE',  ( 0.3913752891026081038, -1.689869761680007576, -0.4075552329090693093 ) ) ;
#28628=CARTESIAN_POINT ( 'NONE',  ( 0.4176572489918210507, -1.668871684954134071, -0.5229746796350916993 ) ) ;
#28641=CARTESIAN_POINT ( 'NONE',  ( 0.4710977142973158394, -1.661186711027925256, -0.4170720528719219500 ) ) ;
#28642=ORIENTED_EDGE ( 'NONE', *, *, #2602, .F. ) ;
#28649=ADVANCED_FACE ( 'NONE', ( #38816 ), #2841, .T. ) ;
#28652=ORIENTED_EDGE ( 'NONE', *, *, #2602, .T. ) ;
#28658=CARTESIAN_POINT ( 'NONE',  ( 0.5964376879960640032, -1.583813977042451526, -0.6035257017628796739 ) ) ;
#28662=AXIS2_PLACEMENT_3D ( 'NONE', #4593, #11198, #13671 ) ;
#28664=CARTESIAN_POINT ( 'NONE',  ( 0.4361429146967321646, -1.593406671728312185, -0.6128992538235386034 ) ) ;
#28674=ADVANCED_FACE ( 'NONE', ( #7556 ), #30875, .F. ) ;
#28679=FACE_OUTER_BOUND ( 'NONE', #9718, .T. ) ;
#28682=ORIENTED_EDGE ( 'NONE', *, *, #703, .T. ) ;
#28689=FACE_OUTER_BOUND ( 'NONE', #21752, .T. ) ;
#28697=ORIENTED_EDGE ( 'NONE', *, *, #20550, .T. ) ;
#28707=CARTESIAN_POINT ( 'NONE',  ( 0.3572222731481287661, -1.622781385286526934, -0.3671481750039431446 ) ) ;
#28731=CARTESIAN_POINT ( 'NONE',  ( 0.4700139829499337396, -1.130594080169405657, -0.6582979126921139068 ) ) ;
#28732=CARTESIAN_POINT ( 'NONE',  ( 0.4151543154610584652, -1.647056610985331959, -0.4022728307239534229 ) ) ;
#28738=CARTESIAN_POINT ( 'NONE',  ( 0.2059273467974226668, -1.283046334493782359, -0.7462941026102624109 ) ) ;
#28743=VERTEX_POINT ( 'NONE', #6078 ) ;
#28750=CARTESIAN_POINT ( 'NONE',  ( 0.1960940348462748284, -2.001616103433511817, -0.3183625921796859326 ) ) ;
#28758=VERTEX_POINT ( 'NONE', #28303 ) ;
#28766=FACE_OUTER_BOUND ( 'NONE', #9466, .T. ) ;
#28781=CARTESIAN_POINT ( 'NONE',  ( 0.4243666725459965261, -1.591076223527387867, -0.4156371400837810537 ) ) ;
#28783=CIRCLE ( 'NONE', #14979, 0.04330708661417336652 ) ;
#28801=CARTESIAN_POINT ( 'NONE',  ( 0.1134872160414416992, -1.333634162614142360, -0.3503315144562280659 ) ) ;
#28804=DIRECTION ( 'NONE',  ( 0.000000000000000000, 0.000000000000000000, -1.000000000000000000 ) ) ;
#28826=CARTESIAN_POINT ( 'NONE',  ( 0.3674944553547283554, -1.749262848119110814, -0.6770320976117242262 ) ) ;
#28828=CARTESIAN_POINT ( 'NONE',  ( 0.3678947686560505304, -1.763302576097276697, -0.5854506657463419694 ) ) ;
#28829=ORIENTED_EDGE ( 'NONE', *, *, #4851, .F. ) ;
#28836=CARTESIAN_POINT ( 'NONE',  ( 0.5254156872246980026, -1.636223382584907071, -0.4246476935767348748 ) ) ;
#28840=CARTESIAN_POINT ( 'NONE',  ( 0.4897592102757906130, -1.696528537887749932, -0.5984293649392183889 ) ) ;
#28841=VERTEX_POINT ( 'NONE', #33219 ) ;
#28851=CARTESIAN_POINT ( 'NONE',  ( 0.4621583407840581526, -1.042755713779721649, -0.5155029497116575543 ) ) ;
#28854=EDGE_CURVE ( 'NONE', #26101, #39763, #23016, .T. ) ;
#28855=FACE_OUTER_BOUND ( 'NONE', #23548, .T. ) ;
#28868=EDGE_CURVE ( 'NONE', #29847, #2400, #20893, .T. ) ;
#28882=DIRECTION ( 'NONE',  ( 0.8660512985181136880, 0.4999551463232369541, 0.000000000000000000 ) ) ;
#28890=CARTESIAN_POINT ( 'NONE',  ( 0.4819756813572292908, -1.590155287500744086, -0.4462383725080293351 ) ) ;
#28896=CARTESIAN_POINT ( 'NONE',  ( 0.6487533847785609264, -1.557452555468215483, -0.6098442386003093407 ) ) ;
#28922=CARTESIAN_POINT ( 'NONE',  ( 0.4650133494175291982, -1.133480851973431847, -0.6660426939124519663 ) ) ;
#28931=VERTEX_POINT ( 'NONE', #35627 ) ;
#28944=CARTESIAN_POINT ( 'NONE',  ( 0.02063935039522163395, -1.619419422640626438, -0.3749979873294493338 ) ) ;
#28953=CARTESIAN_POINT ( 'NONE',  ( 0.1886993031460024173, -1.963322156380002292, -0.6958836544861118911 ) ) ;
#28957=CARTESIAN_POINT ( 'NONE',  ( 0.6426786216763176185, -1.413792888462838127, -0.6263067080391584440 ) ) ;
#28963=CARTESIAN_POINT ( 'NONE',  ( 0.5844093222531523413, -1.481270550429968136, -0.4312484634772048575 ) ) ;
#28975=CARTESIAN_POINT ( 'NONE',  ( 0.4480646913441768131, -1.099213350020603164, -0.6275147848854655264 ) ) ;
#28980=ORIENTED_EDGE ( 'NONE', *, *, #22051, .T. ) ;
#28982=CARTESIAN_POINT ( 'NONE',  ( 0.3619943274630011421, -1.737009005337970313, -0.5415504813999939548 ) ) ;
#28984=DIRECTION ( 'NONE',  ( 0.4999551463232372317, -0.8660512985181133550, 0.000000000000000000 ) ) ;
#28990=CARTESIAN_POINT ( 'NONE',  ( 0.3926032618789407347, -1.756026311479913948, -0.5284552501753293496 ) ) ;
#28991=CARTESIAN_POINT ( 'NONE',  ( 0.001255696819123910566, -1.915471855958320146, -0.3089908321627916066 ) ) ;
#28995=CARTESIAN_POINT ( 'NONE',  ( -2.112273405726188513E-14, -2.183180860297921466, -0.4937760292030871079 ) ) ;
#29007=CARTESIAN_POINT ( 'NONE',  ( -2.112273405726188513E-14, -2.183180860297921466, -0.4937760292030871079 ) ) ;
#29009=CARTESIAN_POINT ( 'NONE',  ( 0.4030327056921976792, -1.680968334469209680, -0.4031266960524464982 ) ) ;
#29014=CARTESIAN_POINT ( 'NONE',  ( 0.1991480113865206902, -2.054949600705703983, -0.6841806413415666421 ) ) ;
#29019=EDGE_CURVE ( 'NONE', #19020, #16852, #37011, .T. ) ;
#29022=ORIENTED_EDGE ( 'NONE', *, *, #14430, .F. ) ;
#29029=CARTESIAN_POINT ( 'NONE',  ( 0.1273306340341417431, -1.236045459326737150, -0.5155029497116575543 ) ) ;
#29031=ADVANCED_FACE ( 'NONE', ( #9748 ), #6146, .T. ) ;
#29037=CIRCLE ( 'NONE', #1520, 0.04330708661417322775 ) ;
#29049=CARTESIAN_POINT ( 'NONE',  ( 0.2284923717121198627, -1.304659949875474068, -0.5155029497116575543 ) ) ;
#29051=DIRECTION ( 'NONE',  ( -1.000000000000000000, 0.000000000000000000, 0.000000000000000000 ) ) ;
#29052=CARTESIAN_POINT ( 'NONE',  ( 0.5187558892663555188, -1.611665626061807854, -0.5500361812898686420 ) ) ;
#29058=FACE_OUTER_BOUND ( 'NONE', #19437, .T. ) ;
#29064=CARTESIAN_POINT ( 'NONE',  ( 0.4559880809074943753, -1.138690969949424314, -0.5155029497116575543 ) ) ;
#29069=EDGE_LOOP ( 'NONE', ( #7113, #516, #32581, #33468, #16903 ) ) ;
#29079=ORIENTED_EDGE ( 'NONE', *, *, #32577, .F. ) ;
#29080=B_SPLINE_CURVE_WITH_KNOTS ( 'NONE', 3,
 ( #1615, #14533, #36746, #30178, #4650, #20735, #5070, #30380, #11251, #26708 ),
 .UNSPECIFIED., .F., .F.,
 ( 4, 2, 2, 2, 4 ),
 ( 2.347203303329887743E-16, 0.0006195027968147369868, 0.001239005593629237184, 0.001858508390443737489, 0.002478011187258237578 ),
 .UNSPECIFIED. ) ;
#29083=CARTESIAN_POINT ( 'NONE',  ( 0.3624697024925027655, -1.755837373810828383, -0.4903785605043212148 ) ) ;
#29085=AXIS2_PLACEMENT_3D ( 'NONE', #37258, #28203, #37449 ) ;
#29094=EDGE_CURVE ( 'NONE', #8354, #23099, #7765, .T. ) ;
#29102=CARTESIAN_POINT ( 'NONE',  ( 0.6635773287780962759, -1.472843899867129158, -0.6183064675240305119 ) ) ;
#29122=ORIENTED_EDGE ( 'NONE', *, *, #37717, .F. ) ;
#29123=DIRECTION ( 'NONE',  ( -0.4999551463232352333, 0.8660512985181146872, 0.000000000000000000 ) ) ;
#29126=CARTESIAN_POINT ( 'NONE',  ( 0.3545348113318227412, -1.718921438480950581, -0.4824991667906958215 ) ) ;
#29132=CARTESIAN_POINT ( 'NONE',  ( 0.2059273467974226113, -1.283046334493782359, -0.3194715457588298002 ) ) ;
#29133=CARTESIAN_POINT ( 'NONE',  ( 0.6620678144876760429, -1.446799780631947252, -0.4151272395384200675 ) ) ;
#29139=CARTESIAN_POINT ( 'NONE',  ( 0.5849095050029387011, -1.491341823319836335, -0.5960747874205124530 ) ) ;
#29142=LINE ( 'NONE', #1006, #34897 ) ;
#29150=VERTEX_POINT ( 'NONE', #4773 ) ;
#29154=ORIENTED_EDGE ( 'NONE', *, *, #29817, .T. ) ;
#29163=TOROIDAL_SURFACE ( 'NONE', #10137, 0.1333070866141734256, 0.02999999999999999889 ) ;
#29166=CARTESIAN_POINT ( 'NONE',  ( 0.3880702231493639021, -1.818540937610624519, -0.4825054957597859628 ) ) ;
#29171=CARTESIAN_POINT ( 'NONE',  ( 0.6430854927599457538, -1.494222493094318427, -0.6187715783251990231 ) ) ;
#29183=VERTEX_POINT ( 'NONE', #38943 ) ;
#29186=TOROIDAL_SURFACE ( 'NONE', #4881, 0.08830708661417342731, 0.01499999999999999944 ) ;
#29197=DIRECTION ( 'NONE',  ( 0.8660512985181133550, 0.4999551463232373982, 0.000000000000000000 ) ) ;
#29198=ORIENTED_EDGE ( 'NONE', *, *, #18726, .F. ) ;
#29200=ORIENTED_EDGE ( 'NONE', *, *, #17128, .T. ) ;
#29203=CARTESIAN_POINT ( 'NONE',  ( 0.5453720701673475668, -1.664424278530242329, -0.4777853237623809202 ) ) ;
#29205=CARTESIAN_POINT ( 'NONE',  ( -2.112273405726188513E-14, -2.183180860297921466, -0.7437760292030870524 ) ) ;
#29206=CARTESIAN_POINT ( 'NONE',  ( 0.04890254750393845107, -1.632792488206058712, -0.3425393862321154392 ) ) ;
#29217=CIRCLE ( 'NONE', #37757, 0.08830708661417320526 ) ;
#29218=B_SPLINE_CURVE_WITH_KNOTS ( 'NONE', 3,
 ( #21539, #23471, #12058, #2401, #17061, #27689, #2591, #18016, #5672, #32883 ),
 .UNSPECIFIED., .F., .F.,
 ( 4, 2, 2, 2, 4 ),
 ( 0.000000000000000000, 0.0007428348738404900358, 0.001485669747680980072, 0.002228504621521470216, 0.002971339495361960143 ),
 .UNSPECIFIED. ) ;
#29227=DIRECTION ( 'NONE',  ( 0.8660512985181132439, 0.4999551463232376758, -6.610988856618925964E-16 ) ) ;
#29229=CARTESIAN_POINT ( 'NONE',  ( 0.1947176629093842759, -1.666009496152422331, -0.6564531187584504712 ) ) ;
#29241=ORIENTED_EDGE ( 'NONE', *, *, #19196, .T. ) ;
#29243=B_SPLINE_CURVE_WITH_KNOTS ( 'NONE', 3,
 ( #2595, #36548, #2200, #24411 ),
 .UNSPECIFIED., .F., .F.,
 ( 4, 4 ),
 ( 0.000000000000000000, 0.001825717054875163796 ),
 .UNSPECIFIED. ) ;
#29244=ORIENTED_EDGE ( 'NONE', *, *, #27646, .F. ) ;
#29245=VERTEX_POINT ( 'NONE', #35866 ) ;
#29253=CARTESIAN_POINT ( 'NONE',  ( 0.5264113014007612001, -1.640729993778266893, -0.5166151207188711680 ) ) ;
#29254=ORIENTED_EDGE ( 'NONE', *, *, #14263, .T. ) ;
#29258=CARTESIAN_POINT ( 'NONE',  ( 0.1989976604547370465, -2.047409678865564686, -0.7132172901365274598 ) ) ;
#29262=DIRECTION ( 'NONE',  ( 0.4999551463232373427, -0.8660512985181134660, 0.000000000000000000 ) ) ;
#29264=B_SPLINE_CURVE_WITH_KNOTS ( 'NONE', 3,
 ( #32501, #39287, #38676, #7391, #35999, #17278, #19756, #10494 ),
 .UNSPECIFIED., .F., .F.,
 ( 4, 2, 2, 4 ),
 ( 0.000000000000000000, 0.0002979885802634735085, 0.0005959771605269470170, 0.001191954321053893167 ),
 .UNSPECIFIED. ) ;
#29288=EDGE_CURVE ( 'NONE', #37556, #6802, #4806, .T. ) ;
#29290=CARTESIAN_POINT ( 'NONE',  ( 0.3666666666666451024, -1.962130349776132210, -0.6793646662227855737 ) ) ;
#29325=CARTESIAN_POINT ( 'NONE',  ( 0.2574750998419692571, -1.178235494106686154, -0.5155029497116575543 ) ) ;
#29326=EDGE_CURVE ( 'NONE', #25550, #26020, #6790, .T. ) ;
#29361=DIRECTION ( 'NONE',  ( 0.8185200378235019114, 0.4725162423735941863, -0.3267313091433876049 ) ) ;
#29368=VERTEX_POINT ( 'NONE', #24901 ) ;
#29369=CARTESIAN_POINT ( 'NONE',  ( 0.5442403261713570917, -1.629017118762910110, -0.4460973077508758600 ) ) ;
#29374=ADVANCED_FACE ( 'NONE', ( #37424 ), #38328, .T. ) ;
#29376=CARTESIAN_POINT ( 'NONE',  ( 0.3853411735684887929, -1.756807109041803150, -0.4499573014716107822 ) ) ;
#29381=DIRECTION ( 'NONE',  ( 0.4999551463232373427, -0.8660512985181134660, 0.000000000000000000 ) ) ;
#29387=CARTESIAN_POINT ( 'NONE',  ( 0.5623653675682384057, -1.585032882041435665, -0.5293222829744327340 ) ) ;
#29391=CARTESIAN_POINT ( 'NONE',  ( 0.5461026827453100418, -1.628340864554156164, -0.5817929004078826738 ) ) ;
#29397=ORIENTED_EDGE ( 'NONE', *, *, #33932, .F. ) ;
#29406=CARTESIAN_POINT ( 'NONE',  ( 0.4378213252392034738, -1.692012427937505281, -0.4124588244304266405 ) ) ;
#29408=CARTESIAN_POINT ( 'NONE',  ( 0.5431858176847103037, -1.654083725324065002, -0.4764654179353626229 ) ) ;
#29411=CARTESIAN_POINT ( 'NONE',  ( 0.03398077991772324724, -1.810320368642273303, -0.3262651145211540871 ) ) ;
#29413=PLANE ( 'NONE',  #5992 ) ;
#29423=CARTESIAN_POINT ( 'NONE',  ( 0.2923286432308245808, -1.660243258845594649, -0.3370932271639339728 ) ) ;
#29424=DIRECTION ( 'NONE',  ( -0.4999551463232372872, 0.8660512985181134660, 0.000000000000000000 ) ) ;
#29429=TOROIDAL_SURFACE ( 'NONE', #32682, 0.04999999999999998196, 0.2000000000000000111 ) ;
#29433=CARTESIAN_POINT ( 'NONE',  ( 0.3938990593055637368, -1.751866802361104369, -0.5730325442411768888 ) ) ;
#29443=ORIENTED_EDGE ( 'NONE', *, *, #19009, .F. ) ;
#29449=VERTEX_POINT ( 'NONE', #23028 ) ;
#29451=DIRECTION ( 'NONE',  ( -0.4999551463232377313, 0.8660512985181132439, -0.000000000000000000 ) ) ;
#29452=CARTESIAN_POINT ( 'NONE',  ( 0.6265145376157257306, -1.617582256290212017, -0.4718557182044338383 ) ) ;
#29455=VERTEX_POINT ( 'NONE', #23236 ) ;
#29462=DIRECTION ( 'NONE',  ( 0.8660512985181132439, 0.4999551463232376758, 0.000000000000000000 ) ) ;
#29465=CARTESIAN_POINT ( 'NONE',  ( 0.4134082608409563320, -1.687121258993206308, -0.4232165953256796231 ) ) ;
#29468=CARTESIAN_POINT ( 'NONE',  ( 0.1994740068363788088, -2.042640899752901529, -0.2765909798240095974 ) ) ;
#29471=CARTESIAN_POINT ( 'NONE',  ( 0.6409058204046232943, -1.459016202299332710, -0.5155029497116575543 ) ) ;
#29477=CARTESIAN_POINT ( 'NONE',  ( 0.5058599984363495450, -1.583313914148366752, -0.4933326546058600659 ) ) ;
#29480=CARTESIAN_POINT ( 'NONE',  ( 0.1999999999999759193, -1.905617227352954135, -0.6587955718153066798 ) ) ;
#29484=CARTESIAN_POINT ( 'NONE',  ( 0.5473076987003111515, -1.651760216406904513, -0.4929644493450987541 ) ) ;
#29491=CARTESIAN_POINT ( 'NONE',  ( 0.3566968277947379362, -1.787709349577662810, -0.5192541119936813221 ) ) ;
#29496=EDGE_CURVE ( 'NONE', #38085, #25046, #26550, .T. ) ;
#29507=ORIENTED_EDGE ( 'NONE', *, *, #38152, .T. ) ;
#29508=ORIENTED_EDGE ( 'NONE', *, *, #6627, .T. ) ;
#29520=CARTESIAN_POINT ( 'NONE',  ( 0.03819165667510639878, -1.740319606980962996, -0.3346916167941055842 ) ) ;
#29528=CARTESIAN_POINT ( 'NONE',  ( 0.02999999938246960748, -2.094414908375987761, -0.7275123218652694845 ) ) ;
#29537=EDGE_CURVE ( 'NONE', #8017, #13521, #14611, .T. ) ;
#29543=VERTEX_POINT ( 'NONE', #28975 ) ;
#29544=EDGE_CURVE ( 'NONE', #2027, #35001, #38666, .T. ) ;
#29547=( BOUNDED_SURFACE ( )  B_SPLINE_SURFACE ( 3, 2, ( 
 ( #16193, #7095, #15762 ),
 ( #28521, #28732, #18873 ),
 ( #12672, #25859, #6302 ),
 ( #22175, #181, #593 ),
 ( #22781, #19664, #6902 ),
 ( #37776, #31602, #9598 ),
 ( #12895, #9998, #32009 ),
 ( #16375, #28311, #13087 ) ),
 .UNSPECIFIED., .F., .F., .T. ) 
 B_SPLINE_SURFACE_WITH_KNOTS ( ( 4, 2, 2, 4 ),
 ( 3, 3 ),
 ( 0.001521769427996497474, 0.002374549442172081172, 0.002800939449259872913, 0.003227329456347664653 ),
 ( 0.000000000000000000, 1.000000000000000000 ),
 .UNSPECIFIED. ) 
 GEOMETRIC_REPRESENTATION_ITEM ( )  RATIONAL_B_SPLINE_SURFACE ( (
 ( 1.000000000000000000, 0.4512702095618630893, 1.000000000000000000),
 ( 1.000000000000000000, 0.4832373129657441813, 1.000000000000000000),
 ( 1.000000000000000000, 0.5089024703303249852, 1.000000000000000000),
 ( 1.000000000000000000, 0.5356172533981554684, 1.000000000000000000),
 ( 1.000000000000000000, 0.5425363809967062023, 1.000000000000000000),
 ( 1.000000000000000000, 0.5510866447777388322, 1.000000000000000000),
 ( 1.000000000000000000, 0.5527681761118921067, 1.000000000000000000),
 ( 1.000000000000000000, 0.5517613080878603915, 1.000000000000000000) ) ) 
 REPRESENTATION_ITEM ( '' )  SURFACE ( )  );
#29550=CARTESIAN_POINT ( 'NONE',  ( 0.4666806433631038864, -1.098312294252236532, -0.6371104447086228806 ) ) ;
#29552=EDGE_LOOP ( 'NONE', ( #15721, #8938, #39707, #32125, #1093 ) ) ;
#29563=FACE_OUTER_BOUND ( 'NONE', #36615, .T. ) ;
#29568=CARTESIAN_POINT ( 'NONE',  ( 0.1734973056165642902, -1.209394307038482497, -0.5155029497116575543 ) ) ;
#29571=CARTESIAN_POINT ( 'NONE',  ( 0.6626494750595320893, -1.486816775434632865, -0.6188922402621547247 ) ) ;
#29577=CARTESIAN_POINT ( 'NONE',  ( 0.5818810567066877715, -1.520385204644366439, -0.5792601642121770755 ) ) ;
#29585=ORIENTED_EDGE ( 'NONE', *, *, #32637, .F. ) ;
#29595=CARTESIAN_POINT ( 'NONE',  ( -2.112273405726188513E-14, -2.097675824466503691, -0.2907077406111384099 ) ) ;
#29604=CARTESIAN_POINT ( 'NONE',  ( 0.1465864560099491842, -1.332653898859956332, -0.3147756667838505495 ) ) ;
#29607=CARTESIAN_POINT ( 'NONE',  ( 0.05361885722424606510, -1.467584822755955143, -0.6509794481950387235 ) ) ;
#29617=FACE_OUTER_BOUND ( 'NONE', #27380, .T. ) ;
#29618=CARTESIAN_POINT ( 'NONE',  ( 0.4460585320772065820, -1.103542852913448558, -0.6309016134502297701 ) ) ;
#29623=CARTESIAN_POINT ( 'NONE',  ( 0.3320003377790358146, -1.522026588550927428, -0.7092149976984114534 ) ) ;
#29624=DIRECTION ( 'NONE',  ( -0.7723395547766002123, 0.000000000000000000, 0.6352098961189780457 ) ) ;
#29628=CARTESIAN_POINT ( 'NONE',  ( 0.3790501254121775299, -1.751389653868420826, -0.5849892083899181916 ) ) ;
#29629=AXIS2_PLACEMENT_3D ( 'NONE', #19890, #1202, #3440 ) ;
#29644=ORIENTED_EDGE ( 'NONE', *, *, #25225, .T. ) ;
#29652=ORIENTED_EDGE ( 'NONE', *, *, #39949, .T. ) ;
#29657=AXIS2_PLACEMENT_3D ( 'NONE', #7257, #32977, #3982 ) ;
#29660=CARTESIAN_POINT ( 'NONE',  ( 0.4616332724396642329, -1.592054364389571042, -0.4300420834888027954 ) ) ;
#29678=CARTESIAN_POINT ( 'NONE',  ( 0.4078704035844273323, -1.593543170983706236, -0.6183053384820467180 ) ) ;
#29682=ORIENTED_EDGE ( 'NONE', *, *, #10982, .F. ) ;
#29683=CARTESIAN_POINT ( 'NONE',  ( -2.112273405726188513E-14, -1.837418632672298768, -0.6339733133327630776 ) ) ;
#29686=DIRECTION ( 'NONE',  ( -0.4999551463232372317, 0.8660512985181135770, -0.000000000000000000 ) ) ;
#29693=EDGE_LOOP ( 'NONE', ( #28682, #18897, #37315, #13352, #34283 ) ) ;
#29694=CARTESIAN_POINT ( 'NONE',  ( 0.03022635123008331204, -1.916038177046143876, -0.6843378419889921682 ) ) ;
#29696=CARTESIAN_POINT ( 'NONE',  ( 0.3595056509374958686, -1.929564378396709357, -0.4933486092489832719 ) ) ;
#29700=CARTESIAN_POINT ( 'NONE',  ( 0.2209260011871197193, -1.309027873449325918, -0.4125659523519145666 ) ) ;
#29712=DIRECTION ( 'NONE',  ( -0.4999551463232372317, 0.8660512985181135770, -0.000000000000000000 ) ) ;
#29718=CARTESIAN_POINT ( 'NONE',  ( 0.3699999999999786793, -2.097675824466503691, -0.4688691127277797022 ) ) ;
#29721=CARTESIAN_POINT ( 'NONE',  ( 0.5337902897905772992, -1.637138699848535328, -0.5488759256308870516 ) ) ;
#29736=EDGE_CURVE ( 'NONE', #23137, #18407, #17982, .T. ) ;
#29753=CARTESIAN_POINT ( 'NONE',  ( 0.1424029337235096226, -1.400533250147911746, -0.6250000000000000000 ) ) ;
#29756=PLANE ( 'NONE',  #5037 ) ;
#29762=CARTESIAN_POINT ( 'NONE',  ( 0.3756960969702827779, -1.762375030584327984, -0.4374392251508507079 ) ) ;
#29765=LINE ( 'NONE', #20122, #37120 ) ;
#29775=EDGE_CURVE ( 'NONE', #35263, #20307, #4209, .T. ) ;
#29776=CARTESIAN_POINT ( 'NONE',  ( 0.6050535996821563289, -1.589783510039989967, -0.5530470261699707013 ) ) ;
#29784=CARTESIAN_POINT ( 'NONE',  ( 0.6144487089066268393, -1.489086973007883730, -0.6152890497467740083 ) ) ;
#29793=CARTESIAN_POINT ( 'NONE',  ( 0.3711231209398546671, -1.768532844275155780, -0.5764367090175167574 ) ) ;
#29804=B_SPLINE_CURVE_WITH_KNOTS ( 'NONE', 3,
 ( #14635, #24135, #11355, #36657 ),
 .UNSPECIFIED., .F., .F.,
 ( 4, 4 ),
 ( 8.673617379884035472E-19, 0.0003185022396561879823 ),
 .UNSPECIFIED. ) ;
#29812=CARTESIAN_POINT ( 'NONE',  ( 0.1734973056165642902, -1.209394307038482497, -0.5155029497116575543 ) ) ;
#29813=ORIENTED_EDGE ( 'NONE', *, *, #975, .F. ) ;
#29817=EDGE_CURVE ( 'NONE', #38249, #30555, #18477, .T. ) ;
#29825=EDGE_CURVE ( 'NONE', #34037, #40101, #39684, .T. ) ;
#29828=DIRECTION ( 'NONE',  ( 0.4999551463232373427, -0.8660512985181134660, 0.000000000000000000 ) ) ;
#29843=EDGE_LOOP ( 'NONE', ( #24211, #16533, #23720, #25001 ) ) ;
#29847=VERTEX_POINT ( 'NONE', #16589 ) ;
#29848=CARTESIAN_POINT ( 'NONE',  ( 0.4738546087217680447, -1.652018268363229181, -0.3975985852014398136 ) ) ;
#29866=EDGE_CURVE ( 'NONE', #12338, #28931, #27863, .T. ) ;
#29870=TOROIDAL_SURFACE ( 'NONE', #22016, 0.05330708661417323663, 0.01000000000000000021 ) ;
#29873=FACE_OUTER_BOUND ( 'NONE', #31322, .T. ) ;
#29876=CARTESIAN_POINT ( 'NONE',  ( 0.4134438183949054602, -1.708815802511751025, -0.4210476217684242517 ) ) ;
#29877=CARTESIAN_POINT ( 'NONE',  ( 0.3827496839977685417, -1.607288045992097070, -0.3194649185273498171 ) ) ;
#29883=CARTESIAN_POINT ( 'NONE',  ( 0.3656015928468621112, -1.617944161404246906, -0.4193447143115660025 ) ) ;
#29885=ADVANCED_FACE ( 'NONE', ( #32019 ), #19361, .T. ) ;
#29887=CARTESIAN_POINT ( 'NONE',  ( 0.6215918093157997149, -1.606820104549159245, -0.5669819737327814746 ) ) ;
#29894=CARTESIAN_POINT ( 'NONE',  ( 0.4126538731429406082, -1.611929415335916271, -0.6681135029249770652 ) ) ;
#29897=CARTESIAN_POINT ( 'NONE',  ( 0.3463972363130231047, -1.700516749477267053, -0.5547452799823860969 ) ) ;
#29900=EDGE_CURVE ( 'NONE', #37623, #2187, #18999, .T. ) ;
#29909=VERTEX_POINT ( 'NONE', #17605 ) ;
#29910=CARTESIAN_POINT ( 'NONE',  ( 0.04917380528055519118, -1.483446811033737989, -0.6748800710299313055 ) ) ;
#29911=CARTESIAN_POINT ( 'NONE',  ( 0.3545247821006056732, -1.838528400036530064, -0.5140887209270352809 ) ) ;
#29935=CARTESIAN_POINT ( 'NONE',  ( 0.1909286924077255587, -1.257064795538239022, -0.6485234391946320676 ) ) ;
#29936=CARTESIAN_POINT ( 'NONE',  ( 0.3944112475498172676, -1.768123242797767558, -0.4830133339744027698 ) ) ;
#29941=CARTESIAN_POINT ( 'NONE',  ( 0.1684145848869400830, -1.308153301062764395, -0.3047563416178276641 ) ) ;
#29942=CARTESIAN_POINT ( 'NONE',  ( 0.5391011117901446381, -1.666771999651815106, -0.5698732322495047020 ) ) ;
#29951=AXIS2_PLACEMENT_3D ( 'NONE', #36311, #8132, #38783 ) ;
#29952=CIRCLE ( 'NONE', #28662, 0.2500000000000000000 ) ;
#29959=CARTESIAN_POINT ( 'NONE',  ( 0.1968260301802208789, -2.003704694174034628, -0.2869878483811844072 ) ) ;
#29963=CARTESIAN_POINT ( 'NONE',  ( 0.3565880379454448579, -1.898203685287057629, -0.4912697616745712592 ) ) ;
#29973=CARTESIAN_POINT ( 'NONE',  ( 0.2469141422421070875, -1.581573626495411444, -0.3511777555542848206 ) ) ;
#29982=CARTESIAN_POINT ( 'NONE',  ( 0.3955374044963104740, -1.750921016457922086, -0.4909020773731604392 ) ) ;
#29989=CARTESIAN_POINT ( 'NONE',  ( 0.6201936192677818260, -1.619527673991476124, -0.4829864890893342255 ) ) ;
#29992=CARTESIAN_POINT ( 'NONE',  ( 0.3975363061031572665, -1.737107943197741866, -0.4349671603868599523 ) ) ;
#29995=CARTESIAN_POINT ( 'NONE',  ( 0.5934855389617087473, -1.553883175902015967, -0.4613003755920050408 ) ) ;
#29996=CARTESIAN_POINT ( 'NONE',  ( 0.2923286432308245808, -1.660243258845594649, -0.3370932271639339728 ) ) ;
#30002=EDGE_LOOP ( 'NONE', ( #22128, #25986 ) ) ;
#30007=ORIENTED_EDGE ( 'NONE', *, *, #3504, .T. ) ;
#30009=CIRCLE ( 'NONE', #16217, 0.2000000000000000111 ) ;
#30011=CARTESIAN_POINT ( 'NONE',  ( -1.974223891136790438E-05, -2.025566271751752634, -0.3135830156841454830 ) ) ;
#30013=CARTESIAN_POINT ( 'NONE',  ( 0.4671438810788549056, -1.683830466669562709, -0.4131679330247047255 ) ) ;
#30026=CARTESIAN_POINT ( 'NONE',  ( 0.03272157658042155332, -1.558775077797650566, -0.6419537545420734848 ) ) ;
#30030=CARTESIAN_POINT ( 'NONE',  ( 0.5423560421123170272, -1.654562585178021017, -0.5568277168365926011 ) ) ;
#30039=TOROIDAL_SURFACE ( 'NONE', #24790, 0.1333070866141734256, 0.02999999999999999889 ) ;
#30041=CARTESIAN_POINT ( 'NONE',  ( 0.5697138663266668734, -1.615732236462104954, -0.5166151207188711680 ) ) ;
#30043=CARTESIAN_POINT ( 'NONE',  ( -2.112273405726188513E-14, -2.183180860297921466, -0.4937760292030871079 ) ) ;
#30063=CARTESIAN_POINT ( 'NONE',  ( 0.6470677971351853630, -1.605717245651640646, -0.4588775069418976060 ) ) ;
#30064=EDGE_CURVE ( 'NONE', #15269, #19021, #31743, .T. ) ;
#30065=CARTESIAN_POINT ( 'NONE',  ( 0.1959288602264626367, -1.265726376210169812, -0.7137151691975773815 ) ) ;
#30068=ADVANCED_FACE ( 'NONE', ( #14923 ), #23568, .F. ) ;
#30079=CARTESIAN_POINT ( 'NONE',  ( 0.3487130776261192500, -1.632007555459813464, -0.6569214161271612618 ) ) ;
#30084=CARTESIAN_POINT ( 'NONE',  ( 0.3479607464745829715, -1.628127890686773327, -0.4301448196738368313 ) ) ;
#30102=ORIENTED_EDGE ( 'NONE', *, *, #16494, .F. ) ;
#30103=CARTESIAN_POINT ( 'NONE',  ( 0.04759610422507894872, -1.631270183090236747, -0.6680909377639540070 ) ) ;
#30105=ORIENTED_EDGE ( 'NONE', *, *, #11200, .F. ) ;
#30111=DIRECTION ( 'NONE',  ( -0.4999551463232377313, 0.8660512985181132439, 0.000000000000000000 ) ) ;
#30118=ORIENTED_EDGE ( 'NONE', *, *, #25522, .F. ) ;
#30120=ORIENTED_EDGE ( 'NONE', *, *, #4704, .T. ) ;
#30130=B_SPLINE_CURVE_WITH_KNOTS ( 'NONE', 3,
 ( #35145, #13122, #16620, #12941 ),
 .UNSPECIFIED., .F., .F.,
 ( 4, 4 ),
 ( 0.000000000000000000, 0.0003267947208782309579 ),
 .UNSPECIFIED. ) ;
#30131=CARTESIAN_POINT ( 'NONE',  ( 0.1726287778302593445, -1.825200482553405612, -0.6823101748829619728 ) ) ;
#30137=ORIENTED_EDGE ( 'NONE', *, *, #32187, .F. ) ;
#30138=LINE ( 'NONE', #26665, #27412 ) ;
#30154=DIRECTION ( 'NONE',  ( 0.000000000000000000, 0.000000000000000000, -1.000000000000000000 ) ) ;
#30163=CARTESIAN_POINT ( 'NONE',  ( 0.4542621314170603442, -1.107174261221695266, -0.6608907272175488234 ) ) ;
#30178=CARTESIAN_POINT ( 'NONE',  ( 0.3769271849960352250, -1.703883853206813459, -0.6148311252412128614 ) ) ;
#30180=CARTESIAN_POINT ( 'NONE',  ( 0.6499855218573453719, -1.553698270513451440, -0.6113109915954698659 ) ) ;
#30181=CARTESIAN_POINT ( 'NONE',  ( 0.03999249430411287026, -1.701782669491467948, -0.6675301993621318708 ) ) ;
#30182=CARTESIAN_POINT ( 'NONE',  ( 0.02999923007304734768, -2.091069160207820410, -0.2612343372939072705 ) ) ;
#30186=CARTESIAN_POINT ( 'NONE',  ( 0.5803799243415090903, -1.524048604864560286, -0.4565139846630590359 ) ) ;
#30196=ORIENTED_EDGE ( 'NONE', *, *, #644, .T. ) ;
#30199=CARTESIAN_POINT ( 'NONE',  ( 0.6984663268742642428, -1.558725849730709934, -0.5155029497116575543 ) ) ;
#30208=CARTESIAN_POINT ( 'NONE',  ( 0.1548063152929342046, -1.283648478974594109, -0.6986461007580347937 ) ) ;
#30209=CARTESIAN_POINT ( 'NONE',  ( 0.3699999728189415915, -2.086898135891332995, -0.5178658011735879363 ) ) ;
#30211=CARTESIAN_POINT ( 'NONE',  ( 0.1551413863202326104, -1.283415300285971172, -0.3361184124323285949 ) ) ;
#30222=DIRECTION ( 'NONE',  ( 0.8660512985181134660, 0.4999551463232371762, 0.000000000000000000 ) ) ;
#30232=CARTESIAN_POINT ( 'NONE',  ( 0.4203826191881493979, -1.700944664958275343, -0.4172566670736510552 ) ) ;
#30234=ORIENTED_EDGE ( 'NONE', *, *, #11903, .F. ) ;
#30237=VERTEX_POINT ( 'NONE', #38951 ) ;
#30256=AXIS2_PLACEMENT_3D ( 'NONE', #9136, #21702, #34236 ) ;
#30265=CARTESIAN_POINT ( 'NONE',  ( 0.3824787400963481354, -1.656932509623952665, -0.4003585709420097727 ) ) ;
#30267=CARTESIAN_POINT ( 'NONE',  ( 0.6189546704162820490, -1.608979253401461085, -0.5612101079336522247 ) ) ;
#30276=CARTESIAN_POINT ( 'NONE',  ( 0.4065986444723444504, -1.612206791548977058, -0.6687116998706487125 ) ) ;
#30281=CARTESIAN_POINT ( 'NONE',  ( 0.3566825243712435922, -1.732690581760574444, -0.5248316541739916907 ) ) ;
#30287=ORIENTED_EDGE ( 'NONE', *, *, #26399, .T. ) ;
#30288=CARTESIAN_POINT ( 'NONE',  ( 0.1999999999999789724, -2.183180860297921466, -0.5437760292030870968 ) ) ;
#30292=ORIENTED_EDGE ( 'NONE', *, *, #13691, .F. ) ;
#30293=CARTESIAN_POINT ( 'NONE',  ( 0.03715482636514332027, -1.738411246770970919, -0.6683936992048589154 ) ) ;
#30296=CARTESIAN_POINT ( 'NONE',  ( 0.3672875303838357142, -1.616970901354836565, -0.6123576500872176531 ) ) ;
#30298=CIRCLE ( 'NONE', #17146, 0.1875727115490686270 ) ;
#30317=CARTESIAN_POINT ( 'NONE',  ( 0.4092580784887682732, -1.709679816849471568, -0.6081479518787427097 ) ) ;
#30321=CARTESIAN_POINT ( 'NONE',  ( 0.1834057154632523778, -1.261407668813178340, -0.7100906059019311822 ) ) ;
#30328=DIRECTION ( 'NONE',  ( 1.000000000000000000, 0.000000000000000000, 0.000000000000000000 ) ) ;
#30332=CARTESIAN_POINT ( 'NONE',  ( 0.1953783392200664493, -2.012295829061851560, -0.6743165020656848307 ) ) ;
#30349=CARTESIAN_POINT ( 'NONE',  ( 0.1957919492576059572, -1.993943356844413817, -0.2893518802698326065 ) ) ;
#30359=ORIENTED_EDGE ( 'NONE', *, *, #16955, .F. ) ;
#30370=CIRCLE ( 'NONE', #23806, 0.1333070866141733701 ) ;
#30371=CARTESIAN_POINT ( 'NONE',  ( 0.3980241511492424444, -2.025796087852232752, -0.2805662142407182036 ) ) ;
#30380=CARTESIAN_POINT ( 'NONE',  ( 0.3632319344357997637, -1.747369632465606282, -0.5982111343698881534 ) ) ;
#30384=CARTESIAN_POINT ( 'NONE',  ( 0.6316962058243321687, -1.601278944064980170, -0.5821188199280620257 ) ) ;
#30385=CARTESIAN_POINT ( 'NONE',  ( 0.1095580259237044773, -1.391696829487717002, -0.6974751144921543800 ) ) ;
#30388=CARTESIAN_POINT ( 'NONE',  ( 0.3695052819757340123, -1.758428263776099287, -0.4278193900811940176 ) ) ;
#30394=AXIS2_PLACEMENT_3D ( 'NONE', #25708, #10068, #848 ) ;
#30398=CARTESIAN_POINT ( 'NONE',  ( 0.4677435473941323751, -1.076338332495886840, -0.6121988916364614619 ) ) ;
#30409=CARTESIAN_POINT ( 'NONE',  ( 0.07892189845977243268, -1.399197548210990627, -0.3632275770745012622 ) ) ;
#30417=DIRECTION ( 'NONE',  ( -0.4999551463232372317, 0.8660512985181135770, -0.000000000000000000 ) ) ;
#30422=ORIENTED_EDGE ( 'NONE', *, *, #38081, .T. ) ;
#30428=CARTESIAN_POINT ( 'NONE',  ( 0.1195693017516585716, -1.324662432614883700, -0.3516852558313144916 ) ) ;
#30453=DIRECTION ( 'NONE',  ( 0.4999551463241143634, -0.8660512985176070933, 0.000000000000000000 ) ) ;
#30457=CIRCLE ( 'NONE', #12078, 0.2200000000000000566 ) ;
#30458=VERTEX_POINT ( 'NONE', #30715 ) ;
#30460=ORIENTED_EDGE ( 'NONE', *, *, #26772, .F. ) ;
#30463=DIRECTION ( 'NONE',  ( -0.4999551463232373427, 0.8660512985181134660, -0.000000000000000000 ) ) ;
#30464=CARTESIAN_POINT ( 'NONE',  ( 0.5150521149620285177, -1.603685588959441466, -0.4158162930565508786 ) ) ;
#30467=EDGE_CURVE ( 'NONE', #26971, #1802, #24553, .T. ) ;
#30472=DIRECTION ( 'NONE',  ( 0.8660512985181134660, 0.4999551463232373427, 0.000000000000000000 ) ) ;
#30477=CARTESIAN_POINT ( 'NONE',  ( 0.4114935271034952380, -1.686083435099848593, -0.4173439381843787044 ) ) ;
#30479=CARTESIAN_POINT ( 'NONE',  ( 0.3377296246109549038, -1.643986942658042905, -0.6496138543457681269 ) ) ;
#30480=AXIS2_PLACEMENT_3D ( 'NONE', #16633, #38633, #23020 ) ;
#30494=CARTESIAN_POINT ( 'NONE',  ( 0.7824441210996690987, -1.527567036798914035, -0.5155029497116575543 ) ) ;
#30500=CARTESIAN_POINT ( 'NONE',  ( 0.3731358418028291601, -1.763283501847145773, -0.4358462980061182379 ) ) ;
#30502=ORIENTED_EDGE ( 'NONE', *, *, #26303, .T. ) ;
#30517=EDGE_CURVE ( 'NONE', #13700, #23240, #31821, .T. ) ;
#30531=CARTESIAN_POINT ( 'NONE',  ( 0.3699999999999786793, -2.097675824466503691, -0.5199442546161117118 ) ) ;
#30536=CARTESIAN_POINT ( 'NONE',  ( 0.3882739051659384599, -1.904129335431319570, -0.4886894917023981155 ) ) ;
#30542=CARTESIAN_POINT ( 'NONE',  ( 0.4795819664771984736, -1.106247336020415917, -0.4111404562665418871 ) ) ;
#30552=FACE_OUTER_BOUND ( 'NONE', #3888, .T. ) ;
#30553=DIRECTION ( 'NONE',  ( 0.000000000000000000, 0.000000000000000000, 1.000000000000000000 ) ) ;
#30555=VERTEX_POINT ( 'NONE', #6817 ) ;
#30559=CARTESIAN_POINT ( 'NONE',  ( 0.3593227136315140791, -1.801274561898448034, -0.3441312665133884896 ) ) ;
#30563=CARTESIAN_POINT ( 'NONE',  ( 0.1757500541653520820, -1.230771478115229245, -0.2869361388274796476 ) ) ;
#30570=DIRECTION ( 'NONE',  ( 0.000000000000000000, 0.000000000000000000, -1.000000000000000000 ) ) ;
#30572=CARTESIAN_POINT ( 'NONE',  ( 0.3334317865496208011, -1.653093244063527090, -0.6440291702909269889 ) ) ;
#30579=CARTESIAN_POINT ( 'NONE',  ( 0.3999999999999789280, -2.097675824466503691, -0.4688691127277795356 ) ) ;
#30587=CARTESIAN_POINT ( 'NONE',  ( 0.6367588599008480177, -1.388265895610014233, -0.6250000000000000000 ) ) ;
#30593=CARTESIAN_POINT ( 'NONE',  ( 0.6050862293119524393, -1.568338382688775567, -0.6158250207463809023 ) ) ;
#30594=AXIS2_PLACEMENT_3D ( 'NONE', #38619, #22610, #13118 ) ;
#30595=CARTESIAN_POINT ( 'NONE',  ( 0.4170115945640069932, -1.702980413955156758, -0.6123808887097255127 ) ) ;
#30604=CARTESIAN_POINT ( 'NONE',  ( 0.3657447301641588155, -2.011766955852946293, -0.4876776895119456778 ) ) ;
#30605=AXIS2_PLACEMENT_3D ( 'NONE', #17025, #442, #13540 ) ;
#30630=ORIENTED_EDGE ( 'NONE', *, *, #644, .F. ) ;
#30631=CARTESIAN_POINT ( 'NONE',  ( 0.1571433491268638127, -1.636854382521477413, -0.3650005568011028823 ) ) ;
#30635=CARTESIAN_POINT ( 'NONE',  ( -1.970642109407529655E-05, -2.025638281578344024, -0.3136921261701958730 ) ) ;
#30637=B_SPLINE_CURVE_WITH_KNOTS ( 'NONE', 3,
 ( #6826, #13208, #31942, #25779, #3762, #21884, #16315, #10129, #35236, #7037, #37484, #19606, #3942, #16503 ),
 .UNSPECIFIED., .F., .F.,
 ( 4, 2, 2, 2, 2, 2, 4 ),
 ( 0.000000000000000000, 0.0004381064775536402511, 0.0008762129551072805021, 0.001752425910214561004, 0.002190532387768201472, 0.002628638865321841506, 0.003504851820429122009 ),
 .UNSPECIFIED. ) ;
#30648=ADVANCED_FACE ( 'NONE', ( #305 ), #27750, .T. ) ;
#30656=CARTESIAN_POINT ( 'NONE',  ( 0.4038347882558627200, -1.728811102478955419, -0.5994564538103192008 ) ) ;
#30667=ORIENTED_EDGE ( 'NONE', *, *, #32769, .T. ) ;
#30676=CARTESIAN_POINT ( 'NONE',  ( 0.5922249234364754811, -1.371803823430798541, -0.6250000000000000000 ) ) ;
#30681=CARTESIAN_POINT ( 'NONE',  ( 0.4183584374824474428, -1.737746862795950697, -0.4437617475756700514 ) ) ;
#30688=CARTESIAN_POINT ( 'NONE',  ( 0.3999835757944618098, -1.598096088517039437, -0.3114834528418581883 ) ) ;
#30690=CARTESIAN_POINT ( 'NONE',  ( 0.3419910132069426956, -1.631574105539462360, -0.5957206493232616307 ) ) ;
#30694=CARTESIAN_POINT ( 'NONE',  ( 0.3841588946375145142, -1.652860766595878772, -0.3962426122320574229 ) ) ;
#30703=CARTESIAN_POINT ( 'NONE',  ( 0.3453005398490904820, -1.702161746735940895, -0.4206499346865002487 ) ) ;
#30709=VERTEX_POINT ( 'NONE', #10728 ) ;
#30715=CARTESIAN_POINT ( 'NONE',  ( 0.2704658693197408703, -1.170736166911837683, -0.5155029497116575543 ) ) ;
#30726=VERTEX_POINT ( 'NONE', #7639 ) ;
#30731=CARTESIAN_POINT ( 'NONE',  ( 0.3690018924180193394, -2.059894194155437397, -0.5029151679812257081 ) ) ;
#30733=CARTESIAN_POINT ( 'NONE',  ( 0.2923286432308245808, -1.660243258845594649, -0.6250000000000000000 ) ) ;
#30739=CARTESIAN_POINT ( 'NONE',  ( 0.3546447787406709629, -1.846711228588695075, -0.5131486097874190522 ) ) ;
#30740=CARTESIAN_POINT ( 'NONE',  ( 0.3699999999999784572, -2.087572556818563907, -0.5179767974037823297 ) ) ;
#30747=LINE ( 'NONE', #8523, #17352 ) ;
#30753=VERTEX_POINT ( 'NONE', #14008 ) ;
#30757=CARTESIAN_POINT ( 'NONE',  ( 0.3690052979743954076, -2.042003302564155298, -0.3074372596445509864 ) ) ;
#30761=ORIENTED_EDGE ( 'NONE', *, *, #35859, .F. ) ;
#30765=CARTESIAN_POINT ( 'NONE',  ( 0.1424029337235096226, -1.400533250147911746, -0.6250000000000000000 ) ) ;
#30768=CARTESIAN_POINT ( 'NONE',  ( 0.3433846349558144495, -1.636536893579917162, -0.6541055532972044340 ) ) ;
#30771=CARTESIAN_POINT ( 'NONE',  ( 0.7059656540691131577, -1.571716619208481935, -0.5155029497116575543 ) ) ;
#30774=CARTESIAN_POINT ( 'NONE',  ( 0.4634712904840415093, -1.711704060178988129, -0.5155029497116575543 ) ) ;
#30775=CARTESIAN_POINT ( 'NONE',  ( 0.3939041149941049924, -1.772452426391821989, -0.3123449749659221730 ) ) ;
#30788=CARTESIAN_POINT ( 'NONE',  ( 0.6412004512100059062, -1.451677482400071773, -0.3985001959979381780 ) ) ;
#30789=CARTESIAN_POINT ( 'NONE',  ( 0.02996954754363531648, -2.053999617283090995, -0.7135042156891373555 ) ) ;
#30797=CARTESIAN_POINT ( 'NONE',  ( 0.4150350604501116814, -1.704167521295949284, -0.6115272160904526855 ) ) ;
#30801=ADVANCED_FACE ( 'NONE', ( #39118 ), #39931, .T. ) ;
#30803=CARTESIAN_POINT ( 'NONE',  ( 0.5008138289901331586, -1.674651764118539443, -0.6059811472733124260 ) ) ;
#30812=SHAPE_DEFINITION_REPRESENTATION ( #22937, #8026 ) ;
#30822=ORIENTED_EDGE ( 'NONE', *, *, #21576, .F. ) ;
#30827=CARTESIAN_POINT ( 'NONE',  ( 0.4311422992558763267, -1.610538320350847208, -0.3671492683199031881 ) ) ;
#30829=CARTESIAN_POINT ( 'NONE',  ( 0.5913314978914147035, -1.514214781277106736, -0.3979390557995906019 ) ) ;
#30845=CARTESIAN_POINT ( 'NONE',  ( 0.1843722651776505406, -1.260849697819215631, -0.2901536752075735692 ) ) ;
#30858=ORIENTED_EDGE ( 'NONE', *, *, #26256, .F. ) ;
#30864=EDGE_CURVE ( 'NONE', #5281, #27329, #27316, .T. ) ;
#30867=B_SPLINE_CURVE_WITH_KNOTS ( 'NONE', 3,
 ( #26317, #30013, #32685, #29406, #20765, #20553 ),
 .UNSPECIFIED., .F., .F.,
 ( 4, 2, 4 ),
 ( 0.000000000000000000, 0.0007708994731598440078, 0.001541798946319688016 ),
 .UNSPECIFIED. ) ;
#30875=( BOUNDED_SURFACE ( )  B_SPLINE_SURFACE ( 3, 2, ( 
 ( #6951, #633, #38625 ),
 ( #28957, #26495, #32659 ),
 ( #39030, #821, #26114 ),
 ( #16839, #13332, #32237 ),
 ( #4057, #4464, #16624 ),
 ( #25905, #38423, #29571 ),
 ( #22407, #29171, #1034 ),
 ( #23010, #13544, #35531 ),
 ( #7333, #19911, #32448 ),
 ( #1225, #39241, #30180 ),
 ( #23436, #5472, #2215 ),
 ( #30593, #2417, #14954 ),
 ( #27508, #10862, #14536 ),
 ( #17224, #39432, #14755 ),
 ( #36748, #8559, #18037 ),
 ( #7949, #23824, #30384 ),
 ( #26901, #21131, #20523 ),
 ( #17825, #33057, #36346 ),
 ( #4865, #26711, #8163 ),
 ( #35952, #29776, #11254 ),
 ( #7759, #27100, #24224 ),
 ( #20740, #33264, #11469 ),
 ( #27317, #5073, #17633 ),
 ( #2010, #39634, #33659 ),
 ( #24033, #17433, #4652 ),
 ( #14139, #1617, #20326 ),
 ( #11063, #36562, #39846 ),
 ( #8367, #32848, #23623 ),
 ( #20936, #33458, #36139 ),
 ( #5265, #11668, #29989 ),
 ( #1822, #14338, #25019 ),
 ( #33887, #9171, #31405 ),
 ( #21736, #27705, #11857 ),
 ( #172, #19056, #15752 ),
 ( #27916, #15570, #12661 ),
 ( #6486, #3409, #3025 ),
 ( #31594, #8772, #40238 ),
 ( #40455, #24422, #34681 ),
 ( #9589, #34270, #37769 ),
 ( #5689, #15965, #25226 ),
 ( #18243, #3208, #37550 ),
 ( #12074, #22168, #40032 ),
 ( #36954, #37168, #12280 ),
 ( #18434, #15358, #21349 ),
 ( #24837, #6293, #8984 ),
 ( #18647, #21552, #15145 ),
 ( #30788, #2609, #24637 ),
 ( #34071, #5872, #28117 ) ),
 .UNSPECIFIED., .F., .F., .T. ) 
 B_SPLINE_SURFACE_WITH_KNOTS ( ( 4, 2, 2, 2, 2, 2, 2, 2, 2, 2, 2, 2, 2, 2, 2, 2, 2, 2, 2, 2, 2, 2, 2, 4 ),
 ( 3, 3 ),
 ( 0.003261766200971520820, 0.004250769295497201089, 0.005239772390022882226, 0.006228775484548562495, 0.007217778579074242765, 0.008206781673599922167, 0.008701283220862762735, 0.009195784768125603303, 0.009690286315388443872, 0.01018478786265128444, 0.01067928940991412501, 0.01117379095717696384, 0.01166829250443980268, 0.01216279405170264324, 0.01265729559896548381, 0.01315179714622832438, 0.01364629869349116495, 0.01414080024075400552, 0.01463530178801684609, 0.01512980333527968665, 0.01611880642980536432, 0.01710780952433104546, 0.01809681261885672660, 0.01908581571338240773 ),
 ( 0.000000000000000000, 1.000000000000000000 ),
 .UNSPECIFIED. ) 
 GEOMETRIC_REPRESENTATION_ITEM ( )  RATIONAL_B_SPLINE_SURFACE ( (
 ( 1.000000000000000000, 0.9336557140612112837, 1.000000000000000000),
 ( 1.000000000000000000, 0.9269669748511076834, 1.000000000000000000),
 ( 1.000000000000000000, 0.9185057473876691025, 1.000000000000000000),
 ( 1.000000000000000000, 0.8983811411394780899, 1.000000000000000000),
 ( 1.000000000000000000, 0.8868705803443834856, 1.000000000000000000),
 ( 1.000000000000000000, 0.8615685732449787082, 1.000000000000000000),
 ( 1.000000000000000000, 0.8476166942854144182, 1.000000000000000000),
 ( 1.000000000000000000, 0.8180751618708101969, 1.000000000000000000),
 ( 1.000000000000000000, 0.8026452689216959646, 1.000000000000000000),
 ( 1.000000000000000000, 0.7711474197545707954, 1.000000000000000000),
 ( 1.000000000000000000, 0.7550167180304484527, 1.000000000000000000),
 ( 1.000000000000000000, 0.7326795836945654283, 1.000000000000000000),
 ( 1.000000000000000000, 0.7254988216173606785, 1.000000000000000000),
 ( 1.000000000000000000, 0.7120213782890315590, 1.000000000000000000),
 ( 1.000000000000000000, 0.7058095999174238688, 1.000000000000000000),
 ( 1.000000000000000000, 0.6951287496146589806, 1.000000000000000000),
 ( 1.000000000000000000, 0.6906111284772815662, 1.000000000000000000),
 ( 1.000000000000000000, 0.6837693063777301461, 1.000000000000000000),
 ( 1.000000000000000000, 0.6814518707835520717, 1.000000000000000000),
 ( 1.000000000000000000, 0.6797285044136155419, 1.000000000000000000),
 ( 1.000000000000000000, 0.6803227108142706481, 1.000000000000000000),
 ( 1.000000000000000000, 0.6840260012167642678, 1.000000000000000000),
 ( 1.000000000000000000, 0.6872325378123951278, 1.000000000000000000),
 ( 1.000000000000000000, 0.6934257698760888378, 1.000000000000000000),
 ( 1.000000000000000000, 0.6961673821949488916, 1.000000000000000000),
 ( 1.000000000000000000, 0.6971230725348070978, 1.000000000000000000),
 ( 1.000000000000000000, 0.6952258568012568141, 1.000000000000000000),
 ( 1.000000000000000000, 0.6895613480052964483, 1.000000000000000000),
 ( 1.000000000000000000, 0.6860771389999574810, 1.000000000000000000),
 ( 1.000000000000000000, 0.6813042296466748082, 1.000000000000000000),
 ( 1.000000000000000000, 0.6800080602364667604, 1.000000000000000000),
 ( 1.000000000000000000, 0.6804313476833027119, 1.000000000000000000),
 ( 1.000000000000000000, 0.6820608860769757920, 1.000000000000000000),
 ( 1.000000000000000000, 0.6877885785809060293, 1.000000000000000000),
 ( 1.000000000000000000, 0.6919289788393708784, 1.000000000000000000),
 ( 1.000000000000000000, 0.7019562628004784033, 1.000000000000000000),
 ( 1.000000000000000000, 0.7078144704192228520, 1.000000000000000000),
 ( 1.000000000000000000, 0.7207186550667057379, 1.000000000000000000),
 ( 1.000000000000000000, 0.7278201325373979680, 1.000000000000000000),
 ( 1.000000000000000000, 0.7499733481817499881, 1.000000000000000000),
 ( 1.000000000000000000, 0.7658307437853975053, 1.000000000000000000),
 ( 1.000000000000000000, 0.7976817372220619262, 1.000000000000000000),
 ( 1.000000000000000000, 0.8132405326115809130, 1.000000000000000000),
 ( 1.000000000000000000, 0.8429607034202760696, 1.000000000000000000),
 ( 1.000000000000000000, 0.8572315153285383627, 1.000000000000000000),
 ( 1.000000000000000000, 0.8831414977311506931, 1.000000000000000000),
 ( 1.000000000000000000, 0.8948694253068246729, 1.000000000000000000),
 ( 1.000000000000000000, 0.9052370393127044945, 1.000000000000000000) ) ) 
 REPRESENTATION_ITEM ( '' )  SURFACE ( )  );
#30884=DIRECTION ( 'NONE',  ( -0.4999551463232373427, 0.8660512985181134660, -0.000000000000000000 ) ) ;
#30897=VERTEX_POINT ( 'NONE', #2892 ) ;
#30902=ORIENTED_EDGE ( 'NONE', *, *, #14586, .T. ) ;
#30925=( NAMED_UNIT ( * ) SI_UNIT ( $, .STERADIAN. ) SOLID_ANGLE_UNIT ( ) );
#30926=FACE_BOUND ( 'NONE', #28538, .T. ) ;
#30933=B_SPLINE_CURVE_WITH_KNOTS ( 'NONE', 3,
 ( #28316, #12682, #25241, #9604, #34693, #6500, #37988, #19070, #31609, #15983 ),
 .UNSPECIFIED., .F., .F.,
 ( 4, 2, 2, 2, 4 ),
 ( 9.033896246548822940E-17, 0.0004326218239507741495, 0.0008652436479014579849, 0.001297865471852141820, 0.001730487295802825764 ),
 .UNSPECIFIED. ) ;
#30940=CARTESIAN_POINT ( 'NONE',  ( -2.112273405726188513E-14, -2.183180860297921466, -0.7137760292030871367 ) ) ;
#30941=AXIS2_PLACEMENT_3D ( 'NONE', #4982, #23126, #27005 ) ;
#30944=CARTESIAN_POINT ( 'NONE',  ( -2.112273405726188513E-14, -2.101103246702401339, -0.2895067904002890935 ) ) ;
#30951=ORIENTED_EDGE ( 'NONE', *, *, #26772, .T. ) ;
#30954=CARTESIAN_POINT ( 'NONE',  ( 0.3728899637934937061, -1.734176460878569914, -0.3423889237934055751 ) ) ;
#30955=CARTESIAN_POINT ( 'NONE',  ( 0.3757471142192211344, -1.766731021160330428, -0.5680748514784754732 ) ) ;
#30957=CARTESIAN_POINT ( 'NONE',  ( 0.2211959769661342168, -1.309495541150525799, -0.4400554600884077350 ) ) ;
#30958=DIRECTION ( 'NONE',  ( 0.000000000000000000, 0.3420201433256721546, 0.9396926207859072067 ) ) ;
#30974=FACE_OUTER_BOUND ( 'NONE', #15787, .T. ) ;
#30987=CARTESIAN_POINT ( 'NONE',  ( 0.1813906338116575978, -1.297206181306920891, -0.7344059994437892591 ) ) ;
#30993=CARTESIAN_POINT ( 'NONE',  ( 0.3591498995103403202, -1.737620376665804267, -0.5147966178037288731 ) ) ;
#30994=CARTESIAN_POINT ( 'NONE',  ( 0.4184753273149498520, -1.633759443312357229, -0.5155029497116575543 ) ) ;
#30996=AXIS2_PLACEMENT_3D ( 'NONE', #19946, #38851, #28804 ) ;
#30997=CARTESIAN_POINT ( 'NONE',  ( 0.4721942231302793669, -1.661553490448594683, -0.6136790096869800815 ) ) ;
#30999=CARTESIAN_POINT ( 'NONE',  ( 0.5299567604580853741, -1.673323247257030522, -0.5639626154586274698 ) ) ;
#31000=VECTOR ( 'NONE', #20770, 39.37007874015748143 ) ;
#31009=CARTESIAN_POINT ( 'NONE',  ( 0.5048660853949354932, -1.606428814459148979, -0.6256849655409983946 ) ) ;
#31018=CARTESIAN_POINT ( 'NONE',  ( 0.6409058204046232943, -1.459016202299332710, -0.5155029497116575543 ) ) ;
#31029=B_SPLINE_CURVE_WITH_KNOTS ( 'NONE', 3,
 ( #30656, #14815, #37418, #2476, #15013, #24283, #25085, #15421, #27379, #40089 ),
 .UNSPECIFIED., .F., .F.,
 ( 4, 2, 2, 2, 4 ),
 ( 1.412501740721826955E-14, 0.0003711039185504978310, 0.0007422078370868705676, 0.001113311755623243304, 0.001484415674159616149 ),
 .UNSPECIFIED. ) ;
#31030=CARTESIAN_POINT ( 'NONE',  ( 0.01053425445852829503, -1.728867745475969109, -0.3673112671014556185 ) ) ;
#31031=ADVANCED_FACE ( 'NONE', ( #37034 ), #21824, .T. ) ;
#31036=CARTESIAN_POINT ( 'NONE',  ( 0.3999999999999787059, -2.097675824466503691, -0.5196396315034578217 ) ) ;
#31041=CARTESIAN_POINT ( 'NONE',  ( 0.007443814426054808607, -1.701641051468849364, -0.6331095842549401276 ) ) ;
#31052=CARTESIAN_POINT ( 'NONE',  ( 0.2027840892200388767, -1.637248379545634958, -0.6903293078929895188 ) ) ;
#31057=VERTEX_POINT ( 'NONE', #25939 ) ;
#31066=AXIS2_PLACEMENT_3D ( 'NONE', #5123, #4712, #35800 ) ;
#31071=CARTESIAN_POINT ( 'NONE',  ( 0.4182170724685722041, -1.587570233393474251, -0.3841720924506121793 ) ) ;
#31073=TOROIDAL_SURFACE ( 'NONE', #25115, 0.05330708661417342398, 0.01000000000000000021 ) ;
#31076=ORIENTED_EDGE ( 'NONE', *, *, #15062, .F. ) ;
#31077=CARTESIAN_POINT ( 'NONE',  ( 0.3863936565759469866, -1.896679156257589538, -0.4880250169076069677 ) ) ;
#31078=CARTESIAN_POINT ( 'NONE',  ( 0.02999999999997886302, -2.183180860297921466, -0.7137760292030871367 ) ) ;
#31082=CIRCLE ( 'NONE', #11365, 0.1700000000000001232 ) ;
#31085=EDGE_CURVE ( 'NONE', #22416, #13200, #6138, .T. ) ;
#31092=CARTESIAN_POINT ( 'NONE',  ( 0.1999999999999789724, -2.097675824466503691, -0.5196396315034578217 ) ) ;
#31103=CARTESIAN_POINT ( 'NONE',  ( 0.3179616082204479444, -1.253011040271057697, -0.5155029497116575543 ) ) ;
#31104=CARTESIAN_POINT ( 'NONE',  ( 0.3289444927862943957, -1.212030846925817196, -0.5155029497116575543 ) ) ;
#31106=B_SPLINE_CURVE_WITH_KNOTS ( 'NONE', 3,
 ( #33708, #6336, #9030, #25276, #2650, #34314, #12322, #23, #40283, #34114 ),
 .UNSPECIFIED., .F., .F.,
 ( 4, 2, 2, 2, 4 ),
 ( 1.734723475976807094E-18, 0.0003557584921360815795, 0.0007115169842721614244, 0.001067275476408241323, 0.001423033968544321114 ),
 .UNSPECIFIED. ) ;
#31122=( BOUNDED_SURFACE ( )  B_SPLINE_SURFACE ( 3, 2, ( 
 ( #27385, #17685, #30232 ),
 ( #2064, #13995, #14392 ),
 ( #11730, #14598, #27171 ),
 ( #24288, #4722, #11534 ),
 ( #39104, #36010, #11121 ),
 ( #29848, #1687, #23680 ) ),
 .UNSPECIFIED., .F., .F., .F. ) 
 B_SPLINE_SURFACE_WITH_KNOTS ( ( 4, 2, 4 ),
 ( 3, 3 ),
 ( -1.301042606982605321E-17, 0.0009782491413249925528, 0.001956498282649998116 ),
 ( 0.000000000000000000, 1.000000000000000000 ),
 .UNSPECIFIED. ) 
 GEOMETRIC_REPRESENTATION_ITEM ( )  RATIONAL_B_SPLINE_SURFACE ( (
 ( 1.000000000000000000, 0.8660688067376841603, 1.000000000000000000),
 ( 1.000000000000000000, 0.8670375503518229499, 1.000000000000000000),
 ( 1.000000000000000000, 0.8618718521359357565, 1.000000000000000000),
 ( 1.000000000000000000, 0.8415687179548819730, 1.000000000000000000),
 ( 1.000000000000000000, 0.8267810924324421329, 1.000000000000000000),
 ( 1.000000000000000000, 0.8102556146343646848, 1.000000000000000000) ) ) 
 REPRESENTATION_ITEM ( '' )  SURFACE ( )  );
#31123=CARTESIAN_POINT ( 'NONE',  ( 0.2914323826288400254, -1.233685883474753497, -0.5166151207188711680 ) ) ;
#31126=AXIS2_PLACEMENT_3D ( 'NONE', #34937, #10264, #13925 ) ;
#31135=DIRECTION ( 'NONE',  ( 1.000000000000000000, 0.000000000000000000, 0.000000000000000000 ) ) ;
#31142=DIRECTION ( 'NONE',  ( -0.4999551463232377313, 0.8660512985181132439, -0.000000000000000000 ) ) ;
#31148=CARTESIAN_POINT ( 'NONE',  ( 0.01384654206388801108, -1.688463842650887781, -0.6347859073314252587 ) ) ;
#31155=CARTESIAN_POINT ( 'NONE',  ( 0.1760056095156050660, -1.754827144506087455, -0.6511199371818791048 ) ) ;
#31166=EDGE_LOOP ( 'NONE', ( #25194, #39995, #8348, #31732 ) ) ;
#31170=ORIENTED_EDGE ( 'NONE', *, *, #15220, .F. ) ;
#31171=ORIENTED_EDGE ( 'NONE', *, *, #40640, .T. ) ;
#31174=CARTESIAN_POINT ( 'NONE',  ( 0.3699999999999789013, -2.097675824466503691, -0.4688691127277795356 ) ) ;
#31181=ORIENTED_EDGE ( 'NONE', *, *, #39949, .F. ) ;
#31187=CARTESIAN_POINT ( 'NONE',  ( 0.3699999999999784017, -2.054734391222358347, -0.6850094247584036511 ) ) ;
#31212=ORIENTED_EDGE ( 'NONE', *, *, #39193, .T. ) ;
#31214=CARTESIAN_POINT ( 'NONE',  ( 0.3891537709046165583, -1.706611523097125049, -0.5991981645855274374 ) ) ;
#31219=CARTESIAN_POINT ( 'NONE',  ( 0.4288946199586322061, -1.677151416097353520, -0.6187118249900269706 ) ) ;
#31221=B_SPLINE_CURVE_WITH_KNOTS ( 'NONE', 3,
 ( #3004, #3389, #25618, #22340, #3602, #9355, #15553, #28707 ),
 .UNSPECIFIED., .F., .F.,
 ( 4, 2, 2, 4 ),
 ( 0.000000000000000000, 0.0009535720482368597890, 0.001430358072355289792, 0.001907144096473719578 ),
 .UNSPECIFIED. ) ;
#31224=CARTESIAN_POINT ( 'NONE',  ( 0.4897592102757907795, -1.696528537887749932, -0.5984293649392188330 ) ) ;
#31237=EDGE_LOOP ( 'NONE', ( #2389, #17349, #37684, #12963, #16912, #30502, #803, #11316, #37633 ) ) ;
#31246=EDGE_LOOP ( 'NONE', ( #17420, #24550, #26961, #29585 ) ) ;
#31247=DIRECTION ( 'NONE',  ( 0.4999551463232373427, -0.8660512985181134660, 0.000000000000000000 ) ) ;
#31249=CARTESIAN_POINT ( 'NONE',  ( 0.5930815638500551712, -1.500577258630007904, -0.3915676963420799961 ) ) ;
#31251=CARTESIAN_POINT ( 'NONE',  ( 0.3238605203897769180, -1.709547670968458943, -0.3346915668799618770 ) ) ;
#31255=CARTESIAN_POINT ( 'NONE',  ( 0.1999999999999786671, -2.166079853131637201, -0.5407606602423821185 ) ) ;
#31256=ORIENTED_EDGE ( 'NONE', *, *, #40605, .T. ) ;
#31257=DIRECTION ( 'NONE',  ( 0.4999551463232377313, -0.8660512985181132439, -0.000000000000000000 ) ) ;
#31271=ORIENTED_EDGE ( 'NONE', *, *, #5215, .T. ) ;
#31273=ORIENTED_EDGE ( 'NONE', *, *, #24878, .T. ) ;
#31279=ORIENTED_EDGE ( 'NONE', *, *, #30864, .T. ) ;
#31282=ADVANCED_FACE ( 'NONE', ( #39410 ), #4837, .T. ) ;
#31287=DIRECTION ( 'NONE',  ( 0.4999551463232372317, -0.8660512985181135770, 0.000000000000000000 ) ) ;
#31290=CARTESIAN_POINT ( 'NONE',  ( -2.112273405726188513E-14, -2.097675824466503691, -0.2588528740066097233 ) ) ;
#31294=AXIS2_PLACEMENT_3D ( 'NONE', #7946, #24030, #20322 ) ;
#31295=DIRECTION ( 'NONE',  ( 0.000000000000000000, -1.000000000000000000, 0.000000000000000000 ) ) ;
#31304=CARTESIAN_POINT ( 'NONE',  ( 0.02999999999997891853, -2.097675824466501915, -0.2588528740066096678 ) ) ;
#31307=CIRCLE ( 'NONE', #40490, 0.03000000000000002318 ) ;
#31310=TOROIDAL_SURFACE ( 'NONE', #13569, 0.08830708661417342731, 0.01499999999999999944 ) ;
#31322=EDGE_LOOP ( 'NONE', ( #16042, #38293, #34749, #30460 ) ) ;
#31330=ORIENTED_EDGE ( 'NONE', *, *, #13209, .F. ) ;
#31331=EDGE_CURVE ( 'NONE', #34358, #3578, #3605, .T. ) ;
#31336=CARTESIAN_POINT ( 'NONE',  ( 0.3485300389640555441, -1.734513092226865449, -0.5719809208048397542 ) ) ;
#31346=EDGE_CURVE ( 'NONE', #16208, #15639, #9531, .T. ) ;
#31352=CARTESIAN_POINT ( 'NONE',  ( 0.5947987396514448077, -1.485632953921246946, -0.6449812926602518370 ) ) ;
#31362=ADVANCED_FACE ( 'NONE', ( #28098, #3386 ), #12865, .F. ) ;
#31363=( BOUNDED_SURFACE ( )  B_SPLINE_SURFACE ( 3, 2, ( 
 ( #22180, #37566, #18662 ),
 ( #37182, #12293, #15585 ),
 ( #28131, #3423, #18447 ),
 ( #30999, #21563, #25456 ),
 ( #34084, #2823, #15372 ),
 ( #27716, #28529, #18880 ),
 ( #27930, #6277, #24652 ),
 ( #18257, #40471, #30803 ),
 ( #2622, #9184, #8999 ),
 ( #31224, #37784, #24852 ) ),
 .UNSPECIFIED., .F., .F., .F. ) 
 B_SPLINE_SURFACE_WITH_KNOTS ( ( 4, 2, 2, 2, 4 ),
 ( 3, 3 ),
 ( 0.000000000000000000, 0.0005548957138909029006, 0.001109791427781805801, 0.001664687141672708702, 0.002219582855563611602 ),
 ( 0.000000000000000000, 1.000000000000000000 ),
 .UNSPECIFIED. ) 
 GEOMETRIC_REPRESENTATION_ITEM ( )  RATIONAL_B_SPLINE_SURFACE ( (
 ( 1.000000000000000000, 0.8164965809277185960, 1.000000000000000000),
 ( 1.000000000000000000, 0.8165294587845374208, 1.000000000000000000),
 ( 1.000000000000000000, 0.8155127232466478082, 1.000000000000000000),
 ( 1.000000000000000000, 0.8083607722978235488, 1.000000000000000000),
 ( 1.000000000000000000, 0.8021782943055887349, 1.000000000000000000),
 ( 1.000000000000000000, 0.7842736402517446193, 1.000000000000000000),
 ( 1.000000000000000000, 0.7723567727536417848, 1.000000000000000000),
 ( 1.000000000000000000, 0.7435640046126961167, 1.000000000000000000),
 ( 1.000000000000000000, 0.7266415285874683327, 1.000000000000000000),
 ( 1.000000000000000000, 0.7071067811843647632, 1.000000000000000000) ) ) 
 REPRESENTATION_ITEM ( '' )  SURFACE ( )  );
#31364=VERTEX_POINT ( 'NONE', #36934 ) ;
#31373=VERTEX_POINT ( 'NONE', #22147 ) ;
#31374=EDGE_LOOP ( 'NONE', ( #899, #28829, #2402 ) ) ;
#31375=DIRECTION ( 'NONE',  ( 0.4999551463232373427, -0.8660512985181134660, 0.000000000000000000 ) ) ;
#31378=CARTESIAN_POINT ( 'NONE',  ( 0.3697297642830735809, -2.079360693035569696, -0.4724975067213835755 ) ) ;
#31384=ORIENTED_EDGE ( 'NONE', *, *, #15580, .F. ) ;
#31388=CARTESIAN_POINT ( 'NONE',  ( 0.4894889402668303746, -1.607606434602806722, -0.3928725284401201612 ) ) ;
#31390=CARTESIAN_POINT ( 'NONE',  ( 0.4511668698691140289, -1.684167190675012415, -0.7187326247832955817 ) ) ;
#31393=DIRECTION ( 'NONE',  ( 0.4999551463232372317, -0.8660512985181134660, 0.000000000000000000 ) ) ;
#31405=CARTESIAN_POINT ( 'NONE',  ( 0.6239059973579713647, -1.614399174532030523, -0.4690470541687177808 ) ) ;
#31413=CARTESIAN_POINT ( 'NONE',  ( 0.3660745003390204477, -2.015859508080472207, -0.4732687194387362739 ) ) ;
#31416=FACE_OUTER_BOUND ( 'NONE', #21198, .T. ) ;
#31418=ORIENTED_EDGE ( 'NONE', *, *, #39910, .T. ) ;
#31424=CARTESIAN_POINT ( 'NONE',  ( 0.5144487370624802880, -1.604612665234552926, -0.6158392069828952931 ) ) ;
#31426=ORIENTED_EDGE ( 'NONE', *, *, #12176, .T. ) ;
#31430=ORIENTED_EDGE ( 'NONE', *, *, #34936, .T. ) ;
#31438=CYLINDRICAL_SURFACE ( 'NONE', #39207, 0.1033070866141734129 ) ;
#31440=ORIENTED_EDGE ( 'NONE', *, *, #24615, .F. ) ;
#31442=CARTESIAN_POINT ( 'NONE',  ( -0.004906298587631130297, -2.039712202718448442, -0.3118752401674445007 ) ) ;
#31444=CARTESIAN_POINT ( 'NONE',  ( 0.6630839938131345423, -1.446213159395746128, -0.6155857397476032222 ) ) ;
#31445=CARTESIAN_POINT ( 'NONE',  ( 0.2647196283856586563, -1.647466429234020646, -0.3433666575725142223 ) ) ;
#31446=CARTESIAN_POINT ( 'NONE',  ( 0.3335364369457424760, -1.652728420514769425, -0.6442615712401940087 ) ) ;
#31448=CARTESIAN_POINT ( 'NONE',  ( 0.4019696390288734489, -1.758754468419369221, -0.5306525527942117515 ) ) ;
#31450=DIRECTION ( 'NONE',  ( 0.5682870691672845531, 0.000000000000000000, -0.8228303634512146303 ) ) ;
#31462=ORIENTED_EDGE ( 'NONE', *, *, #38971, .T. ) ;
#31471=ORIENTED_EDGE ( 'NONE', *, *, #39294, .T. ) ;
#31479=DIRECTION ( 'NONE',  ( 1.000000000000000000, 0.000000000000000000, 0.000000000000000000 ) ) ;
#31480=EDGE_LOOP ( 'NONE', ( #27578, #7538, #32171, #34606, #3552, #29122, #15729 ) ) ;
#31481=ORIENTED_EDGE ( 'NONE', *, *, #791, .F. ) ;
#31482=CARTESIAN_POINT ( 'NONE',  ( 0.4688459138424371786, -1.061988423737608045, -0.4248180574663140141 ) ) ;
#31492=CARTESIAN_POINT ( 'NONE',  ( 0.3722391882570431632, -1.729214173715589720, -0.4195648250677492808 ) ) ;
#31515=CARTESIAN_POINT ( 'NONE',  ( 0.3409152363046567547, -1.516880185093696154, -0.5318766032426672785 ) ) ;
#31518=CARTESIAN_POINT ( 'NONE',  ( 0.4120574151838698462, -1.590911390411421156, -0.3441652514538682817 ) ) ;
#31521=DIRECTION ( 'NONE',  ( 0.000000000000000000, 0.000000000000000000, -1.000000000000000000 ) ) ;
#31525=B_SPLINE_CURVE_WITH_KNOTS ( 'NONE', 3,
 ( #10554, #7677, #23129, #20242, #38940, #1529 ),
 .UNSPECIFIED., .F., .F.,
 ( 4, 2, 4 ),
 ( 0.000000000000000000, 0.0006315621964318843306, 0.001263124392863768661 ),
 .UNSPECIFIED. ) ;
#31544=CARTESIAN_POINT ( 'NONE',  ( 0.2133635201206025567, -1.295927705172547739, -0.4087570219343043543 ) ) ;
#31548=EDGE_LOOP ( 'NONE', ( #10774, #37742, #33188, #18043 ) ) ;
#31556=CARTESIAN_POINT ( 'NONE',  ( 0.4178394282659816938, -1.669152271385904607, -0.5063121030242170306 ) ) ;
#31569=CARTESIAN_POINT ( 'NONE',  ( 0.4708300887478357732, -1.591450557125715148, -0.4363017091322234364 ) ) ;
#31574=DIRECTION ( 'NONE',  ( -0.4999551463232373427, 0.8660512985181134660, -0.000000000000000000 ) ) ;
#31582=ADVANCED_FACE ( 'NONE', ( #9303 ), #39575, .T. ) ;
#31592=CIRCLE ( 'NONE', #4005, 0.1700000000000000400 ) ;
#31594=CARTESIAN_POINT ( 'NONE',  ( 0.5958209082783288979, -1.583864344932945478, -0.4282463924674004274 ) ) ;
#31595=CARTESIAN_POINT ( 'NONE',  ( 0.3999999999999786504, -2.092100694519134052, -0.4698241118115154547 ) ) ;
#31599=ADVANCED_FACE ( 'NONE', ( #15499 ), #31958, .F. ) ;
#31600=ORIENTED_EDGE ( 'NONE', *, *, #10693, .T. ) ;
#31601=FACE_OUTER_BOUND ( 'NONE', #22439, .T. ) ;
#31602=CARTESIAN_POINT ( 'NONE',  ( 0.3909945020765858148, -1.648962484502373149, -0.3938746075551732839 ) ) ;
#31608=VERTEX_POINT ( 'NONE', #29258 ) ;
#31609=CARTESIAN_POINT ( 'NONE',  ( 0.4130089464348675188, -1.611935647216347300, -0.6680384904433120941 ) ) ;
#31628=CIRCLE ( 'NONE', #39428, 0.04330708661417322775 ) ;
#31637=CARTESIAN_POINT ( 'NONE',  ( 0.1115022060487694811, -1.514603223676135757, -0.3697424615991000696 ) ) ;
#31642=CARTESIAN_POINT ( 'NONE',  ( 0.1909286924077255032, -1.257064795538239022, -0.2869361388274795921 ) ) ;
#31647=CARTESIAN_POINT ( 'NONE',  ( 0.1589950187058424280, -2.107936428766274073, -0.7005084057759861649 ) ) ;
#31650=VECTOR ( 'NONE', #38250, 39.37007874015748143 ) ;
#31655=CIRCLE ( 'NONE', #13896, 0.1333070866141734534 ) ;
#31657=EDGE_CURVE ( 'NONE', #32089, #24957, #17447, .T. ) ;
#31666=EDGE_LOOP ( 'NONE', ( #37469, #1686, #26143 ) ) ;
#31671=ORIENTED_EDGE ( 'NONE', *, *, #37167, .T. ) ;
#31681=VERTEX_POINT ( 'NONE', #22289 ) ;
#31698=CARTESIAN_POINT ( 'NONE',  ( 0.3820855590050560857, -1.701428075840956344, -0.4116647734693053007 ) ) ;
#31707=AXIS2_PLACEMENT_3D ( 'NONE', #29568, #7757, #7330 ) ;
#31717=ORIENTED_EDGE ( 'NONE', *, *, #8977, .F. ) ;
#31718=B_SPLINE_CURVE_WITH_KNOTS ( 'NONE', 3,
 ( #35135, #19509, #7125, #38013, #15796, #214 ),
 .UNSPECIFIED., .F., .F.,
 ( 4, 2, 4 ),
 ( 0.000000000000000000, 0.0006045613306913027790, 0.001209122661382605558 ),
 .UNSPECIFIED. ) ;
#31724=CARTESIAN_POINT ( 'NONE',  ( 0.6418149653042463099, -1.608749606796000098, -0.5875140676452391686 ) ) ;
#31730=CARTESIAN_POINT ( 'NONE',  ( 0.6413879784614744395, -1.405912376546664122, -0.6250000000000000000 ) ) ;
#31732=ORIENTED_EDGE ( 'NONE', *, *, #28075, .T. ) ;
#31739=AXIS2_PLACEMENT_3D ( 'NONE', #25078, #11912, #2662 ) ;
#31743=B_SPLINE_CURVE_WITH_KNOTS ( 'NONE', 3,
 ( #8339, #4828, #33624, #29959, #30349, #39814, #36307, #8129, #5043, #33236, #1978, #14500, #2179, #11432, #23999, #5236, #14718, #11639, #12433, #12040, #5841, #5654 ),
 .UNSPECIFIED., .F., .F.,
 ( 4, 2, 2, 2, 2, 2, 2, 2, 2, 2, 4 ),
 ( 0.000000000000000000, 0.0007691844400138901378, 0.001538368880027780276, 0.003076737760055560118, 0.006153475520111119368, 0.007691844400138887934, 0.008461028840152783059, 0.009230213280166679052, 0.01076858216019446757, 0.01153776660020836183, 0.01230695104022225608 ),
 .UNSPECIFIED. ) ;
#31745=CARTESIAN_POINT ( 'NONE',  ( 0.4494697147526631742, -1.096181161593837050, -0.6251428030132534230 ) ) ;
#31769=CARTESIAN_POINT ( 'NONE',  ( 0.4064036231482041073, -1.678616732723309024, -0.5150861416748760968 ) ) ;
#31776=EDGE_CURVE ( 'NONE', #13497, #32636, #11040, .T. ) ;
#31777=ORIENTED_EDGE ( 'NONE', *, *, #32624, .F. ) ;
#31788=CARTESIAN_POINT ( 'NONE',  ( 0.4137599315576335757, -1.590143257116447995, -0.4137273532990812797 ) ) ;
#31790=CARTESIAN_POINT ( 'NONE',  ( 0.1999999999999780564, -2.097675824466503247, -0.7286991843995637153 ) ) ;
#31802=AXIS2_PLACEMENT_3D ( 'NONE', #21893, #28449, #16127 ) ;
#31806=CARTESIAN_POINT ( 'NONE',  ( 0.4795819664771984736, -1.106247336020415917, -0.4111404562665418871 ) ) ;
#31821=CIRCLE ( 'NONE', #22009, 0.05330708661417342398 ) ;
#31846=CARTESIAN_POINT ( 'NONE',  ( 0.09522563388679633478, -1.586419958512597539, -0.3717731054125978374 ) ) ;
#31848=EDGE_CURVE ( 'NONE', #28606, #20339, #9577, .T. ) ;
#31851=CARTESIAN_POINT ( 'NONE',  ( 0.2534230856981304347, -1.365321207853003926, -0.2869361388274794256 ) ) ;
#31853=CARTESIAN_POINT ( 'NONE',  ( 0.4234909963964843538, -1.082397635545747638, -0.5155029497116575543 ) ) ;
#31854=CARTESIAN_POINT ( 'NONE',  ( 0.3943729676430805520, -1.992383741152799370, -0.7037009085642309536 ) ) ;
#31876=CARTESIAN_POINT ( 'NONE',  ( 0.5746577578530626118, -1.612782564726902290, -0.5066312177471922196 ) ) ;
#31879=DIRECTION ( 'NONE',  ( 0.4999551463232372317, -0.8660512985181135770, 0.000000000000000000 ) ) ;
#31886=CARTESIAN_POINT ( 'NONE',  ( 0.1934284681205496736, -1.261395051998276839, -0.3194747338454530516 ) ) ;
#31890=CARTESIAN_POINT ( 'NONE',  ( 0.06691088171154270514, -1.526692643628365209, -0.3435217948658035314 ) ) ;
#31902=EDGE_CURVE ( 'NONE', #3578, #40101, #37136, .T. ) ;
#31905=AXIS2_PLACEMENT_3D ( 'NONE', #31092, #6391, #40549 ) ;
#31907=DIRECTION ( 'NONE',  ( 0.000000000000000000, 0.000000000000000000, -1.000000000000000000 ) ) ;
#31911=CARTESIAN_POINT ( 'NONE',  ( 0.1889659664986145515, -1.964260910147563655, -0.6656705585301033734 ) ) ;
#31913=CARTESIAN_POINT ( 'NONE',  ( 0.3996799965260696141, -1.685664405872516980, -0.5055465857900723892 ) ) ;
#31917=CARTESIAN_POINT ( 'NONE',  ( 0.3737379149731986927, -1.762635032660671230, -0.5786828194896244115 ) ) ;
#31918=ORIENTED_EDGE ( 'NONE', *, *, #5215, .F. ) ;
#31924=ADVANCED_FACE ( 'NONE', ( #36383 ), #17063, .T. ) ;
#31926=CARTESIAN_POINT ( 'NONE',  ( 0.5188695029506764644, -1.672825691405887216, -0.4370831669522161067 ) ) ;
#31929=AXIS2_PLACEMENT_3D ( 'NONE', #23004, #35741, #816 ) ;
#31930=ORIENTED_EDGE ( 'NONE', *, *, #16964, .F. ) ;
#31931=ORIENTED_EDGE ( 'NONE', *, *, #22319, .F. ) ;
#31932=DIRECTION ( 'NONE',  ( 0.7956551220374307176, 0.4593167559955306789, 0.3949190352937466675 ) ) ;
#31942=CARTESIAN_POINT ( 'NONE',  ( 0.6438069111488841090, -1.607599693877530544, -0.4632284053853421568 ) ) ;
#31954=AXIS2_PLACEMENT_3D ( 'NONE', #29064, #9541, #9740 ) ;
#31958=( BOUNDED_SURFACE ( )  B_SPLINE_SURFACE ( 3, 2, ( 
 ( #37481, #21881, #34409 ),
 ( #18986, #14885, #15894 ),
 ( #19784, #35423, #19189 ),
 ( #25376, #13413, #31518 ) ),
 .UNSPECIFIED., .F., .F., .T. ) 
 B_SPLINE_SURFACE_WITH_KNOTS ( ( 4, 4 ),
 ( 3, 3 ),
 ( -8.673617379884035472E-19, 0.002131800461895016693 ),
 ( 0.4549088439910530246, 0.5960639224100784395 ),
 .UNSPECIFIED. ) 
 GEOMETRIC_REPRESENTATION_ITEM ( )  RATIONAL_B_SPLINE_SURFACE ( (
 ( 0.8536398787998742410, 0.8498830870480222899, 0.8578866998027966373),
 ( 0.8543866741646273244, 0.8506490512590678676, 0.8586118259709549783),
 ( 0.8547489119030206028, 0.8510205869656279898, 0.8589635529307095840),
 ( 0.8547444188128500153, 0.8510159785461998139, 0.8589591902131400447) ) ) 
 REPRESENTATION_ITEM ( '' )  SURFACE ( )  );
#31971=ORIENTED_EDGE ( 'NONE', *, *, #13500, .F. ) ;
#31974=DIRECTION ( 'NONE',  ( 0.8660512985181133550, 0.4999551463232372872, 0.000000000000000000 ) ) ;
#31979=CARTESIAN_POINT ( 'NONE',  ( 0.1909286924077255032, -1.257064795538239022, -0.2869361388274795921 ) ) ;
#31987=CARTESIAN_POINT ( 'NONE',  ( 0.5063069112233773428, -1.619831626756517595, -0.4536019516388486439 ) ) ;
#32005=CARTESIAN_POINT ( 'NONE',  ( 0.2923286432308245808, -1.660243258845594649, -0.6250000000000000000 ) ) ;
#32009=CARTESIAN_POINT ( 'NONE',  ( 0.3742950363398350744, -1.612925599803100907, -0.4159227622875389385 ) ) ;
#32015=EDGE_CURVE ( 'NONE', #37937, #9810, #8596, .T. ) ;
#32019=FACE_OUTER_BOUND ( 'NONE', #24505, .T. ) ;
#32031=CARTESIAN_POINT ( 'NONE',  ( 0.3496751906377999486, -1.633240291291184088, -0.3739997235031339851 ) ) ;
#32038=CARTESIAN_POINT ( 'NONE',  ( 0.5262299346437796510, -1.635933710071385550, -0.4253948248519428543 ) ) ;
#32044=CARTESIAN_POINT ( 'NONE',  ( 0.08681952791238080336, -1.461498312203829864, -0.3696288966504583939 ) ) ;
#32048=B_SPLINE_CURVE_WITH_KNOTS ( 'NONE', 3,
 ( #16882, #29618, #19371, #35794, #872, #32290 ),
 .UNSPECIFIED., .F., .F.,
 ( 4, 2, 4 ),
 ( 0.000000000000000000, 0.0004418112746277370710, 0.0008836225492554741420 ),
 .UNSPECIFIED. ) ;
#32049=DIRECTION ( 'NONE',  ( -0.000000000000000000, 0.9679004486746793923, 0.2513338844154409668 ) ) ;
#32051=CARTESIAN_POINT ( 'NONE',  ( 0.3961980758757063792, -2.017725590686155979, -0.5051786489766182386 ) ) ;
#32063=CARTESIAN_POINT ( 'NONE',  ( 0.5834517445836356897, -1.469888346549154123, -0.4281759616558344361 ) ) ;
#32064=CARTESIAN_POINT ( 'NONE',  ( -2.125292368820994835E-14, -2.097675824466503691, -0.2907077406111384654 ) ) ;
#32074=CARTESIAN_POINT ( 'NONE',  ( 0.3553889254481614746, -1.722186678249592262, -0.4852332081978528167 ) ) ;
#32083=CARTESIAN_POINT ( 'NONE',  ( 0.5317043845607695163, -1.659957901717503237, -0.4539538042794677986 ) ) ;
#32087=CARTESIAN_POINT ( 'NONE',  ( 0.02679060571419135048, -1.592882453846480306, -0.3460849381908203126 ) ) ;
#32089=VERTEX_POINT ( 'NONE', #2457 ) ;
#32103=EDGE_CURVE ( 'NONE', #17298, #20307, #5515, .T. ) ;
#32106=CARTESIAN_POINT ( 'NONE',  ( 0.2927350798623002959, -1.544518291098198715, -0.6925464747855896164 ) ) ;
#32107=CARTESIAN_POINT ( 'NONE',  ( 0.2483187509121489445, -1.578255509793611733, -0.6753565671395465042 ) ) ;
#32110=CARTESIAN_POINT ( 'NONE',  ( 0.3572467526666761040, -1.837614999197383803, -0.4832994198719710033 ) ) ;
#32121=CARTESIAN_POINT ( 'NONE',  ( 0.09152739630308469321, -1.274033986120670425, -0.5155029497116575543 ) ) ;
#32125=ORIENTED_EDGE ( 'NONE', *, *, #29496, .F. ) ;
#32136=CARTESIAN_POINT ( 'NONE',  ( 0.3616412802241143476, -1.759290408630900693, -0.5212859374495405484 ) ) ;
#32139=CARTESIAN_POINT ( 'NONE',  ( 0.5854253530110696824, -1.600634416322008979, -0.5807582330271072735 ) ) ;
#32140=CARTESIAN_POINT ( 'NONE',  ( 0.4159916692016358830, -1.069406866067976081, -0.5155029497116575543 ) ) ;
#32144=CARTESIAN_POINT ( 'NONE',  ( 0.4932954302610373931, -1.588333833162793862, -0.5706078562424887757 ) ) ;
#32149=CARTESIAN_POINT ( 'NONE',  ( 0.4697623592636160361, -1.061459377010899541, -0.6056023639864149821 ) ) ;
#32155=CARTESIAN_POINT ( 'NONE',  ( 0.3699999999999786793, -2.143627883852845528, -0.5325888117242428832 ) ) ;
#32169=CARTESIAN_POINT ( 'NONE',  ( 0.3624061103390766592, -1.968824918581878025, -0.4968426515054770176 ) ) ;
#32171=ORIENTED_EDGE ( 'NONE', *, *, #22101, .T. ) ;
#32177=CARTESIAN_POINT ( 'NONE',  ( 0.4939403457259635144, -1.587801743525764975, -0.4617121892232378122 ) ) ;
#32180=VERTEX_POINT ( 'NONE', #19303 ) ;
#32183=CARTESIAN_POINT ( 'NONE',  ( 0.2207973309884857516, -1.612506204770620455, -0.3262751652180214679 ) ) ;
#32185=( BOUNDED_SURFACE ( )  B_SPLINE_SURFACE ( 3, 2, ( 
 ( #13120, #37824, #9639 ),
 ( #34931, #3462, #9216 ),
 ( #38214, #35142, #12938 ),
 ( #25485, #6738, #37403 ),
 ( #38021, #9830, #16231 ),
 ( #19313, #31854, #3672 ),
 ( #6946, #19518, #32051 ),
 ( #28953, #5411, #4052 ),
 ( #17976, #19701, #1776 ),
 ( #27043, #39377, #30536 ),
 ( #36284, #39572, #38418 ),
 ( #30131, #16617, #14691 ),
 ( #4802, #7134, #29166 ),
 ( #5021, #11619, #1028 ),
 ( #10255, #10441, #29936 ),
 ( #1959, #26850, #23003 ),
 ( #14473, #11199, #26107 ),
 ( #14288, #23763, #17378 ),
 ( #22823, #17586, #33214 ),
 ( #39787, #11405, #23973 ),
 ( #32233, #13539, #38621 ),
 ( #35527, #35343, #24177 ),
 ( #17768, #7328, #8102 ),
 ( #36505, #13326, #20680 ),
 ( #8317, #5218, #36702 ),
 ( #20887, #19906, #32996 ) ),
 .UNSPECIFIED., .F., .F., .F. ) 
 B_SPLINE_SURFACE_WITH_KNOTS ( ( 4, 2, 2, 2, 2, 2, 2, 2, 2, 2, 2, 2, 4 ),
 ( 3, 3 ),
 ( 0.03478970966414503263, 0.03529932688707621696, 0.03580894411000740130, 0.03682817855586976996, 0.03886664744759451423, 0.04090511633931925850, 0.04294358523104399583, 0.04498205412276873316, 0.04600128856863110183, 0.04702052301449347743, 0.04803975746035585304, 0.04905899190621822170, 0.05109746079794295903 ),
 ( 0.000000000000000000, 1.000000000000000000 ),
 .UNSPECIFIED. ) 
 GEOMETRIC_REPRESENTATION_ITEM ( )  RATIONAL_B_SPLINE_SURFACE ( (
 ( 1.000000000000000000, 0.7053326528219874270, 1.000000000000000000),
 ( 1.000000000000000000, 0.7069087193608286634, 1.000000000000000000),
 ( 1.000000000000000000, 0.7074454249098807157, 1.000000000000000000),
 ( 1.000000000000000000, 0.7079727039066889827, 1.000000000000000000),
 ( 1.000000000000000000, 0.7079140579849851900, 1.000000000000000000),
 ( 1.000000000000000000, 0.7072990859638627059, 1.000000000000000000),
 ( 1.000000000000000000, 0.7062992663257997572, 1.000000000000000000),
 ( 1.000000000000000000, 0.7026654075174076919, 1.000000000000000000),
 ( 1.000000000000000000, 0.6993568048661583658, 1.000000000000000000),
 ( 1.000000000000000000, 0.6923303540839972348, 1.000000000000000000),
 ( 1.000000000000000000, 0.6885467396574445065, 1.000000000000000000),
 ( 1.000000000000000000, 0.6809569680526224023, 1.000000000000000000),
 ( 1.000000000000000000, 0.6771650901614095774, 1.000000000000000000),
 ( 1.000000000000000000, 0.6704471956692915624, 1.000000000000000000),
 ( 1.000000000000000000, 0.6675067785250806685, 1.000000000000000000),
 ( 1.000000000000000000, 0.6649784099743589749, 1.000000000000000000),
 ( 1.000000000000000000, 0.6644567522674703630, 1.000000000000000000),
 ( 1.000000000000000000, 0.6643594168463616834, 1.000000000000000000),
 ( 1.000000000000000000, 0.6647836916441944854, 1.000000000000000000),
 ( 1.000000000000000000, 0.6667676599422263095, 1.000000000000000000),
 ( 1.000000000000000000, 0.6683270600133986994, 1.000000000000000000),
 ( 1.000000000000000000, 0.6727537477507504748, 1.000000000000000000),
 ( 1.000000000000000000, 0.6756357399904314720, 1.000000000000000000),
 ( 1.000000000000000000, 0.6860398255729156514, 1.000000000000000000),
 ( 1.000000000000000000, 0.6954024235277513899, 1.000000000000000000),
 ( 1.000000000000000000, 0.7067908011272805435, 1.000000000000000000) ) ) 
 REPRESENTATION_ITEM ( '' )  SURFACE ( )  );
#32187=EDGE_CURVE ( 'NONE', #16904, #9810, #27921, .T. ) ;
#32190=DIRECTION ( 'NONE',  ( -0.5115305431914159984, 0.8592650949400278959, 0.000000000000000000 ) ) ;
#32192=AXIS2_PLACEMENT_3D ( 'NONE', #2825, #15374, #18056 ) ;
#32194=CARTESIAN_POINT ( 'NONE',  ( 0.5090125390690136697, -1.650034892930424268, -0.5917945072846980681 ) ) ;
#32197=CARTESIAN_POINT ( 'NONE',  ( 0.1851558620279397105, -1.247064763968795287, -0.6244862546769320844 ) ) ;
#32202=CARTESIAN_POINT ( 'NONE',  ( 0.3658297366832102271, -1.745592370396174875, -0.4954708084374069288 ) ) ;
#32206=CARTESIAN_POINT ( 'NONE',  ( 0.3788106256558574914, -1.616048764795402937, -0.3641495012956140198 ) ) ;
#32213=ORIENTED_EDGE ( 'NONE', *, *, #21830, .F. ) ;
#32226=CARTESIAN_POINT ( 'NONE',  ( 0.001665905518637939096, -1.790954619074065945, -0.3617774004250685072 ) ) ;
#32228=DIRECTION ( 'NONE',  ( 1.000000000000000000, 0.000000000000000000, 0.000000000000000000 ) ) ;
#32233=CARTESIAN_POINT ( 'NONE',  ( 0.2100158411153514038, -1.623712120995903341, -0.6928538852213783628 ) ) ;
#32237=CARTESIAN_POINT ( 'NONE',  ( 0.6635990329685389488, -1.451118425079158891, -0.6162234092229578186 ) ) ;
#32253=DIRECTION ( 'NONE',  ( 0.8660512985181132439, 0.4999551463232376758, 0.000000000000000000 ) ) ;
#32254=CARTESIAN_POINT ( 'NONE',  ( 0.3433798484762162762, -1.649580330210344226, -0.4420781474354099072 ) ) ;
#32261=CARTESIAN_POINT ( 'NONE',  ( 0.3391898079600526028, -1.708268844615858484, -0.6004883020675078065 ) ) ;
#32263=CARTESIAN_POINT ( 'NONE',  ( 0.6004930002435877601, -1.482345764245047937, -0.6229362720418619714 ) ) ;
#32267=CARTESIAN_POINT ( 'NONE',  ( 0.5361355449682986274, -1.657745371039847759, -0.4610437686141751201 ) ) ;
#32271=CARTESIAN_POINT ( 'NONE',  ( 0.03256590615868563965, -1.845618522021015728, -0.3210350534622004592 ) ) ;
#32278=CARTESIAN_POINT ( 'NONE',  ( 0.1999999999999789724, -2.183180860297921466, -0.2737760292030870235 ) ) ;
#32285=CIRCLE ( 'NONE', #38830, 0.2000000000000000111 ) ;
#32288=DIRECTION ( 'NONE',  ( 0.4999551463232372317, -0.8660512985181135770, 0.000000000000000000 ) ) ;
#32290=CARTESIAN_POINT ( 'NONE',  ( 0.4291849790131893050, -1.119523916798046859, -0.6481113851292223949 ) ) ;
#32295=CARTESIAN_POINT ( 'NONE',  ( 0.1781635123675364418, -1.733799861008286758, -0.6515288039002870013 ) ) ;
#32297=CARTESIAN_POINT ( 'NONE',  ( 0.1748197985926945586, -1.826458824642884782, -0.6524116373567239169 ) ) ;
#32299=CARTESIAN_POINT ( 'NONE',  ( 0.2409193767872376546, -1.343661558146008073, -0.2869361388274795921 ) ) ;
#32302=CARTESIAN_POINT ( 'NONE',  ( 0.3795613398208534384, -1.760143698493221942, -0.5723197561600823491 ) ) ;
#32307=CARTESIAN_POINT ( 'NONE',  ( 0.4738546087217575531, -1.652018268363231401, -0.3975985852014373156 ) ) ;
#32322=ORIENTED_EDGE ( 'NONE', *, *, #14586, .F. ) ;
#32347=AXIS2_PLACEMENT_3D ( 'NONE', #9711, #25762, #901 ) ;
#32351=CARTESIAN_POINT ( 'NONE',  ( 0.3220325133609698853, -1.710602945088052884, -0.6976313533424302049 ) ) ;
#32361=CARTESIAN_POINT ( 'NONE',  ( 0.3545879618755022888, -1.837530425579354754, -0.4889651724334035388 ) ) ;
#32370=CIRCLE ( 'NONE', #12007, 0.1333070866141734812 ) ;
#32377=AXIS2_PLACEMENT_3D ( 'NONE', #23485, #13983, #39095 ) ;
#32395=CARTESIAN_POINT ( 'NONE',  ( 0.5313292079975693305, -1.639131752853789203, -0.5569014201383083451 ) ) ;
#32403=DIRECTION ( 'NONE',  ( -0.7993299944781128152, -0.4614381908250200781, 0.3848978513524763390 ) ) ;
#32411=AXIS2_PLACEMENT_3D ( 'NONE', #25123, #19157, #22666 ) ;
#32413=DIRECTION ( 'NONE',  ( -0.4999551463232372317, 0.8660512985181133550, -0.000000000000000000 ) ) ;
#32418=FACE_OUTER_BOUND ( 'NONE', #10070, .T. ) ;
#32421=EDGE_LOOP ( 'NONE', ( #25234, #8379, #33225, #3875 ) ) ;
#32426=DIRECTION ( 'NONE',  ( -0.8660512985181141321, -0.4999551463232362325, 0.000000000000000000 ) ) ;
#32433=CARTESIAN_POINT ( 'NONE',  ( 0.3888736924534981765, -1.922885813500992302, -0.5052802514659558986 ) ) ;
#32444=CARTESIAN_POINT ( 'NONE',  ( 0.1999999999999789724, -2.107936428766273629, -0.7005084057759867200 ) ) ;
#32448=CARTESIAN_POINT ( 'NONE',  ( 0.6554566019120018350, -1.532497645495064287, -0.6162739285286029656 ) ) ;
#32454=CARTESIAN_POINT ( 'NONE',  ( 0.5807455352771149215, -1.554996163023655065, -0.4302623287978634692 ) ) ;
#32456=CARTESIAN_POINT ( 'NONE',  ( 0.02999999999997872077, -2.097675824466503691, -0.2588528740066097233 ) ) ;
#32458=ORIENTED_EDGE ( 'NONE', *, *, #12667, .T. ) ;
#32462=ORIENTED_EDGE ( 'NONE', *, *, #34633, .T. ) ;
#32465=CARTESIAN_POINT ( 'NONE',  ( 0.3574355869465279389, -1.729638559385621166, -0.4925610001298441065 ) ) ;
#32467=DIRECTION ( 'NONE',  ( 0.8660512985181133550, 0.4999551463232371207, 0.000000000000000000 ) ) ;
#32472=CARTESIAN_POINT ( 'NONE',  ( 0.5849095050029387011, -1.491341823319836335, -0.5960747874205124530 ) ) ;
#32475=CARTESIAN_POINT ( 'NONE',  ( 0.5308991136117184872, -1.672779244483038719, -0.4688114127759857030 ) ) ;
#32479=CARTESIAN_POINT ( 'NONE',  ( 0.05387575222800708441, -1.597043685520700862, -0.3437276073321817726 ) ) ;
#32481=CARTESIAN_POINT ( 'NONE',  ( -2.112273405726188513E-14, -2.183180860297921466, -0.2437760292030870524 ) ) ;
#32486=CARTESIAN_POINT ( 'NONE',  ( 0.4810758011828559777, -1.682094021195914113, -0.6143846718455718836 ) ) ;
#32494=FACE_OUTER_BOUND ( 'NONE', #11126, .T. ) ;
#32501=CARTESIAN_POINT ( 'NONE',  ( 0.1909286924077255310, -1.257064795538239022, -0.3824824602286830411 ) ) ;
#32502=AXIS2_PLACEMENT_3D ( 'NONE', #14948, #18424, #12273 ) ;
#32505=CARTESIAN_POINT ( 'NONE',  ( 0.1886650716668294425, -1.684993351743720336, -0.6545385004037254095 ) ) ;
#32514=AXIS2_PLACEMENT_3D ( 'NONE', #27488, #37146, #21930 ) ;
#32516=CARTESIAN_POINT ( 'NONE',  ( 0.4989284167723000429, -1.653128005833214065, -0.4311520333451080433 ) ) ;
#32525=CARTESIAN_POINT ( 'NONE',  ( 0.2059273467974228888, -1.283046334493782803, -0.6702542665264737964 ) ) ;
#32526=CARTESIAN_POINT ( 'NONE',  ( 0.5237801217064862458, -1.180371363492203285, -0.6194292131661300882 ) ) ;
#32529=CARTESIAN_POINT ( 'NONE',  ( 0.6223120740387964034, -1.620008259572149445, -0.4840127556439880463 ) ) ;
#32537=ORIENTED_EDGE ( 'NONE', *, *, #39802, .F. ) ;
#32539=CARTESIAN_POINT ( 'NONE',  ( 0.1759300380180282841, -1.231083256582695906, -0.6184399470714002645 ) ) ;
#32545=CARTESIAN_POINT ( 'NONE',  ( 0.3999999999999798161, -2.166079853131637645, -0.4467913981637911536 ) ) ;
#32566=CARTESIAN_POINT ( 'NONE',  ( 0.2117601568378603694, -1.293150266309827101, -0.7462941026102624109 ) ) ;
#32574=CARTESIAN_POINT ( 'NONE',  ( -2.120170153832874165E-14, -2.097675824466503691, -0.6968677163258657492 ) ) ;
#32576=CARTESIAN_POINT ( 'NONE',  ( 0.3560973459019345921, -1.892274349130671274, -0.5076868541395752610 ) ) ;
#32577=EDGE_CURVE ( 'NONE', #24493, #20049, #2423, .T. ) ;
#32581=ORIENTED_EDGE ( 'NONE', *, *, #24513, .T. ) ;
#32593=CARTESIAN_POINT ( 'NONE',  ( 0.6593903862521710568, -1.512843973183619850, -0.6186210669918369431 ) ) ;
#32594=B_SPLINE_CURVE_WITH_KNOTS ( 'NONE', 3,
 ( #3846, #3451, #618, #38612, #13713, #25673, #22993, #38208, #10030, #32433, #35134, #6935, #808, #13316 ),
 .UNSPECIFIED., .F., .F.,
 ( 4, 2, 2, 2, 2, 2, 4 ),
 ( 0.001790297533228681851, 0.002478079898554628058, 0.003165862263880574699, 0.004541426994532467981, 0.005916991725184360396, 0.006604774090510308338, 0.007292556455836254545 ),
 .UNSPECIFIED. ) ;
#32607=CARTESIAN_POINT ( 'NONE',  ( 0.5503547679451166186, -1.661547860700446799, -0.5401600205605633365 ) ) ;
#32610=FACE_OUTER_BOUND ( 'NONE', #40407, .T. ) ;
#32611=EDGE_CURVE ( 'NONE', #32971, #25148, #12080, .T. ) ;
#32615=CARTESIAN_POINT ( 'NONE',  ( 0.2059273467974226113, -1.283046334493782359, -0.7137159211901564770 ) ) ;
#32618=CARTESIAN_POINT ( 'NONE',  ( 0.3585037315287261661, -1.733294065422876784, -0.4968629709071194500 ) ) ;
#32624=EDGE_CURVE ( 'NONE', #20049, #22416, #13179, .T. ) ;
#32625=CARTESIAN_POINT ( 'NONE',  ( 0.6530643362242376515, -1.539305493024291094, -0.4161285573133042814 ) ) ;
#32630=DIRECTION ( 'NONE',  ( -0.4999551463232377313, 0.8660512985181132439, -0.000000000000000000 ) ) ;
#32636=VERTEX_POINT ( 'NONE', #34239 ) ;
#32637=EDGE_CURVE ( 'NONE', #3269, #35263, #19951, .T. ) ;
#32649=CARTESIAN_POINT ( 'NONE',  ( 0.3984114568195522010, -1.599003643269838904, -0.5155029497116575543 ) ) ;
#32650=CARTESIAN_POINT ( 'NONE',  ( 0.4111143676683018389, -1.741928728223572920, -0.4339933128339369950 ) ) ;
#32652=CARTESIAN_POINT ( 'NONE',  ( 0.3265224326933078847, -1.121055775672392452, -0.5155029497116575543 ) ) ;
#32659=CARTESIAN_POINT ( 'NONE',  ( 0.6596696466511408063, -1.414650502503907559, -0.6114726203884881528 ) ) ;
#32666=CARTESIAN_POINT ( 'NONE',  ( 0.5859173466656659723, -1.569541677886773012, -0.5263893777432389065 ) ) ;
#32667=CARTESIAN_POINT ( 'NONE',  ( 0.4806378395295556882, -1.105637800341302102, -0.6194292131661300882 ) ) ;
#32673=( BOUNDED_SURFACE ( )  B_SPLINE_SURFACE ( 3, 2, ( 
 ( #3214, #27711, #2616 ),
 ( #6301, #15154, #40245 ),
 ( #12082, #36962, #9597 ),
 ( #15974, #37176, #21744 ),
 ( #27923, #40040, #24643 ),
 ( #34687, #11863, #30993 ) ),
 .UNSPECIFIED., .F., .F., .F. ) 
 B_SPLINE_SURFACE_WITH_KNOTS ( ( 4, 2, 4 ),
 ( 3, 3 ),
 ( -2.108773225484306124E-17, 0.0002308790202334583513, 0.0004617580404669377903 ),
 ( 0.000000000000000000, 1.000000000000000000 ),
 .UNSPECIFIED. ) 
 GEOMETRIC_REPRESENTATION_ITEM ( )  RATIONAL_B_SPLINE_SURFACE ( (
 ( 1.000000000000000000, 0.9183064432839348479, 1.000000000000000000),
 ( 1.000000000000000000, 0.9259132747140148556, 1.000000000000000000),
 ( 1.000000000000000000, 0.9308516525543161224, 1.000000000000000000),
 ( 1.000000000000000000, 0.9333900639176514469, 1.000000000000000000),
 ( 1.000000000000000000, 0.9310108186281401688, 1.000000000000000000),
 ( 1.000000000000000000, 0.9252764552858380176, 1.000000000000000000) ) ) 
 REPRESENTATION_ITEM ( '' )  SURFACE ( )  );
#32676=CARTESIAN_POINT ( 'NONE',  ( 0.4887921365776448090, -1.679766821171225999, -0.4193976862638449377 ) ) ;
#32682=AXIS2_PLACEMENT_3D ( 'NONE', #5956, #31287, #12545 ) ;
#32685=CARTESIAN_POINT ( 'NONE',  ( 0.4572526883583915014, -1.685933642108535357, -0.4119903234399788228 ) ) ;
#32691=CARTESIAN_POINT ( 'NONE',  ( 0.1317419978059748698, -1.353679905699192831, -0.3213817580603143265 ) ) ;
#32699=DIRECTION ( 'NONE',  ( -1.000000000000000000, -0.000000000000000000, -0.000000000000000000 ) ) ;
#32712=DIRECTION ( 'NONE',  ( 0.000000000000000000, 0.000000000000000000, -1.000000000000000000 ) ) ;
#32717=CARTESIAN_POINT ( 'NONE',  ( 0.2059273467974226113, -1.283046334493782803, -0.3194715457588298557 ) ) ;
#32730=DIRECTION ( 'NONE',  ( -0.8660512985181135770, -0.4999551463232371207, 0.000000000000000000 ) ) ;
#32743=CARTESIAN_POINT ( 'NONE',  ( 0.4815782007885943128, -1.590841155114501193, -0.5855112036560438105 ) ) ;
#32759=EDGE_LOOP ( 'NONE', ( #39494, #31430, #13252, #30761 ) ) ;
#32760=CARTESIAN_POINT ( 'NONE',  ( 0.3389453752120347718, -1.642550427334032337, -0.5887789075332919841 ) ) ;
#32768=CARTESIAN_POINT ( 'NONE',  ( -3.340522353737697295E-05, -2.021039392244021737, -0.7047055906517447621 ) ) ;
#32769=EDGE_CURVE ( 'NONE', #13144, #29455, #15150, .T. ) ;
#32775=ORIENTED_EDGE ( 'NONE', *, *, #2652, .T. ) ;
#32785=EDGE_CURVE ( 'NONE', #23204, #36736, #17533, .T. ) ;
#32787=CARTESIAN_POINT ( 'NONE',  ( 0.6505833821421317387, -1.551223176788856017, -0.6117998873676726568 ) ) ;
#32791=CARTESIAN_POINT ( 'NONE',  ( 0.4409062655693438137, -1.690090444797295977, -0.2869361388274795921 ) ) ;
#32792=CARTESIAN_POINT ( 'NONE',  ( 0.1909286924077255587, -1.257064795538239022, -0.6702538898043716165 ) ) ;
#32793=PLANE ( 'NONE',  #11949 ) ;
#32795=CARTESIAN_POINT ( 'NONE',  ( 0.02999999999997886302, -2.183180860297921466, -0.4937760292030871079 ) ) ;
#32798=CARTESIAN_POINT ( 'NONE',  ( 0.04100175935075398709, -1.705062125326649580, -0.3379690677246707242 ) ) ;
#32799=CARTESIAN_POINT ( 'NONE',  ( 0.5284743900675886730, -1.670479918469192970, -0.5846305483259907065 ) ) ;
#32806=CARTESIAN_POINT ( 'NONE',  ( 0.3645450313092892247, -1.732400383701045543, -0.4756653114284276063 ) ) ;
#32818=CARTESIAN_POINT ( 'NONE',  ( 0.5749221830005468714, -1.540359961810453759, -0.4819944042435657661 ) ) ;
#32821=ADVANCED_FACE ( 'NONE', ( #39137 ), #6957, .T. ) ;
#32836=CARTESIAN_POINT ( 'NONE',  ( 0.3811932541547525810, -1.750588582039273033, -0.4368655358042922709 ) ) ;
#32839=CARTESIAN_POINT ( 'NONE',  ( 0.3925301276612734314, -1.756377271995030576, -0.4843757382520814114 ) ) ;
#32848=CARTESIAN_POINT ( 'NONE',  ( 0.6016870789291266508, -1.595135992794870727, -0.4985500141948422947 ) ) ;
#32855=CARTESIAN_POINT ( 'NONE',  ( 0.5714446559762420552, -1.545268339499498378, -0.5210154178133508118 ) ) ;
#32863=ORIENTED_EDGE ( 'NONE', *, *, #2720, .T. ) ;
#32881=CARTESIAN_POINT ( 'NONE',  ( 0.3999999999999787059, -2.097675824466503691, -0.4937760292030871079 ) ) ;
#32883=CARTESIAN_POINT ( 'NONE',  ( 0.4262438152663738933, -1.592651821845863402, -0.6151431148613257793 ) ) ;
#32900=DIRECTION ( 'NONE',  ( -0.4999551463232372317, 0.8660512985181135770, -0.000000000000000000 ) ) ;
#32906=CARTESIAN_POINT ( 'NONE',  ( 0.3752374054691312577, -1.754338789473355087, -0.5850131874919822783 ) ) ;
#32909=CARTESIAN_POINT ( 'NONE',  ( 0.3699999999999786793, -2.183180860297921466, -0.4937760292030871079 ) ) ;
#32911=EDGE_LOOP ( 'NONE', ( #36729, #36867, #21459, #3243 ) ) ;
#32914=DIRECTION ( 'NONE',  ( -0.8132816101496389560, -0.4694921964796399116, -0.3437296903631308909 ) ) ;
#32946=CARTESIAN_POINT ( 'NONE',  ( 0.5057508247701024695, -1.620212811793598107, -0.5782665205887309590 ) ) ;
#32963=ORIENTED_EDGE ( 'NONE', *, *, #39910, .F. ) ;
#32964=DIRECTION ( 'NONE',  ( -1.000000000000000000, 0.000000000000000000, 0.000000000000000000 ) ) ;
#32971=VERTEX_POINT ( 'NONE', #39939 ) ;
#32973=CARTESIAN_POINT ( 'NONE',  ( 0.1153287684445949701, -1.330270486660940277, -0.7080039676230125423 ) ) ;
#32974=CARTESIAN_POINT ( 'NONE',  ( 0.3595108577967162100, -1.929697767679888987, -0.4979555812093512390 ) ) ;
#32977=DIRECTION ( 'NONE',  ( 0.4999551463232372317, -0.8660512985181135770, 0.000000000000000000 ) ) ;
#32987=ORIENTED_EDGE ( 'NONE', *, *, #39666, .T. ) ;
#32994=CIRCLE ( 'NONE', #27758, 0.08830708661417341343 ) ;
#32996=CARTESIAN_POINT ( 'NONE',  ( 0.4409062655693434807, -1.690090444797295532, -0.5318766032425230605 ) ) ;
#33000=CARTESIAN_POINT ( 'NONE',  ( 0.03256515207864835171, -1.845689418459394826, -0.3210198295332938323 ) ) ;
#33001=CARTESIAN_POINT ( 'NONE',  ( 0.5260376822698199506, -1.642293686627224414, -0.5683488690136782040 ) ) ;
#33006=ADVANCED_FACE ( 'NONE', ( #34369 ), #37677, .F. ) ;
#33019=CIRCLE ( 'NONE', #33664, 0.02999999999999997113 ) ;
#33021=AXIS2_PLACEMENT_3D ( 'NONE', #35905, #4811, #20897 ) ;
#33039=DIRECTION ( 'NONE',  ( -1.000000000000000000, 0.000000000000000000, -0.000000000000000000 ) ) ;
#33042=DIRECTION ( 'NONE',  ( 0.8660512985181135770, 0.4999551463232370652, 0.000000000000000000 ) ) ;
#33053=VECTOR ( 'NONE', #37414, 39.37007874015748143 ) ;
#33057=CARTESIAN_POINT ( 'NONE',  ( 0.6080071089777098203, -1.584981494572885730, -0.5642241644406634782 ) ) ;
#33062=EDGE_CURVE ( 'NONE', #25706, #3269, #13393, .T. ) ;
#33065=CARTESIAN_POINT ( 'NONE',  ( 0.5697212493628158736, -1.577360437427027806, -0.5635484681258001727 ) ) ;
#33070=ADVANCED_FACE ( 'NONE', ( #9876 ), #22875, .F. ) ;
#33078=AXIS2_PLACEMENT_3D ( 'NONE', #30288, #3484, #6551 ) ;
#33093=FACE_OUTER_BOUND ( 'NONE', #5767, .T. ) ;
#33096=CARTESIAN_POINT ( 'NONE',  ( 0.09514782613886782481, -1.363928122608234927, -0.6711990196306176770 ) ) ;
#33111=FACE_OUTER_BOUND ( 'NONE', #8247, .T. ) ;
#33117=DIRECTION ( 'NONE',  ( 0.4999551463232372317, -0.8660512985181135770, 0.000000000000000000 ) ) ;
#33118=CARTESIAN_POINT ( 'NONE',  ( 0.3695849881062516218, -1.765902858937650199, -0.5832748682907470394 ) ) ;
#33119=EDGE_CURVE ( 'NONE', #29847, #37277, #16023, .T. ) ;
#33123=ORIENTED_EDGE ( 'NONE', *, *, #22536, .T. ) ;
#33132=ORIENTED_EDGE ( 'NONE', *, *, #14836, .F. ) ;
#33138=CARTESIAN_POINT ( 'NONE',  ( 0.5195836351326650338, -1.602777390882857533, -0.4212996487385544109 ) ) ;
#33139=CARTESIAN_POINT ( 'NONE',  ( 0.3534309663918363542, -1.740588291835677870, -0.3303540215336857044 ) ) ;
#33145=EDGE_CURVE ( 'NONE', #17298, #28471, #16614, .T. ) ;
#33149=AXIS2_PLACEMENT_3D ( 'NONE', #16192, #4425, #29123 ) ;
#33153=CARTESIAN_POINT ( 'NONE',  ( 0.3112311390139286815, -1.649331203103300059, -0.3389060930261176829 ) ) ;
#33154=CARTESIAN_POINT ( 'NONE',  ( -2.128280327564064936E-14, -2.097675824466503691, -0.6968677163258657492 ) ) ;
#33157=CARTESIAN_POINT ( 'NONE',  ( 0.3854651929502717067, -1.696813303095609404, -0.4100924813245869216 ) ) ;
#33163=( BOUNDED_SURFACE ( )  B_SPLINE_SURFACE ( 3, 2, ( 
 ( #13217, #34813, #3557 ),
 ( #19413, #16125, #28664 ),
 ( #34207, #532, #13029 ),
 ( #35020, #25784, #10138 ),
 ( #6018, #15510, #4362 ),
 ( #13426, #7042, #32743 ),
 ( #20013, #7226, #38520 ),
 ( #19611, #32946, #23319 ),
 ( #19796, #16922, #32144 ),
 ( #22710, #10352, #13625 ),
 ( #4749, #29052, #14235 ),
 ( #16512, #35242, #1119 ) ),
 .UNSPECIFIED., .F., .F., .F. ) 
 B_SPLINE_SURFACE_WITH_KNOTS ( ( 4, 2, 2, 2, 2, 4 ),
 ( 3, 3 ),
 ( 1.507041019754851163E-16, 0.0009292827807487099570, 0.001858565561497269210, 0.002323206951871548999, 0.002787848342245828354, 0.003717131122994387499 ),
 ( 0.000000000000000000, 1.000000000000000000 ),
 .UNSPECIFIED. ) 
 GEOMETRIC_REPRESENTATION_ITEM ( )  RATIONAL_B_SPLINE_SURFACE ( (
 ( 1.000000000000000000, 0.5022121722253957143, 1.000000000000000000),
 ( 1.000000000000000000, 0.5252469407714646099, 1.000000000000000000),
 ( 1.000000000000000000, 0.5463897451926625903, 1.000000000000000000),
 ( 1.000000000000000000, 0.5861329644067504452, 1.000000000000000000),
 ( 1.000000000000000000, 0.6040810576437375401, 1.000000000000000000),
 ( 1.000000000000000000, 0.6289914906242201065, 1.000000000000000000),
 ( 1.000000000000000000, 0.6370577570986643012, 1.000000000000000000),
 ( 1.000000000000000000, 0.6525045360464006849, 1.000000000000000000),
 ( 1.000000000000000000, 0.6598645560874571991, 1.000000000000000000),
 ( 1.000000000000000000, 0.6813382805142172982, 1.000000000000000000),
 ( 1.000000000000000000, 0.6952409275468639516, 1.000000000000000000),
 ( 1.000000000000000000, 0.7071067811865489050, 1.000000000000000000) ) ) 
 REPRESENTATION_ITEM ( '' )  SURFACE ( )  );
#33167=CARTESIAN_POINT ( 'NONE',  ( 0.6184088846978791354, -1.609314212450322357, -0.4711275932451951531 ) ) ;
#33174=CARTESIAN_POINT ( 'NONE',  ( 0.3935098752428118352, -1.601833234276202056, -0.6187469409402625020 ) ) ;
#33178=EDGE_LOOP ( 'NONE', ( #29244, #25263, #25353, #36879 ) ) ;
#33179=CARTESIAN_POINT ( 'NONE',  ( 0.4159916692016358830, -1.069406866067976081, -0.5155029497116575543 ) ) ;
#33186=CIRCLE ( 'NONE', #10851, 0.04330708661417343591 ) ;
#33188=ORIENTED_EDGE ( 'NONE', *, *, #4704, .F. ) ;
#33190=CARTESIAN_POINT ( 'NONE',  ( 0.009551370979964050878, -1.736475153700349550, -0.6662139729480507366 ) ) ;
#33192=CARTESIAN_POINT ( 'NONE',  ( 0.6620678144876760429, -1.446799780631947252, -0.4151272395384200675 ) ) ;
#33204=EDGE_LOOP ( 'NONE', ( #18829, #9131, #16741, #13685 ) ) ;
#33205=ORIENTED_EDGE ( 'NONE', *, *, #930, .T. ) ;
#33214=CARTESIAN_POINT ( 'NONE',  ( 0.4080314874273783254, -1.727341531470994562, -0.4910957289382530400 ) ) ;
#33216=CARTESIAN_POINT ( 'NONE',  ( 0.3591498995103406533, -1.737620376665804933, -0.5147966178037263196 ) ) ;
#33219=CARTESIAN_POINT ( 'NONE',  ( 0.1995529058109158649, -2.050896138459939344, -0.3054326997595754878 ) ) ;
#33223=DIRECTION ( 'NONE',  ( 0.4999551463232372317, -0.8660512985181133550, 0.000000000000000000 ) ) ;
#33225=ORIENTED_EDGE ( 'NONE', *, *, #38663, .F. ) ;
#33227=DIRECTION ( 'NONE',  ( -0.8660512985181131329, -0.4999551463232375648, -0.000000000000000000 ) ) ;
#33236=CARTESIAN_POINT ( 'NONE',  ( 0.1793546593917179355, -1.785823421859094706, -0.3235890279080452236 ) ) ;
#33240=CARTESIAN_POINT ( 'NONE',  ( 0.5725052286446696836, -1.544230605290505931, -0.5333758322335983015 ) ) ;
#33241=EDGE_LOOP ( 'NONE', ( #29682, #6987, #30105, #40305, #25107 ) ) ;
#33242=CIRCLE ( 'NONE', #15515, 0.03000000000000006481 ) ;
#33244=ORIENTED_EDGE ( 'NONE', *, *, #32785, .T. ) ;
#33249=VERTEX_POINT ( 'NONE', #31304 ) ;
#33257=CARTESIAN_POINT ( 'NONE',  ( 0.3969700875655671202, -1.750093955434230741, -0.5306525527941791109 ) ) ;
#33264=CARTESIAN_POINT ( 'NONE',  ( 0.6028087430831944316, -1.593422650548542485, -0.5410972547399238719 ) ) ;
#33273=CARTESIAN_POINT ( 'NONE',  ( 0.5762035759104484622, -1.538322682916094308, -0.5547479506342967159 ) ) ;
#33274=CARTESIAN_POINT ( 'NONE',  ( 0.4317026225184690813, -1.612351040652626466, -0.6637038356405958739 ) ) ;
#33283=ORIENTED_EDGE ( 'NONE', *, *, #5147, .F. ) ;
#33288=CARTESIAN_POINT ( 'NONE',  ( 0.3604126524395246944, -1.757925354409644925, -0.5278718762441512169 ) ) ;
#33294=CARTESIAN_POINT ( 'NONE',  ( 0.1371161371553715480, -1.302047841212754964, -0.3409434894749658329 ) ) ;
#33296=AXIS2_PLACEMENT_3D ( 'NONE', #28197, #18523, #34360 ) ;
#33297=ORIENTED_EDGE ( 'NONE', *, *, #15982, .T. ) ;
#33300=CARTESIAN_POINT ( 'NONE',  ( 0.3699999999999786793, -2.097675824466503691, -0.5196396315034578217 ) ) ;
#33316=DIRECTION ( 'NONE',  ( 1.000000000000000000, 0.000000000000000000, 0.000000000000000000 ) ) ;
#33317=ADVANCED_FACE ( 'NONE', ( #39083 ), #10140, .T. ) ;
#33319=CARTESIAN_POINT ( 'NONE',  ( 0.3920598280443489680, -1.752928556019227591, -0.5830366350881619475 ) ) ;
#33322=ORIENTED_EDGE ( 'NONE', *, *, #16515, .T. ) ;
#33326=DIRECTION ( 'NONE',  ( 0.4999551463232372317, -0.8660512985181135770, 0.000000000000000000 ) ) ;
#33335=CARTESIAN_POINT ( 'NONE',  ( 0.5313892105359160345, -1.599996326799270951, -0.4392153793885997248 ) ) ;
#33336=CARTESIAN_POINT ( 'NONE',  ( 0.6312476157716652159, -1.614849939179139993, -0.4878779670507682464 ) ) ;
#33339=ORIENTED_EDGE ( 'NONE', *, *, #28582, .T. ) ;
#33341=FACE_OUTER_BOUND ( 'NONE', #24372, .T. ) ;
#33344=EDGE_CURVE ( 'NONE', #30897, #25449, #20369, .T. ) ;
#33347=CARTESIAN_POINT ( 'NONE',  ( -6.834804016303107315E-15, -2.091147721901837286, -0.7263522089647810320 ) ) ;
#33348=CARTESIAN_POINT ( 'NONE',  ( 0.3331689678465135640, -1.752618680477372015, -0.5145915016017981181 ) ) ;
#33350=CARTESIAN_POINT ( 'NONE',  ( 0.3696071792890020524, -1.752960286906630527, -0.4262381047308068660 ) ) ;
#33353=AXIS2_PLACEMENT_3D ( 'NONE', #6562, #3099, #15642 ) ;
#33370=CARTESIAN_POINT ( 'NONE',  ( 0.3544525855955824589, -1.628498139902171848, -0.6593841416021899438 ) ) ;
#33375=CARTESIAN_POINT ( 'NONE',  ( 0.3579995238153922399, -1.735700120908051147, -0.5200972866788388105 ) ) ;
#33379=CARTESIAN_POINT ( 'NONE',  ( 0.3875836258550495184, -1.829270650397434306, -0.5020249712731550407 ) ) ;
#33384=ORIENTED_EDGE ( 'NONE', *, *, #33510, .F. ) ;
#33385=CARTESIAN_POINT ( 'NONE',  ( 0.02978343732698200338, -2.020922945396928849, -0.7048595805910107259 ) ) ;
#33405=CARTESIAN_POINT ( 'NONE',  ( 0.4291849790131893050, -1.119523916798046859, -0.6481113851292223949 ) ) ;
#33409=CARTESIAN_POINT ( 'NONE',  ( 0.1909286924077254199, -1.257064795538238577, -0.7137147910238503812 ) ) ;
#33414=CARTESIAN_POINT ( 'NONE',  ( -2.112273405726188513E-14, -2.183180860297921466, -0.2737760292030870235 ) ) ;
#33415=CARTESIAN_POINT ( 'NONE',  ( 0.3686425856813914104, -2.055607201583817378, -0.5118490229217781406 ) ) ;
#33423=FACE_OUTER_BOUND ( 'NONE', #21987, .T. ) ;
#33432=DIRECTION ( 'NONE',  ( 0.8308509739180691689, 0.4796346601509333119, 0.2822007298383447660 ) ) ;
#33433=PLANE ( 'NONE',  #29951 ) ;
#33442=CARTESIAN_POINT ( 'NONE',  ( 0.4291849790131893050, -1.119523916798046859, -0.6481113851292223949 ) ) ;
#33454=CARTESIAN_POINT ( 'NONE',  ( 0.3812071769896454021, -1.763750790280050440, -0.4536492913030992780 ) ) ;
#33458=CARTESIAN_POINT ( 'NONE',  ( 0.6021587300967877754, -1.594267875390501299, -0.4941518814792995040 ) ) ;
#33468=ORIENTED_EDGE ( 'NONE', *, *, #14177, .F. ) ;
#33478=CARTESIAN_POINT ( 'NONE',  ( 0.1870594268264934579, -1.259298449876196546, -0.3210044779109010871 ) ) ;
#33479=ORIENTED_EDGE ( 'NONE', *, *, #21830, .T. ) ;
#33480=CARTESIAN_POINT ( 'NONE',  ( 0.3316932917563030214, -1.670249455300529373, -0.6321824137348459605 ) ) ;
#33488=DIRECTION ( 'NONE',  ( 0.8660512985181134660, 0.4999551463232372872, 0.000000000000000000 ) ) ;
#33495=( BOUNDED_SURFACE ( )  B_SPLINE_SURFACE ( 3, 2, ( 
 ( #29465, #35429, #3948 ),
 ( #4748, #39325, #36035 ),
 ( #20011, #35841, #29877 ),
 ( #14233, #16510, #10743 ) ),
 .UNSPECIFIED., .F., .F., .F. ) 
 B_SPLINE_SURFACE_WITH_KNOTS ( ( 4, 4 ),
 ( 3, 3 ),
 ( -8.673617379884035472E-19, 0.002131800461895017127 ),
 ( 0.2677726292740011393, 0.6617067281966368952 ),
 .UNSPECIFIED. ) 
 GEOMETRIC_REPRESENTATION_ITEM ( )  RATIONAL_B_SPLINE_SURFACE ( (
 ( 0.8842712169365705144, 0.8302746405399135110, 0.8678740401095079715),
 ( 0.8848617173956563331, 0.8311406558908633890, 0.8685482063619062165),
 ( 0.8851481433175512059, 0.8315607220253672383, 0.8688752148974330236),
 ( 0.8851445905748156484, 0.8315555116488135834, 0.8688711587799162750) ) ) 
 REPRESENTATION_ITEM ( '' )  SURFACE ( )  );
#33497=CYLINDRICAL_SURFACE ( 'NONE', #18096, 0.04330708661417322775 ) ;
#33502=DIRECTION ( 'NONE',  ( -0.1858595909941333224, -0.1072932506077245995, 0.9767007580674449407 ) ) ;
#33510=EDGE_CURVE ( 'NONE', #7743, #4952, #3071, .T. ) ;
#33515=DIRECTION ( 'NONE',  ( 0.8660512985181135770, 0.4999551463232372317, 0.000000000000000000 ) ) ;
#33520=EDGE_CURVE ( 'NONE', #22416, #2187, #18688, .T. ) ;
#33526=CARTESIAN_POINT ( 'NONE',  ( 0.4996500228059882476, -1.606261977825028442, -0.4006985388676789217 ) ) ;
#33531=ORIENTED_EDGE ( 'NONE', *, *, #10922, .F. ) ;
#33532=CARTESIAN_POINT ( 'NONE',  ( 0.02999999999997886302, -2.183180860297921466, -0.2737760292030870235 ) ) ;
#33544=CARTESIAN_POINT ( 'NONE',  ( 0.3699999999999797895, -2.143572916703662123, -0.4549832530184109713 ) ) ;
#33545=AXIS2_PLACEMENT_3D ( 'NONE', #15375, #3222, #474 ) ;
#33548=CARTESIAN_POINT ( 'NONE',  ( 0.3398838260239651077, -1.651575993044620771, -0.3838325942033110061 ) ) ;
#33561=CARTESIAN_POINT ( 'NONE',  ( 0.4567505080237029280, -1.144430849087659352, -0.6312584490681862892 ) ) ;
#33567=CARTESIAN_POINT ( 'NONE',  ( 0.3870357883928292608, -1.780379272394887913, -0.5270016673789699180 ) ) ;
#33573=ORIENTED_EDGE ( 'NONE', *, *, #18232, .T. ) ;
#33574=CARTESIAN_POINT ( 'NONE',  ( 0.07465030803409943017, -1.408573555510644892, -0.6612025271909880431 ) ) ;
#33597=CARTESIAN_POINT ( 'NONE',  ( 0.3699999999999786793, -2.080243653848455665, -0.5192469000150281566 ) ) ;
#33598=AXIS2_PLACEMENT_3D ( 'NONE', #5349, #39935, #24309 ) ;
#33600=CARTESIAN_POINT ( 'NONE',  ( 0.1251191340379213812, -1.316096326284950324, -0.6814256523839956614 ) ) ;
#33604=CIRCLE ( 'NONE', #7310, 0.2500000000000000000 ) ;
#33608=CARTESIAN_POINT ( 'NONE',  ( 0.3610211414937801733, -1.953816409086856609, -0.6684869201605642131 ) ) ;
#33610=DIRECTION ( 'NONE',  ( 0.8660512985181132439, 0.4999551463232379533, 4.610901147014540750E-15 ) ) ;
#33612=ADVANCED_FACE ( 'NONE', ( #15806 ), #1614, .F. ) ;
#33615=ADVANCED_FACE ( 'NONE', ( #25280 ), #32185, .T. ) ;
#33623=EDGE_CURVE ( 'NONE', #23421, #27179, #429, .T. ) ;
#33624=CARTESIAN_POINT ( 'NONE',  ( 0.1985601496691580814, -2.023190444054567383, -0.2819993563027929917 ) ) ;
#33636=AXIS2_PLACEMENT_3D ( 'NONE', #1080, #38864, #26546 ) ;
#33647=CARTESIAN_POINT ( 'NONE',  ( 0.3912351814900760227, -1.953326783438015468, -0.4997197400164905545 ) ) ;
#33652=CARTESIAN_POINT ( 'NONE',  ( 0.02999999999997886302, -2.097675824466503691, -0.6968677163258658602 ) ) ;
#33659=CARTESIAN_POINT ( 'NONE',  ( 0.6169636335926310666, -1.622911811178471497, -0.5279922895341171429 ) ) ;
#33660=CARTESIAN_POINT ( 'NONE',  ( 0.08964076868335302262, -1.440626440711184619, -0.6869804198957685237 ) ) ;
#33662=CARTESIAN_POINT ( 'NONE',  ( 0.3829573361688640154, -1.749254992990724622, -0.4372965273082253246 ) ) ;
#33664=AXIS2_PLACEMENT_3D ( 'NONE', #17077, #1467, #1677 ) ;
#33668=CARTESIAN_POINT ( 'NONE',  ( 0.3626617637547003836, -1.756793103646928644, -0.5948424371531259025 ) ) ;
#33672=DIRECTION ( 'NONE',  ( 0.4999551463232372317, -0.8660512985181134660, 0.000000000000000000 ) ) ;
#33673=B_SPLINE_CURVE_WITH_KNOTS ( 'NONE', 3,
 ( #14571, #8201, #35781, #11504, #14179, #20564, #30208, #39670, #13763, #4499, #33096, #17062, #26744, #29607, #26329, #30026, #1853, #7593, #14368, #20168, #26932, #20361, #26535, #39074, #39465, #10899, #11290, #23859, #36382, #24071 ),
 .UNSPECIFIED., .F., .F.,
 ( 4, 2, 2, 2, 2, 2, 2, 2, 2, 2, 2, 2, 2, 2, 4 ),
 ( -5.999999999964222910E-08, 0.0003594096777401402550, 0.0007188793554802801536, 0.001437818710960556698, 0.002875697421921122581, 0.004313576132881688681, 0.005751454843842254347, 0.008627212265763385679, 0.01006509097672395221, 0.01150296968768451875, 0.01437872710960562753, 0.01725448453152673978, 0.02013024195344785203, 0.02156812066440840989, 0.02300599937536896428 ),
 .UNSPECIFIED. ) ;
#33674=B_SPLINE_SURFACE_WITH_KNOTS ( 'NONE', 3, 3, ( 
 ( #12516, #27754, #28163, #28, #15808, #34321, #12120, #24469, #3257, #12721 ),
 ( #28357, #24686, #40503, #25071, #25282, #21400, #19108, #16024, #37605, #31647 ),
 ( #33938, #37216, #9428, #18913, #37826, #18696, #37406, #22211, #6134, #9642 ),
 ( #21596, #2655, #5922, #18484, #31041, #22006, #28567, #37003, #34531, #227 ) ),
 .UNSPECIFIED., .F., .F., .F.,
 ( 4, 4 ),
 ( 4, 3, 3, 4 ),
 ( 0.3963327724766242399, 1.014871814752778434 ),
 ( -1.046553497504219397E-15, 0.4999999999999997224, 0.7500000000000001110, 1.000000000000000444 ),
 .UNSPECIFIED. ) ;
#33700=CARTESIAN_POINT ( 'NONE',  ( 0.4219866632171650478, -1.610104465087853765, -0.3647299066799348233 ) ) ;
#33705=CARTESIAN_POINT ( 'NONE',  ( 0.5718134511589890723, -1.573821939672337411, -0.4594826857674059739 ) ) ;
#33708=CARTESIAN_POINT ( 'NONE',  ( 0.5840964882222685617, -1.491811162635231058, -0.4356935235874836998 ) ) ;
#33719=DIRECTION ( 'NONE',  ( 0.000000000000000000, 0.000000000000000000, -1.000000000000000000 ) ) ;
#33724=DIRECTION ( 'NONE',  ( -0.8660512985181130219, -0.4999551463232377868, 0.000000000000000000 ) ) ;
#33725=ORIENTED_EDGE ( 'NONE', *, *, #29326, .T. ) ;
#33727=CIRCLE ( 'NONE', #37015, 0.01499999999999997689 ) ;
#33728=VERTEX_POINT ( 'NONE', #28248 ) ;
#33739=VERTEX_POINT ( 'NONE', #112 ) ;
#33753=( BOUNDED_SURFACE ( )  B_SPLINE_SURFACE ( 3, 2, ( 
 ( #31790, #25432, #574 ),
 ( #34862, #13069, #15344 ),
 ( #6671, #22546, #12450 ),
 ( #25621, #18633, #38153 ) ),
 .UNSPECIFIED., .F., .F., .T. ) 
 B_SPLINE_SURFACE_WITH_KNOTS ( ( 4, 4 ),
 ( 3, 3 ),
 ( -1.387778780781445676E-17, 0.001804009323275673022 ),
 ( 0.000000000000000000, 1.000000000000000000 ),
 .UNSPECIFIED. ) 
 GEOMETRIC_REPRESENTATION_ITEM ( )  RATIONAL_B_SPLINE_SURFACE ( (
 ( 1.000000000000000000, 0.7071067811865464625, 1.000000000000000000),
 ( 1.000000000000000000, 0.7071042723947947861, 1.000000000000000000),
 ( 1.000000000000000000, 0.7064338697126878452, 1.000000000000000000),
 ( 1.000000000000000000, 0.7053326528219889813, 1.000000000000000000) ) ) 
 REPRESENTATION_ITEM ( '' )  SURFACE ( )  );
#33758=CARTESIAN_POINT ( 'NONE',  ( 0.4170221576077899894, -1.703439424313293094, -0.4186838340555589233 ) ) ;
#33767=CARTESIAN_POINT ( 'NONE',  ( 0.3681092974666538842, -1.616496510625566208, -0.4182513407341701406 ) ) ;
#33779=CARTESIAN_POINT ( 'NONE',  ( 0.2629665421248923995, -1.157745397434066126, -0.5155029497116575543 ) ) ;
#33780=EDGE_CURVE ( 'NONE', #30237, #29543, #4297, .T. ) ;
#33781=CARTESIAN_POINT ( 'NONE',  ( 0.3761389819862501205, -1.668938135269312895, -0.4224620603250751616 ) ) ;
#33782=EDGE_LOOP ( 'NONE', ( #6964, #27249, #24812, #23134 ) ) ;
#33796=AXIS2_PLACEMENT_3D ( 'NONE', #12085, #33672, #5484 ) ;
#33803=VERTEX_POINT ( 'NONE', #38721 ) ;
#33811=ORIENTED_EDGE ( 'NONE', *, *, #34158, .F. ) ;
#33821=ADVANCED_FACE ( 'NONE', ( #29058 ), #5633, .T. ) ;
#33822=CARTESIAN_POINT ( 'NONE',  ( 0.5840964882222685617, -1.491811162635231058, -0.4356935235874836998 ) ) ;
#33824=AXIS2_PLACEMENT_3D ( 'NONE', #20675, #29712, #19849 ) ;
#33825=CARTESIAN_POINT ( 'NONE',  ( 0.06046277342610767436, -1.448078595047667116, -0.6496421378630458099 ) ) ;
#33834=LINE ( 'NONE', #15096, #22611 ) ;
#33840=DIRECTION ( 'NONE',  ( 0.2259631160204149669, 0.000000000000000000, 0.9741358581832129104 ) ) ;
#33851=CARTESIAN_POINT ( 'NONE',  ( 0.3573173253698222473, -1.879934324363079501, -0.3378928523157883612 ) ) ;
#33855=CARTESIAN_POINT ( 'NONE',  ( 0.2211959769661343000, -1.309495541150525799, -0.7462941026102624109 ) ) ;
#33856=ORIENTED_EDGE ( 'NONE', *, *, #25995, .F. ) ;
#33858=EDGE_LOOP ( 'NONE', ( #3455, #39463, #38954, #19034 ) ) ;
#33869=CARTESIAN_POINT ( 'NONE',  ( 0.3868936632023516897, -1.853519627552301152, -0.3097036711958909283 ) ) ;
#33879=CARTESIAN_POINT ( 'NONE',  ( 0.6300550326132239309, -1.371036769560420421, -0.6250000000000000000 ) ) ;
#33885=EDGE_CURVE ( 'NONE', #28931, #38085, #13823, .T. ) ;
#33887=CARTESIAN_POINT ( 'NONE',  ( 0.5822092398946240310, -1.604441550281183737, -0.4592476338510794176 ) ) ;
#33888=VECTOR ( 'NONE', #3284, 39.37007874015748143 ) ;
#33897=CARTESIAN_POINT ( 'NONE',  ( 0.4170115945640068822, -1.702980413955155425, -0.6123808887097256237 ) ) ;
#33898=EDGE_CURVE ( 'NONE', #24795, #21660, #20475, .T. ) ;
#33903=VERTEX_POINT ( 'NONE', #7662 ) ;
#33904=CARTESIAN_POINT ( 'NONE',  ( 0.1994740068363786423, -2.042640899752901085, -0.2765909798240093198 ) ) ;
#33924=AXIS2_PLACEMENT_3D ( 'NONE', #21581, #18072, #12106 ) ;
#33932=EDGE_CURVE ( 'NONE', #36711, #20307, #29804, .T. ) ;
#33938=CARTESIAN_POINT ( 'NONE',  ( 0.2490119727783751402, -1.333982754301515028, -0.7187326247832955817 ) ) ;
#33943=CARTESIAN_POINT ( 'NONE',  ( 0.5782730993802743802, -1.562463384465315519, -0.5918479448017719413 ) ) ;
#33947=CARTESIAN_POINT ( 'NONE',  ( 0.1960722456818422554, -1.288731303253010330, -0.2917126172454976296 ) ) ;
#33987=ORIENTED_EDGE ( 'NONE', *, *, #36869, .F. ) ;
#33992=ORIENTED_EDGE ( 'NONE', *, *, #11938, .T. ) ;
#34003=CIRCLE ( 'NONE', #40578, 0.01499999999999997342 ) ;
#34004=CARTESIAN_POINT ( 'NONE',  ( 0.2059273467974226113, -1.283046334493782359, -0.7462941026102624109 ) ) ;
#34022=CARTESIAN_POINT ( 'NONE',  ( 0.3673039290742221574, -2.033686460013540476, -0.5076811077424107088 ) ) ;
#34037=VERTEX_POINT ( 'NONE', #27205 ) ;
#34040=CARTESIAN_POINT ( 'NONE',  ( 0.3663529472107202034, -2.014034532710156533, -0.3144416355455260104 ) ) ;
#34042=DIRECTION ( 'NONE',  ( -0.4999551463232377313, 0.8660512985181132439, 0.000000000000000000 ) ) ;
#34056=CARTESIAN_POINT ( 'NONE',  ( 0.1655517683749154478, -1.273122889555738935, -0.2993625373774341791 ) ) ;
#34058=DIRECTION ( 'NONE',  ( 0.8660512985181134660, 0.4999551463232372317, 0.000000000000000000 ) ) ;
#34059=CARTESIAN_POINT ( 'NONE',  ( 0.1978993062382036205, -2.015598760273982215, -0.2839550029289699129 ) ) ;
#34071=CARTESIAN_POINT ( 'NONE',  ( 0.6417090595529835184, -1.440402100915940675, -0.4001723068962777519 ) ) ;
#34072=CARTESIAN_POINT ( 'NONE',  ( 0.03188314084667491499, -1.843474523003271415, -0.6753216049888512984 ) ) ;
#34076=ORIENTED_EDGE ( 'NONE', *, *, #9641, .F. ) ;
#34079=CARTESIAN_POINT ( 'NONE',  ( 0.3675360074875105854, -2.037884037106168389, -0.4877351960998094205 ) ) ;
#34080=CARTESIAN_POINT ( 'NONE',  ( 0.4258288446711951392, -1.697684769104331526, -0.6161890926816561143 ) ) ;
#34084=CARTESIAN_POINT ( 'NONE',  ( 0.5260973920207011600, -1.675551188159756677, -0.5699138614228782540 ) ) ;
#34092=CARTESIAN_POINT ( 'NONE',  ( 0.5304790502634055827, -1.600740321689024359, -0.5932381786332882045 ) ) ;
#34103=CARTESIAN_POINT ( 'NONE',  ( 0.2456699162554547011, -1.579418306085378143, -0.3207381830095928921 ) ) ;
#34108=VERTEX_POINT ( 'NONE', #24527 ) ;
#34114=CARTESIAN_POINT ( 'NONE',  ( 0.5934892211655993233, -1.486388914344519696, -0.3866566986715374021 ) ) ;
#34116=B_SPLINE_CURVE_WITH_KNOTS ( 'NONE', 3,
 ( #14814, #24282, #27565, #19329, #6960, #15818, #24893, #12951, #31052, #25299, #3082, #19119, #22413, #6544, #12336, #237, #6147, #34738, #27975, #18924, #18711, #35161, #6351, #34945, #22220, #37417 ),
 .UNSPECIFIED., .F., .F.,
 ( 4, 2, 2, 2, 2, 2, 2, 2, 2, 2, 2, 2, 4 ),
 ( 0.000000000000000000, 0.0008799450821173545071, 0.001759890164234709014, 0.002639835246352063847, 0.003519780328469418029, 0.004399725410586773078, 0.005279670492704127693, 0.007039560656938837792, 0.008799450821173547890, 0.01055934098540825886, 0.01231923114964296982, 0.01319917623176032444, 0.01407912131387767905 ),
 .UNSPECIFIED. ) ;
#34126=CARTESIAN_POINT ( 'NONE',  ( 0.5947987396514448077, -1.485632953921246946, -0.6449812926602518370 ) ) ;
#34128=CARTESIAN_POINT ( 'NONE',  ( 0.2011892967074957184, -1.251141541415955682, -0.7187326247832955817 ) ) ;
#34137=EDGE_CURVE ( 'NONE', #16545, #30897, #10720, .T. ) ;
#34141=EDGE_LOOP ( 'NONE', ( #7154, #14359, #18225, #7306, #29652, #3049, #28474, #30007, #22925, #19136 ) ) ;
#34146=CARTESIAN_POINT ( 'NONE',  ( 0.4915260346479126685, -1.695508583366576616, -0.4333519947141558637 ) ) ;
#34148=CARTESIAN_POINT ( 'NONE',  ( 0.2850999234409680172, -1.647721251208171367, -0.3633777075355690833 ) ) ;
#34152=CARTESIAN_POINT ( 'NONE',  ( 0.4660077270438260921, -1.088784338607927449, -0.4093149438083810154 ) ) ;
#34153=CARTESIAN_POINT ( 'NONE',  ( 0.3989031518297398993, -1.748978033746103833, -0.4505407471312883882 ) ) ;
#34158=EDGE_CURVE ( 'NONE', #31681, #40066, #28559, .T. ) ;
#34166=DIRECTION ( 'NONE',  ( 0.8660512985181134660, 0.4999551463232371207, 0.000000000000000000 ) ) ;
#34168=AXIS2_PLACEMENT_3D ( 'NONE', #1636, #10662, #38832 ) ;
#34190=CARTESIAN_POINT ( 'NONE',  ( 0.3321231534132307872, -1.664232048909226380, -0.6363989157131245689 ) ) ;
#34198=CIRCLE ( 'NONE', #22396, 0.01500000000000007057 ) ;
#34204=CIRCLE ( 'NONE', #11889, 0.1033070866141732325 ) ;
#34207=CARTESIAN_POINT ( 'NONE',  ( 0.4654635148381854326, -1.611437027087300855, -0.6524167923582313566 ) ) ;
#34211=CARTESIAN_POINT ( 'NONE',  ( 0.0005143298144824101203, -1.951520895201868111, -0.6590200376447251651 ) ) ;
#34215=CARTESIAN_POINT ( 'NONE',  ( 0.4758903444788569193, -1.092184862719652205, -0.4175441261731758780 ) ) ;
#34216=AXIS2_PLACEMENT_3D ( 'NONE', #14164, #39453, #23646 ) ;
#34217=CARTESIAN_POINT ( 'NONE',  ( 0.2349883165480021185, -1.593155449794408485, -0.6704283676663660430 ) ) ;
#34221=CIRCLE ( 'NONE', #17143, 0.1033070866141732880 ) ;
#34232=EDGE_LOOP ( 'NONE', ( #6035, #6112, #36825 ) ) ;
#34236=DIRECTION ( 'NONE',  ( -0.4999551463232311255, 0.8660512985181170187, 0.000000000000000000 ) ) ;
#34238=CARTESIAN_POINT ( 'NONE',  ( 0.3666869875394455636, -1.756572920003051541, -0.3440370208071864000 ) ) ;
#34239=CARTESIAN_POINT ( 'NONE',  ( -2.128333683970191216E-14, -2.097675824466503691, -0.2907100122647986451 ) ) ;
#34241=FACE_OUTER_BOUND ( 'NONE', #35171, .T. ) ;
#34250=CARTESIAN_POINT ( 'NONE',  ( 0.4262438152663738933, -1.592651821845863402, -0.6151431148613257793 ) ) ;
#34251=DIRECTION ( 'NONE',  ( 0.000000000000000000, -0.5295275951190198116, -0.8482927124568896415 ) ) ;
#34253=CARTESIAN_POINT ( 'NONE',  ( 0.3964264789023509428, -1.761207211030865194, -0.3116577597928051890 ) ) ;
#34262=DIRECTION ( 'NONE',  ( 0.8660512985181135770, 0.4999551463232370652, 0.000000000000000000 ) ) ;
#34268=CARTESIAN_POINT ( 'NONE',  ( 0.3264244126186546802, -1.294301107126978767, -0.5166151207188711680 ) ) ;
#34270=CARTESIAN_POINT ( 'NONE',  ( 0.6184362100440952137, -1.564428388872008746, -0.4403698313141179432 ) ) ;
#34272=CARTESIAN_POINT ( 'NONE',  ( 0.02999999999997886302, -2.107936428766274073, -0.2870436526301869962 ) ) ;
#34278=CARTESIAN_POINT ( 'NONE',  ( 0.4057297589136773519, -1.717105997358977065, -0.6044639876195223582 ) ) ;
#34280=AXIS2_PLACEMENT_3D ( 'NONE', #6730, #16224, #28560 ) ;
#34281=CARTESIAN_POINT ( 'NONE',  ( 0.5344271610666608829, -1.636795983080443051, -0.4842394454172543328 ) ) ;
#34282=CARTESIAN_POINT ( 'NONE',  ( 0.1323301854973741309, -1.244705972311918263, -0.5155029497116575543 ) ) ;
#34283=ORIENTED_EDGE ( 'NONE', *, *, #36099, .F. ) ;
#34294=ORIENTED_EDGE ( 'NONE', *, *, #5528, .F. ) ;
#34304=CARTESIAN_POINT ( 'NONE',  ( 0.4560259861529415981, -1.119845760975095139, -0.4237974160008213809 ) ) ;
#34309=ORIENTED_EDGE ( 'NONE', *, *, #14738, .T. ) ;
#34310=CARTESIAN_POINT ( 'NONE',  ( 0.2860007606812444703, -1.398056877809351839, -0.3144976166544465324 ) ) ;
#34312=CARTESIAN_POINT ( 'NONE',  ( -2.031982644102707652E-14, -2.061923090639281586, -0.3032530188522716830 ) ) ;
#34314=CARTESIAN_POINT ( 'NONE',  ( 0.5994069634879333197, -1.482972712863466436, -0.4086340618636334909 ) ) ;
#34321=CARTESIAN_POINT ( 'NONE',  ( 0.2397041043040182284, -1.887673249773291095, -0.6585554176240054902 ) ) ;
#34330=CARTESIAN_POINT ( 'NONE',  ( 0.5617906032868313915, -1.585432954525022531, -0.5313147025850599725 ) ) ;
#34348=AXIS2_PLACEMENT_3D ( 'NONE', #34268, #36559, #11666 ) ;
#34349=ORIENTED_EDGE ( 'NONE', *, *, #24543, .T. ) ;
#34354=DIRECTION ( 'NONE',  ( 0.4999551463232373427, -0.8660512985181134660, 0.000000000000000000 ) ) ;
#34358=VERTEX_POINT ( 'NONE', #15620 ) ;
#34360=DIRECTION ( 'NONE',  ( 0.8660512985181135770, 0.4999551463232370652, 0.000000000000000000 ) ) ;
#34369=FACE_OUTER_BOUND ( 'NONE', #4392, .T. ) ;
#34385=CARTESIAN_POINT ( 'NONE',  ( 0.5333644791322821321, -1.633651814608773734, -0.5988298493401544853 ) ) ;
#34406=ORIENTED_EDGE ( 'NONE', *, *, #8112, .T. ) ;
#34408=CIRCLE ( 'NONE', #8768, 0.1033070866141732325 ) ;
#34409=CARTESIAN_POINT ( 'NONE',  ( 0.3567375191406563784, -1.622233719184205336, -0.3666517953721947776 ) ) ;
#34412=DIRECTION ( 'NONE',  ( 1.000000000000000000, 0.000000000000000000, 0.000000000000000000 ) ) ;
#34414=VERTEX_POINT ( 'NONE', #7140 ) ;
#34428=CARTESIAN_POINT ( 'NONE',  ( 0.4688459138424372341, -1.061988423737608045, -0.4248180574663140141 ) ) ;
#34442=ORIENTED_EDGE ( 'NONE', *, *, #9958, .T. ) ;
#34448=B_SPLINE_CURVE_WITH_KNOTS ( 'NONE', 3,
 ( #20619, #17525, #27409, #11143 ),
 .UNSPECIFIED., .F., .F.,
 ( 4, 4 ),
 ( -6.000000000378846861E-08, 0.001468701496818329089 ),
 .UNSPECIFIED. ) ;
#34449=CARTESIAN_POINT ( 'NONE',  ( 0.3636045566369612292, -1.982526720389788721, -0.3214018419552013839 ) ) ;
#34450=CARTESIAN_POINT ( 'NONE',  ( 0.3711181956551158900, -1.768536140287003011, -0.5764455761630662423 ) ) ;
#34456=VERTEX_POINT ( 'NONE', #17225 ) ;
#34461=CARTESIAN_POINT ( 'NONE',  ( 0.4208456803029674287, -1.590742843837566811, -0.4148738790983051428 ) ) ;
#34465=CARTESIAN_POINT ( 'NONE',  ( 0.4018863715143964899, -1.731540629620808680, -0.3052291807102240906 ) ) ;
#34488=FACE_OUTER_BOUND ( 'NONE', #21925, .T. ) ;
#34493=CIRCLE ( 'NONE', #35789, 0.03000000000000003705 ) ;
#34496=CARTESIAN_POINT ( 'NONE',  ( 0.3868427017360319686, -1.755940305036085558, -0.5592542411036628414 ) ) ;
#34503=ORIENTED_EDGE ( 'NONE', *, *, #5884, .F. ) ;
#34513=CARTESIAN_POINT ( 'NONE',  ( 0.3568401510066848137, -1.627103573605686027, -0.3706434065951008661 ) ) ;
#34522=CARTESIAN_POINT ( 'NONE',  ( 0.6067096000040144155, -1.405345748401797712, -0.6250000000000000000 ) ) ;
#34523=CARTESIAN_POINT ( 'NONE',  ( 0.4688459138424372341, -1.061988423737608045, -0.4248180574663140141 ) ) ;
#34525=B_SPLINE_CURVE_WITH_KNOTS ( 'NONE', 3,
 ( #21005, #5553, #14006, #27397 ),
 .UNSPECIFIED., .F., .F.,
 ( 4, 4 ),
 ( 0.000000000000000000, 0.0003263726155882985011 ),
 .UNSPECIFIED. ) ;
#34531=CARTESIAN_POINT ( 'NONE',  ( -0.005948725901132238467, -2.039406408238342294, -0.6755655181501677431 ) ) ;
#34543=CARTESIAN_POINT ( 'NONE',  ( 0.5831586614430237514, -1.507066788378804478, -0.4433506751720494021 ) ) ;
#34544=CARTESIAN_POINT ( 'NONE',  ( 0.4311002502204824838, -1.610536115251105738, -0.3671355303406891313 ) ) ;
#34559=CARTESIAN_POINT ( 'NONE',  ( 0.5994846556772400747, -1.482927862621986392, -0.6371164520993247704 ) ) ;
#34578=CARTESIAN_POINT ( 'NONE',  ( -2.104403335822566002E-14, -2.101103024888176130, -0.2895076595251908080 ) ) ;
#34583=CARTESIAN_POINT ( 'NONE',  ( 0.2842326993136328195, -1.549395603922531617, -0.7208999815284821144 ) ) ;
#34584=DIRECTION ( 'NONE',  ( 0.8660512985181133550, 0.4999551463232372872, 0.000000000000000000 ) ) ;
#34585=EDGE_CURVE ( 'NONE', #2897, #36711, #19463, .T. ) ;
#34586=CARTESIAN_POINT ( 'NONE',  ( 0.1999999999999787226, -2.097675824466502803, -0.4688691127277801463 ) ) ;
#34592=PRODUCT_CONTEXT ( 'NONE', #18750, 'mechanical' ) ;
#34598=CARTESIAN_POINT ( 'NONE',  ( 0.3674440818730608238, -1.689157367836090273, -0.4373319235121027604 ) ) ;
#34600=CARTESIAN_POINT ( 'NONE',  ( 0.4469283285619459201, -1.099869350908816878, -0.4033480720695140631 ) ) ;
#34606=ORIENTED_EDGE ( 'NONE', *, *, #975, .T. ) ;
#34613=EDGE_CURVE ( 'NONE', #545, #10778, #25889, .T. ) ;
#34620=CARTESIAN_POINT ( 'NONE',  ( 0.3698249976192136135, -1.096058018356230734, -0.5155029497116575543 ) ) ;
#34625=DIRECTION ( 'NONE',  ( 0.8660512985181134660, 0.4999551463232372317, 0.000000000000000000 ) ) ;
#34627=ADVANCED_FACE ( 'NONE', ( #21350 ), #26534, .T. ) ;
#34631=EDGE_CURVE ( 'NONE', #40066, #13061, #37770, .T. ) ;
#34633=EDGE_CURVE ( 'NONE', #39255, #19455, #12597, .T. ) ;
#34642=CARTESIAN_POINT ( 'NONE',  ( 0.2075534016687414773, -1.285863081042195377, -0.3981962265531751588 ) ) ;
#34650=CARTESIAN_POINT ( 'NONE',  ( -2.112273405726188513E-14, -2.097675824466503691, -0.6968637352380161465 ) ) ;
#34652=CARTESIAN_POINT ( 'NONE',  ( 0.1995529058109177523, -2.050896138459941564, -0.3054326997595748217 ) ) ;
#34653=EDGE_CURVE ( 'NONE', #38249, #27529, #30457, .T. ) ;
#34656=CARTESIAN_POINT ( 'NONE',  ( -2.112273405726188513E-14, -2.097675824466503691, -0.7286991843995640483 ) ) ;
#34658=CARTESIAN_POINT ( 'NONE',  ( 0.3324871086615504012, -1.659137217475707304, -0.6399689536651966826 ) ) ;
#34676=EDGE_CURVE ( 'NONE', #12314, #19872, #17986, .T. ) ;
#34681=CARTESIAN_POINT ( 'NONE',  ( 0.6382086589690751932, -1.585474446196608600, -0.4355293602703178557 ) ) ;
#34687=CARTESIAN_POINT ( 'NONE',  ( 0.3616412802242882085, -1.759290408629955671, -0.5212859374497357257 ) ) ;
#34689=CARTESIAN_POINT ( 'NONE',  ( 0.3660631757498663541, -2.015934369490486322, -0.5042582106743112025 ) ) ;
#34693=CARTESIAN_POINT ( 'NONE',  ( 0.3794148853686062361, -1.617193962983704880, -0.6670239321470404770 ) ) ;
#34707=ORIENTED_EDGE ( 'NONE', *, *, #29288, .F. ) ;
#34726=DIRECTION ( 'NONE',  ( -0.9624590225244425978, 0.000000000000000000, 0.2714270251122657407 ) ) ;
#34731=EDGE_CURVE ( 'NONE', #11734, #29150, #16019, .T. ) ;
#34738=CARTESIAN_POINT ( 'NONE',  ( 0.1760929562092026501, -1.869776474524332821, -0.6851114302485398211 ) ) ;
#34749=ORIENTED_EDGE ( 'NONE', *, *, #38438, .F. ) ;
#34756=CARTESIAN_POINT ( 'NONE',  ( 0.3895888470569853768, -1.758301358926936730, -0.4737257729874836398 ) ) ;
#34782=DIRECTION ( 'NONE',  ( 0.7649703263416960386, 0.000000000000000000, 0.6440655244745516761 ) ) ;
#34790=B_SPLINE_CURVE_WITH_KNOTS ( 'NONE', 3,
 ( #8191, #33288, #17654, #14982, #36981, #18273, #9564, #14562, #22331, #27129, #33480, #34658 ),
 .UNSPECIFIED., .F., .F.,
 ( 4, 2, 2, 2, 2, 4 ),
 ( 5.485677294651095664E-18, 0.0005133272912129524610, 0.001026654582425899284, 0.002053309164851789027, 0.003079963747277678771, 0.004106618329703567646 ),
 .UNSPECIFIED. ) ;
#34791=CARTESIAN_POINT ( 'NONE',  ( 0.4862737308021083393, -1.680336247396838401, -0.4180171117579152273 ) ) ;
#34795=CARTESIAN_POINT ( 'NONE',  ( 0.5399038930177495477, -1.667580954481910904, -0.5371941175943450997 ) ) ;
#34797=ADVANCED_FACE ( 'NONE', ( #19658 ), #16937, .F. ) ;
#34799=CARTESIAN_POINT ( 'NONE',  ( 0.6226517055508813403, -1.619812196680018967, -0.5481868501644782121 ) ) ;
#34801=DIRECTION ( 'NONE',  ( -1.000000000000000000, -0.000000000000000000, -0.000000000000000000 ) ) ;
#34806=CARTESIAN_POINT ( 'NONE',  ( 0.6111238512687238167, -1.556616907971307473, -0.6228061396314235054 ) ) ;
#34813=CARTESIAN_POINT ( 'NONE',  ( 0.4296077269088026673, -1.643823256665882360, -0.6213498245139347231 ) ) ;
#34814=AXIS2_PLACEMENT_3D ( 'NONE', #27164, #17880, #8424 ) ;
#34824=DIRECTION ( 'NONE',  ( 0.8660512985181134660, 0.4999551463232372317, 0.000000000000000000 ) ) ;
#34825=EDGE_CURVE ( 'NONE', #7054, #17084, #16535, .T. ) ;
#34834=ORIENTED_EDGE ( 'NONE', *, *, #22319, .T. ) ;
#34840=AXIS2_PLACEMENT_3D ( 'NONE', #8230, #33326, #33515 ) ;
#34842=CARTESIAN_POINT ( 'NONE',  ( 0.1834964085430285941, -1.226715333008844055, -0.5155029497116575543 ) ) ;
#34854=ORIENTED_EDGE ( 'NONE', *, *, #13789, .T. ) ;
#34858=CARTESIAN_POINT ( 'NONE',  ( 0.5208586528260464865, -1.609295453103910090, -0.4933326546058600659 ) ) ;
#34862=CARTESIAN_POINT ( 'NONE',  ( 0.1999999999657006700, -2.081909887788347291, -0.7229608527333891699 ) ) ;
#34863=CARTESIAN_POINT ( 'NONE',  ( 0.4035771952761294523, -1.734704018191087549, -0.3063975415960173421 ) ) ;
#34870=B_SPLINE_CURVE_WITH_KNOTS ( 'NONE', 3,
 ( #10879, #9704, #37680, #22272, #9898, #19582, #22076, #3312, #38279, #16480 ),
 .UNSPECIFIED., .F., .F.,
 ( 4, 2, 2, 2, 4 ),
 ( 0.000000000000000000, 0.0003203988590849021789, 0.0006407977181698043577, 0.0009611965772547065908, 0.001281595436339608715 ),
 .UNSPECIFIED. ) ;
#34881=CARTESIAN_POINT ( 'NONE',  ( 0.4634865284762403892, -1.134362257022321518, -0.3648515278348755109 ) ) ;
#34895=CARTESIAN_POINT ( 'NONE',  ( 0.1909286924077257253, -1.257064795538239466, -0.7137159211901564770 ) ) ;
#34897=VECTOR ( 'NONE', #13519, 39.37007874015748854 ) ;
#34902=EDGE_CURVE ( 'NONE', #31681, #29245, #33834, .T. ) ;
#34911=FACE_OUTER_BOUND ( 'NONE', #6700, .T. ) ;
#34914=ORIENTED_EDGE ( 'NONE', *, *, #29900, .F. ) ;
#34917=ORIENTED_EDGE ( 'NONE', *, *, #16732, .F. ) ;
#34924=DIRECTION ( 'NONE',  ( 0.8660512985181139101, 0.4999551463232363990, 0.000000000000000000 ) ) ;
#34928=CARTESIAN_POINT ( 'NONE',  ( 0.3832704658403437992, -1.758002489716280259, -0.5572338524550815020 ) ) ;
#34931=CARTESIAN_POINT ( 'NONE',  ( 0.1988220064826623501, -2.042432882251850934, -0.7119240600711291833 ) ) ;
#34933=CARTESIAN_POINT ( 'NONE',  ( 0.3436341067576287323, -1.695284785612029443, -0.4149094092406203638 ) ) ;
#34936=EDGE_CURVE ( 'NONE', #9058, #18975, #26305, .T. ) ;
#34937=CARTESIAN_POINT ( 'NONE',  ( 0.4209912206648682154, -1.078067379053157193, -0.5155029497116575543 ) ) ;
#34939=ADVANCED_FACE ( 'NONE', ( #18384 ), #22478, .F. ) ;
#34943=CARTESIAN_POINT ( 'NONE',  ( 0.6004354142920773629, -1.537439897621929896, -0.4422550059529070654 ) ) ;
#34945=CARTESIAN_POINT ( 'NONE',  ( 0.1973311420822173867, -2.025401704179647933, -0.7077925230234759502 ) ) ;
#34955=ORIENTED_EDGE ( 'NONE', *, *, #160, .T. ) ;
#34965=B_SPLINE_CURVE_WITH_KNOTS ( 'NONE', 3,
 ( #36260, #18360, #26829, #36872, #23736, #33192 ),
 .UNSPECIFIED., .F., .F.,
 ( 4, 2, 4 ),
 ( 4.906538933386825900E-18, 0.0003977219821689530698, 0.0007954439643379011523 ),
 .UNSPECIFIED. ) ;
#34971=CARTESIAN_POINT ( 'NONE',  ( 0.1989976604547370465, -2.047409678865564686, -0.7132172901365274598 ) ) ;
#34985=CARTESIAN_POINT ( 'NONE',  ( 0.1742107032092684304, -1.802736856131804011, -0.6515483580219902926 ) ) ;
#34987=CARTESIAN_POINT ( 'NONE',  ( 0.2100859181409473475, -1.630899271293733355, -0.6615904437728673537 ) ) ;
#34990=CARTESIAN_POINT ( 'NONE',  ( 0.2914323826288400254, -1.233685883474753497, -0.5166151207188711680 ) ) ;
#34999=FACE_OUTER_BOUND ( 'NONE', #33241, .T. ) ;
#35001=VERTEX_POINT ( 'NONE', #19576 ) ;
#35013=CARTESIAN_POINT ( 'NONE',  ( 0.5747588096728203366, -1.612720233196342168, -0.5227372493886142113 ) ) ;
#35020=CARTESIAN_POINT ( 'NONE',  ( 0.4902907973143189047, -1.608820546470212109, -0.6381618420067222130 ) ) ;
#35027=CARTESIAN_POINT ( 'NONE',  ( 0.4320371192881574118, -1.117877429793240118, -0.3862585142794699444 ) ) ;
#35032=DIRECTION ( 'NONE',  ( -0.4999551463232377313, 0.8660512985181132439, -0.000000000000000000 ) ) ;
#35034=ADVANCED_FACE ( 'NONE', ( #7010 ), #8280, .T. ) ;
#35046=ORIENTED_EDGE ( 'NONE', *, *, #17337, .T. ) ;
#35052=ORIENTED_EDGE ( 'NONE', *, *, #36086, .F. ) ;
#35055=CARTESIAN_POINT ( 'NONE',  ( 0.3831477286273856087, -1.691467851574164127, -0.3353491032924195148 ) ) ;
#35069=CARTESIAN_POINT ( 'NONE',  ( 0.4680314439923284886, -1.633517906973578349, -0.4203363782011557692 ) ) ;
#35073=EDGE_CURVE ( 'NONE', #357, #12314, #7189, .T. ) ;
#35080=( BOUNDED_SURFACE ( )  B_SPLINE_SURFACE ( 3, 2, ( 
 ( #11960, #14423, #2514 ),
 ( #4968, #30694, #33767 ),
 ( #36842, #23923, #29883 ),
 ( #26990, #27418, #36654 ),
 ( #14240, #30265, #36453 ),
 ( #26804, #39330, #8875 ),
 ( #24524, #17535, #27601 ),
 ( #27204, #21025, #30084 ),
 ( #33548, #24317, #14853 ),
 ( #5358, #17920, #1912 ) ),
 .UNSPECIFIED., .F., .F., .T. ) 
 B_SPLINE_SURFACE_WITH_KNOTS ( ( 4, 2, 2, 2, 4 ),
 ( 3, 3 ),
 ( 0.002207820581699636471, 0.002505005507268364285, 0.002802190432837092099, 0.003099375358405819913, 0.003396560283974547727 ),
 ( 0.000000000000000000, 1.000000000000000000 ),
 .UNSPECIFIED. ) 
 GEOMETRIC_REPRESENTATION_ITEM ( )  RATIONAL_B_SPLINE_SURFACE ( (
 ( 1.000000000000000000, 0.5517613080878712717, 1.000000000000000000),
 ( 1.000000000000000000, 0.5512582163888796183, 1.000000000000000000),
 ( 1.000000000000000000, 0.5482345409571344197, 1.000000000000000000),
 ( 1.000000000000000000, 0.5377007643832122374, 1.000000000000000000),
 ( 1.000000000000000000, 0.5301184884994317725, 1.000000000000000000),
 ( 1.000000000000000000, 0.5117099482123855791, 1.000000000000000000),
 ( 1.000000000000000000, 0.5010294111536789385, 1.000000000000000000),
 ( 1.000000000000000000, 0.4783064819327327855, 1.000000000000000000),
 ( 1.000000000000000000, 0.4661873777990636625, 1.000000000000000000),
 ( 1.000000000000000000, 0.4546663607401262852, 1.000000000000000000) ) ) 
 REPRESENTATION_ITEM ( '' )  SURFACE ( )  );
#35082=AXIS2_PLACEMENT_3D ( 'NONE', #6311, #11870, #6096 ) ;
#35085=AXIS2_PLACEMENT_3D ( 'NONE', #14491, #27059, #4229 ) ;
#35087=DIRECTION ( 'NONE',  ( 0.2577569635876607590, 0.1487982532522210410, -0.9546834174485054891 ) ) ;
#35101=CARTESIAN_POINT ( 'NONE',  ( 0.4909801108973092520, -1.199306193601649362, -0.5155029497116575543 ) ) ;
#35107=DIRECTION ( 'NONE',  ( 0.4999551463232385085, -0.8660512985181127998, 0.000000000000000000 ) ) ;
#35110=DIRECTION ( 'NONE',  ( 0.8660512985181134660, 0.4999551463232373427, 0.000000000000000000 ) ) ;
#35111=DIRECTION ( 'NONE',  ( 0.4999551463232372317, -0.8660512985181135770, 0.000000000000000000 ) ) ;
#35113=ORIENTED_EDGE ( 'NONE', *, *, #24326, .T. ) ;
#35134=CARTESIAN_POINT ( 'NONE',  ( 0.3895823661253040027, -1.931635654259855173, -0.5036415101835181041 ) ) ;
#35135=CARTESIAN_POINT ( 'NONE',  ( 0.4806378395295556882, -1.105637800341302102, -0.6194292131661300882 ) ) ;
#35138=DIRECTION ( 'NONE',  ( 0.000000000000000000, 0.000000000000000000, -1.000000000000000000 ) ) ;
#35142=CARTESIAN_POINT ( 'NONE',  ( 0.3981442986168809428, -2.030926130361281334, -0.7104987781722165163 ) ) ;
#35145=CARTESIAN_POINT ( 'NONE',  ( 0.2011892967074957184, -1.251141541415955682, -0.7187326247832955817 ) ) ;
#35157=VECTOR ( 'NONE', #2766, 39.37007874015748143 ) ;
#35161=CARTESIAN_POINT ( 'NONE',  ( 0.1929609155355634653, -1.992353606873398020, -0.7010103324791125967 ) ) ;
#35162=PLANE ( 'NONE',  #13866 ) ;
#35165=CARTESIAN_POINT ( 'NONE',  ( 0.3757471142192235214, -1.766731021160328874, -0.5680748514784772496 ) ) ;
#35168=CARTESIAN_POINT ( 'NONE',  ( 0.3432713340272304237, -1.639810668526975324, -0.4375135453339642488 ) ) ;
#35171=EDGE_LOOP ( 'NONE', ( #30667, #20802, #11366, #31426, #13142, #24400 ) ) ;
#35173=ORIENTED_EDGE ( 'NONE', *, *, #37719, .T. ) ;
#35177=CARTESIAN_POINT ( 'NONE',  ( 0.5477732146854656925, -1.663038142904176730, -0.4856124366662120662 ) ) ;
#35183=CARTESIAN_POINT ( 'NONE',  ( 0.02145472682158336766, -1.629281619508914591, -0.3446454179893428948 ) ) ;
#35197=AXIS2_PLACEMENT_3D ( 'NONE', #8212, #17669, #17275 ) ;
#35205=CARTESIAN_POINT ( 'NONE',  ( 0.2084121485138739627, -1.634114042384106957, -0.6610165342446623349 ) ) ;
#35208=CARTESIAN_POINT ( 'NONE',  ( 0.4259076111796487041, -1.664108905841751085, -0.5318766032425232826 ) ) ;
#35212=CARTESIAN_POINT ( 'NONE',  ( 0.3650110843922287907, -1.763165835160773076, -0.5889551152805394540 ) ) ;
#35228=CARTESIAN_POINT ( 'NONE',  ( 0.6186988268989424000, -1.622094119273066681, -0.5291206216937438533 ) ) ;
#35230=DIRECTION ( 'NONE',  ( -0.4999551463232372317, 0.8660512985181135770, -0.000000000000000000 ) ) ;
#35236=CARTESIAN_POINT ( 'NONE',  ( 0.6278493015850613590, -1.616811722123548956, -0.5276078387414424586 ) ) ;
#35242=CARTESIAN_POINT ( 'NONE',  ( 0.5203574591657224024, -1.609584782789360125, -0.5401600205605632254 ) ) ;
#35263=VERTEX_POINT ( 'NONE', #34128 ) ;
#35270=FACE_OUTER_BOUND ( 'NONE', #33782, .T. ) ;
#35271=ORIENTED_EDGE ( 'NONE', *, *, #22661, .F. ) ;
#35277=CARTESIAN_POINT ( 'NONE',  ( 0.5462348416196847189, -1.594646255991501338, -0.4868944820179722521 ) ) ;
#35280=ORIENTED_EDGE ( 'NONE', *, *, #22736, .F. ) ;
#35291=B_SPLINE_SURFACE_WITH_KNOTS ( 'NONE', 3, 1, ( 
 ( #353, #31979 ),
 ( #15726, #28275 ),
 ( #9562, #6655 ),
 ( #34656, #561 ) ),
 .UNSPECIFIED., .F., .F., .F.,
 ( 4, 4 ),
 ( 2, 2 ),
 ( 0.000000000000000000, 1.000000000000000000 ),
 ( 0.000000000000000000, 1.000000000000000000 ),
 .UNSPECIFIED. ) ;
#35296=CARTESIAN_POINT ( 'NONE',  ( 0.5116966680315802041, -1.675313993414271341, -0.6001126952423705418 ) ) ;
#35311=ORIENTED_EDGE ( 'NONE', *, *, #6180, .T. ) ;
#35315=CARTESIAN_POINT ( 'NONE',  ( 0.6547994310234585003, -1.589707258511555255, -0.5155029497116575543 ) ) ;
#35331=ORIENTED_EDGE ( 'NONE', *, *, #5475, .F. ) ;
#35343=CARTESIAN_POINT ( 'NONE',  ( 0.3908699498952687423, -1.745013346922102748, -0.7175586304900263279 ) ) ;
#35344=FACE_OUTER_BOUND ( 'NONE', #12485, .T. ) ;
#35355=CARTESIAN_POINT ( 'NONE',  ( 0.5875654382963820810, -1.532386235059486346, -0.4097741950298078306 ) ) ;
#35358=CARTESIAN_POINT ( 'NONE',  ( 0.1991480113865206902, -2.054949600705703983, -0.6841806413415666421 ) ) ;
#35359=CARTESIAN_POINT ( 'NONE',  ( 0.2059260937967708482, -1.283047057827471082, -0.2869367607460444614 ) ) ;
#35360=ADVANCED_FACE ( 'NONE', ( #6350 ), #9841, .F. ) ;
#35362=EDGE_LOOP ( 'NONE', ( #28980, #10002, #26371, #2884 ) ) ;
#35364=EDGE_LOOP ( 'NONE', ( #710, #26455 ) ) ;
#35373=CARTESIAN_POINT ( 'NONE',  ( 0.6009178235190556494, -1.482100521748198396, -0.6278260014982935955 ) ) ;
#35376=ADVANCED_FACE ( 'NONE', ( #39642 ), #29163, .F. ) ;
#35378=CYLINDRICAL_SURFACE ( 'NONE', #2509, 0.04330708661417343591 ) ;
#35379=DIRECTION ( 'NONE',  ( 0.4999551463232372317, -0.8660512985181133550, 0.000000000000000000 ) ) ;
#35380=CARTESIAN_POINT ( 'NONE',  ( 0.09698018536738627071, -1.424165361423572751, -0.3353914638860537312 ) ) ;
#35393=B_SPLINE_CURVE_WITH_KNOTS ( 'NONE', 3,
 ( #39752, #32760, #14252, #10980, #17340, #29897, #11165, #20850, #1922, #30281, #33375, #9088 ),
 .UNSPECIFIED., .F., .F.,
 ( 4, 2, 2, 2, 2, 4 ),
 ( 0.001091185218850428823, 0.001968393139851580542, 0.002845601060852732261, 0.003722808981853884414, 0.004161412942354461575, 0.004600016902855039169 ),
 .UNSPECIFIED. ) ;
#35395=CARTESIAN_POINT ( 'NONE',  ( 0.4850543146008196027, -1.678681405600182641, -0.6440782542835996605 ) ) ;
#35396=CARTESIAN_POINT ( 'NONE',  ( 0.2127756690299808795, -1.279092926711003830, -0.7170389573829240026 ) ) ;
#35397=PRODUCT ( 'Lower Pivot Bracket', 'Lower Pivot Bracket', '', ( #34592 ) ) ;
#35398=CARTESIAN_POINT ( 'NONE',  ( 0.2011892967074957184, -1.251141541415955682, -0.3144976166544468099 ) ) ;
#35399=CARTESIAN_POINT ( 'NONE',  ( 0.1784765141246957565, -1.731228076122506954, -0.6515962173610828634 ) ) ;
#35405=ORIENTED_EDGE ( 'NONE', *, *, #18503, .F. ) ;
#35411=ORIENTED_EDGE ( 'NONE', *, *, #39666, .F. ) ;
#35416=CARTESIAN_POINT ( 'NONE',  ( 0.6180462672592140771, -1.622470829695115135, -0.5097172539320682372 ) ) ;
#35419=CYLINDRICAL_SURFACE ( 'NONE', #19850, 0.2500000000000000000 ) ;
#35421=ADVANCED_FACE ( 'NONE', ( #15578 ), #36394, .F. ) ;
#35423=CARTESIAN_POINT ( 'NONE',  ( 0.4058447956437031268, -1.613147253033901940, -0.3639822749465717600 ) ) ;
#35429=CARTESIAN_POINT ( 'NONE',  ( 0.3849858519270614177, -1.672779373200289132, -0.3639115729092421425 ) ) ;
#35434=CARTESIAN_POINT ( 'NONE',  ( 0.4564594823903532217, -1.083519075567892953, -0.6177465903673754477 ) ) ;
#35452=CARTESIAN_POINT ( 'NONE',  ( 0.1999999999999789724, -2.107936428766273629, -0.7005084057759867200 ) ) ;
#35453=CARTESIAN_POINT ( 'NONE',  ( 0.4259076111796464836, -1.664108905841752195, -0.4991292961807995421 ) ) ;
#35462=CARTESIAN_POINT ( 'NONE',  ( 0.5446426061928973938, -1.595565423594093035, -0.4737885531983786480 ) ) ;
#35466=UNCERTAINTY_MEASURE_WITH_UNIT (LENGTH_MEASURE( 1.000000000000000082E-05 ), #11616, 'distance_accuracy_value', 'NONE');
#35469=CARTESIAN_POINT ( 'NONE',  ( 0.3365215356197720498, -1.138376801642753788, -0.5155029497116575543 ) ) ;
#35470=DIRECTION ( 'NONE',  ( 0.8660512985181133550, 0.4999551463232372872, 0.000000000000000000 ) ) ;
#35487=CARTESIAN_POINT ( 'NONE',  ( 0.3564725003429615735, -1.740492809915490824, -0.4610359798238701234 ) ) ;
#35492=CARTESIAN_POINT ( 'NONE',  ( 0.3625960434667531151, -1.762758894398492204, -0.5926935080085831142 ) ) ;
#35493=CARTESIAN_POINT ( 'NONE',  ( 0.5641559342961582901, -1.318727562814529186, -0.4122610257295771796 ) ) ;
#35494=CARTESIAN_POINT ( 'NONE',  ( 0.1943568813818912500, -1.255085766440153350, -0.7153666819277929578 ) ) ;
#35498=CARTESIAN_POINT ( 'NONE',  ( 0.5752615338540276735, -1.540169966941223656, -0.5501209398761891523 ) ) ;
#35511=ADVANCED_FACE ( 'NONE', ( #34488 ), #29547, .F. ) ;
#35514=ORIENTED_EDGE ( 'NONE', *, *, #31346, .F. ) ;
#35515=CARTESIAN_POINT ( 'NONE',  ( 0.4845663548694630895, -1.649128766679687885, -0.4001533324282806059 ) ) ;
#35521=CIRCLE ( 'NONE', #9890, 0.05000000000000000971 ) ;
#35524=CARTESIAN_POINT ( 'NONE',  ( 0.3926032618789480622, -1.756026311479843782, -0.5284552501753819742 ) ) ;
#35527=CARTESIAN_POINT ( 'NONE',  ( 0.2219270030867450672, -1.605284576339639058, -0.6971167956771215923 ) ) ;
#35531=CARTESIAN_POINT ( 'NONE',  ( 0.6577877771461339007, -1.521478526558629918, -0.6177285882837185715 ) ) ;
#35538=CARTESIAN_POINT ( 'NONE',  ( 0.5866118575717673700, -1.567667628983530514, -0.4946522480570327285 ) ) ;
#35551=AXIS2_PLACEMENT_3D ( 'NONE', #22370, #19278, #38180 ) ;
#35553=CARTESIAN_POINT ( 'NONE',  ( 0.5776039811709874350, -1.609991024422577466, -0.4771844860517738818 ) ) ;
#35560=CARTESIAN_POINT ( 'NONE',  ( 0.3879575449432395851, -1.659955875966154126, -0.6176084244450640304 ) ) ;
#35562=CYLINDRICAL_SURFACE ( 'NONE', #4763, 0.1033070866141734129 ) ;
#35568=CARTESIAN_POINT ( 'NONE',  ( 0.01274160805156434109, -1.703734511057651835, -0.3678759453203773178 ) ) ;
#35573=CARTESIAN_POINT ( 'NONE',  ( 0.1999999999999789724, -2.097675824466503247, -0.7286991843995637153 ) ) ;
#35575=CARTESIAN_POINT ( 'NONE',  ( 0.3657412124346848259, -2.011863122366571055, -0.5036770633976842548 ) ) ;
#35589=B_SPLINE_CURVE_WITH_KNOTS ( 'NONE', 3,
 ( #21010, #26970, #11134, #2493, #30065, #1702, #39504, #15035, #27584, #14221 ),
 .UNSPECIFIED., .F., .F.,
 ( 4, 3, 3, 4 ),
 ( 0.002857558714824972711, 0.003238527401515360615, 0.003619527401515320545, 0.003619558715365647078 ),
 .UNSPECIFIED. ) ;
#35595=CARTESIAN_POINT ( 'NONE',  ( 0.3581651676567015330, -1.812542450072600841, -0.6671711558045307910 ) ) ;
#35606=ORIENTED_EDGE ( 'NONE', *, *, #5851, .T. ) ;
#35620=ORIENTED_EDGE ( 'NONE', *, *, #22365, .T. ) ;
#35626=CARTESIAN_POINT ( 'NONE',  ( 0.5039816396062418713, -1.584398255417020174, -0.4834617919644653150 ) ) ;
#35627=CARTESIAN_POINT ( 'NONE',  ( 0.2161879510971927432, -1.277123080371499242, -0.3144976166544468099 ) ) ;
#35631=EDGE_CURVE ( 'NONE', #28175, #2063, #29218, .T. ) ;
#35638=EDGE_CURVE ( 'NONE', #40101, #3578, #11423, .T. ) ;
#35640=DIRECTION ( 'NONE',  ( -0.8660512985181130219, -0.4999551463232378978, -3.305494428309464757E-15 ) ) ;
#35650=CARTESIAN_POINT ( 'NONE',  ( 0.7227111374362353846, -1.527409785822605448, -0.4111404562665418871 ) ) ;
#35656=CARTESIAN_POINT ( 'NONE',  ( 0.2209260011871197471, -1.309027873449325918, -0.6184399470714002645 ) ) ;
#35662=DIRECTION ( 'NONE',  ( 0.000000000000000000, 0.8951985963847274297, -0.4456674466806093138 ) ) ;
#35664=CARTESIAN_POINT ( 'NONE',  ( 0.3657108496600825487, -1.757413321709223375, -0.5058915056509059038 ) ) ;
#35689=CARTESIAN_POINT ( 'NONE',  ( 0.1909286924077254199, -1.257064795538238577, -0.7137147910238503812 ) ) ;
#35703=FACE_OUTER_BOUND ( 'NONE', #11315, .T. ) ;
#35722=CARTESIAN_POINT ( 'NONE',  ( 0.1886749731537993857, -1.710201859072882691, -0.3585638508453504181 ) ) ;
#35728=ORIENTED_EDGE ( 'NONE', *, *, #7152, .F. ) ;
#35733=CARTESIAN_POINT ( 'NONE',  ( -2.112273405726188513E-14, -2.097675824466503691, -0.6968637352380161465 ) ) ;
#35736=CARTESIAN_POINT ( 'NONE',  ( 0.3946758974465285896, -1.754660907246334833, -0.5213155647942423476 ) ) ;
#35741=DIRECTION ( 'NONE',  ( -0.000000000000000000, -0.9396926207859078728, -0.3420201433256705448 ) ) ;
#35751=CARTESIAN_POINT ( 'NONE',  ( 0.5909067581049517459, -1.559819890239460882, -0.5597400662906658608 ) ) ;
#35760=AXIS2_PLACEMENT_3D ( 'NONE', #602, #19076, #35110 ) ;
#35771=ORIENTED_EDGE ( 'NONE', *, *, #38152, .F. ) ;
#35772=DIRECTION ( 'NONE',  ( -0.8155480960843040084, -0.4959942097372370129, -0.2981124735404419579 ) ) ;
#35778=CARTESIAN_POINT ( 'NONE',  ( 0.09811733985272647063, -1.358709011939960964, -0.3562893400942814259 ) ) ;
#35781=CARTESIAN_POINT ( 'NONE',  ( 0.1831885191726025097, -1.261723239126609775, -0.7105730338104595534 ) ) ;
#35789=AXIS2_PLACEMENT_3D ( 'NONE', #23567, #20066, #11012 ) ;
#35794=CARTESIAN_POINT ( 'NONE',  ( 0.4370582351334127980, -1.114183277624516410, -0.6414096453823977528 ) ) ;
#35800=DIRECTION ( 'NONE',  ( 0.000000000000000000, 0.000000000000000000, -1.000000000000000000 ) ) ;
#35804=DIRECTION ( 'NONE',  ( 0.8660512985181135770, 0.4999551463232370652, 0.000000000000000000 ) ) ;
#35815=VECTOR ( 'NONE', #21890, 39.37007874015748854 ) ;
#35841=CARTESIAN_POINT ( 'NONE',  ( 0.4221466955848551250, -1.651713303066375760, -0.3505199372179519379 ) ) ;
#35844=CARTESIAN_POINT ( 'NONE',  ( 0.08402806910823619468, -1.261043216642898868, -0.5155029497116575543 ) ) ;
#35848=AXIS2_PLACEMENT_3D ( 'NONE', #19882, #35111, #6917 ) ;
#35856=DIRECTION ( 'NONE',  ( -0.4999551463232372317, 0.8660512985181134660, -0.000000000000000000 ) ) ;
#35859=EDGE_CURVE ( 'NONE', #22853, #39958, #18419, .T. ) ;
#35866=CARTESIAN_POINT ( 'NONE',  ( 0.2109795887149964189, -1.360945235397178044, -0.5155029497116575543 ) ) ;
#35867=EDGE_CURVE ( 'NONE', #37622, #24860, #38371, .T. ) ;
#35869=ORIENTED_EDGE ( 'NONE', *, *, #18964, .F. ) ;
#35871=CARTESIAN_POINT ( 'NONE',  ( 0.02997031417520805083, -2.054978514977984450, -0.7138428137902104176 ) ) ;
#35872=ORIENTED_EDGE ( 'NONE', *, *, #5390, .F. ) ;
#35902=CARTESIAN_POINT ( 'NONE',  ( 0.5026267308880598694, -1.652365288181674829, -0.5975130115846424284 ) ) ;
#35905=CARTESIAN_POINT ( 'NONE',  ( 0.7059656540691128246, -1.571716619208481935, -0.5155029497116575543 ) ) ;
#35918=DIRECTION ( 'NONE',  ( 0.8660512985181139101, 0.4999551463232363990, 0.000000000000000000 ) ) ;
#35920=CARTESIAN_POINT ( 'NONE',  ( 0.3688287100932481910, -1.620193688671676124, -0.3664956448573821746 ) ) ;
#35921=CARTESIAN_POINT ( 'NONE',  ( 0.3791840186072914509, -1.765062149505512545, -0.4492540378293045644 ) ) ;
#35925=CARTESIAN_POINT ( 'NONE',  ( 0.3624061103390691096, -1.968824918581854932, -0.4968426515055719972 ) ) ;
#35926=CARTESIAN_POINT ( 'NONE',  ( 0.5809658878212304867, -1.521239092202069321, -0.4539086719639525702 ) ) ;
#35928=CARTESIAN_POINT ( 'NONE',  ( 0.4278413765848551042, -1.120299553241070001, -0.3830631589809550541 ) ) ;
#35933=CARTESIAN_POINT ( 'NONE',  ( 0.4480646913441767576, -1.099213350020603386, -0.6275147848854656374 ) ) ;
#35934=CARTESIAN_POINT ( 'NONE',  ( 0.1811099676929339986, -1.851639177593427998, -0.3465146202863149671 ) ) ;
#35945=CARTESIAN_POINT ( 'NONE',  ( 0.4040087334063396374, -1.746030677407556908, -0.4508910978256960300 ) ) ;
#35947=DIRECTION ( 'NONE',  ( 0.4999551463232372317, -0.8660512985181133550, 0.000000000000000000 ) ) ;
#35952=CARTESIAN_POINT ( 'NONE',  ( 0.5807707845827529969, -1.606612587616919496, -0.5663761035934116173 ) ) ;
#35958=CARTESIAN_POINT ( 'NONE',  ( 0.5622555065282687226, -1.585093207106438973, -0.5030031773219529878 ) ) ;
#35959=CARTESIAN_POINT ( 'NONE',  ( 6.300911482189779063E-14, -2.091072893779495345, -0.2612338433542039096 ) ) ;
#35961=ADVANCED_FACE ( 'NONE', ( #12874 ), #33753, .T. ) ;
#35966=ORIENTED_EDGE ( 'NONE', *, *, #33520, .F. ) ;
#35969=ORIENTED_EDGE ( 'NONE', *, *, #22279, .F. ) ;
#35971=CARTESIAN_POINT ( 'NONE',  ( 0.6324675381817486119, -1.498808774185486525, -0.3951404225454540065 ) ) ;
#35977=ORIENTED_EDGE ( 'NONE', *, *, #34676, .F. ) ;
#35978=CARTESIAN_POINT ( 'NONE',  ( 0.5312361872299876664, -1.568664717035958001, -0.4868944820179721966 ) ) ;
#35982=CARTESIAN_POINT ( 'NONE',  ( 0.1991480113865258528, -2.054949600705707091, -0.6841806413415671972 ) ) ;
#35983=ORIENTED_EDGE ( 'NONE', *, *, #38638, .F. ) ;
#35993=CARTESIAN_POINT ( 'NONE',  ( 0.4234909963964844648, -1.082397635545747638, -0.5155029497116575543 ) ) ;
#35999=CARTESIAN_POINT ( 'NONE',  ( 0.1879272134313860199, -1.251865459589703633, -0.4009530412211869121 ) ) ;
#36001=DIRECTION ( 'NONE',  ( 0.000000000000000000, 0.000000000000000000, -1.000000000000000000 ) ) ;
#36002=CARTESIAN_POINT ( 'NONE',  ( 0.4897592102757906130, -1.696528537887749932, -0.5984293649392183889 ) ) ;
#36005=DIRECTION ( 'NONE',  ( -0.8660512985181132439, -0.4999551463232375093, 0.000000000000000000 ) ) ;
#36010=CARTESIAN_POINT ( 'NONE',  ( 0.4617378601122623105, -1.664140217285515089, -0.4140004630914397299 ) ) ;
#36019=DIRECTION ( 'NONE',  ( 0.8660512985181134660, 0.4999551463232372317, 0.000000000000000000 ) ) ;
#36021=CARTESIAN_POINT ( 'NONE',  ( 0.6213189662415743442, -1.606914084853001246, -0.4645767070828071277 ) ) ;
#36026=B_SPLINE_CURVE_WITH_KNOTS ( 'NONE', 3,
 ( #38267, #12784, #1085, #25962, #32107, #7392, #16677, #3521, #35205, #9885, #29229, #16284, #22459, #32295, #37882, #34985, #16472, #6793, #19377, #9697, #31911, #7007, #3730, #10317, #3914, #29014 ),
 .UNSPECIFIED., .F., .F.,
 ( 4, 2, 2, 2, 2, 2, 2, 2, 2, 2, 2, 2, 4 ),
 ( 0.000000000000000000, 0.0009027245942062626840, 0.001805449188412525368, 0.002708173782618787835, 0.003610898376825050736, 0.004513622971031313637, 0.005416347565237575670, 0.007221796753650082390, 0.009027245942062589110, 0.01083269513047509409, 0.01263814431888760081, 0.01354086891309385157, 0.01444359350730010406 ),
 .UNSPECIFIED. ) ;
#36032=CARTESIAN_POINT ( 'NONE',  ( 0.4699303087857425454, -1.591526288972971992, -0.4356248681750835017 ) ) ;
#36034=CARTESIAN_POINT ( 'NONE',  ( 0.4109940520397017960, -1.749134648671465619, -0.4344985177731692239 ) ) ;
#36035=CARTESIAN_POINT ( 'NONE',  ( 0.3656312763845015468, -1.616885411836818998, -0.3263777939557699903 ) ) ;
#36039=CARTESIAN_POINT ( 'NONE',  ( 0.1999999999999789724, -2.183180860297921466, -0.7137760292030871367 ) ) ;
#36042=DIRECTION ( 'NONE',  ( 0.8660512985181133550, 0.4999551463232372872, 0.000000000000000000 ) ) ;
#36044=EDGE_CURVE ( 'NONE', #19627, #556, #21938, .T. ) ;
#36052=CARTESIAN_POINT ( 'NONE',  ( 0.4186432780919981389, -1.612034538517056692, -0.6668481824684691084 ) ) ;
#36053=DIRECTION ( 'NONE',  ( 1.060606950627616773E-16, 6.122684696619993730E-17, 1.000000000000000000 ) ) ;
#36056=CARTESIAN_POINT ( 'NONE',  ( 0.1739430406544926755, -1.555536796503983243, -0.6758258725061466743 ) ) ;
#36060=FACE_OUTER_BOUND ( 'NONE', #27081, .T. ) ;
#36066=CARTESIAN_POINT ( 'NONE',  ( 0.08761651290939830028, -1.378853951282039469, -0.6937690615011236073 ) ) ;
#36068=CARTESIAN_POINT ( 'NONE',  ( 0.3569902980463470765, -1.891667118059767283, -0.4992937296425578042 ) ) ;
#36072=ORIENTED_EDGE ( 'NONE', *, *, #36044, .T. ) ;
#36074=EDGE_CURVE ( 'NONE', #24795, #31373, #23336, .T. ) ;
#36086=EDGE_CURVE ( 'NONE', #28931, #7674, #6596, .T. ) ;
#36099=EDGE_CURVE ( 'NONE', #23099, #13465, #21994, .T. ) ;
#36134=CARTESIAN_POINT ( 'NONE',  ( 0.3902882956839560658, -1.753951228373453519, -0.4725945316380958383 ) ) ;
#36139=CARTESIAN_POINT ( 'NONE',  ( 0.6182991044115986323, -1.621655261782950941, -0.4927229840283234297 ) ) ;
#36147=CARTESIAN_POINT ( 'NONE',  ( 0.5986005277559497406, -1.542134511451966672, -0.4467108566020089877 ) ) ;
#36158=ORIENTED_EDGE ( 'NONE', *, *, #33145, .T. ) ;
#36167=ORIENTED_EDGE ( 'NONE', *, *, #28582, .F. ) ;
#36172=CARTESIAN_POINT ( 'NONE',  ( 0.4584717390208091770, -1.703043547193807017, -0.5155029497116575543 ) ) ;
#36181=CARTESIAN_POINT ( 'NONE',  ( -2.115421433687637455E-14, -2.107936428766274073, -0.7005084057759867200 ) ) ;
#36194=CYLINDRICAL_SURFACE ( 'NONE', #27779, 0.2200000000000000566 ) ;
#36198=CARTESIAN_POINT ( 'NONE',  ( 0.3626185512632494334, -1.769924452066289122, -0.5899438298025727612 ) ) ;
#36218=TOROIDAL_SURFACE ( 'NONE', #764, 0.08830708661417323302, 0.01499999999999999944 ) ;
#36223=DIRECTION ( 'NONE',  ( 0.000000000000000000, 0.000000000000000000, 1.000000000000000000 ) ) ;
#36236=CARTESIAN_POINT ( 'NONE',  ( 0.3999999999999788169, -2.097675824466504135, -0.4688691127277798687 ) ) ;
#36249=CARTESIAN_POINT ( 'NONE',  ( 0.08495623427412302142, -1.462573956620219828, -0.6626765092577833194 ) ) ;
#36253=CARTESIAN_POINT ( 'NONE',  ( 0.3895837468212401400, -1.765804909494755437, -0.5282886827880538538 ) ) ;
#36259=CARTESIAN_POINT ( 'NONE',  ( 0.02130150994101746853, -1.626723050439328855, -0.6382336971175220919 ) ) ;
#36260=CARTESIAN_POINT ( 'NONE',  ( 0.6400160853294423191, -1.459529829645036081, -0.3976988710621562895 ) ) ;
#36264=ORIENTED_EDGE ( 'NONE', *, *, #26606, .T. ) ;
#36265=CARTESIAN_POINT ( 'NONE',  ( 0.5474628067970259693, -1.166699794256029987, -0.6317669042598009765 ) ) ;
#36281=DIRECTION ( 'NONE',  ( 0.4999551463232373427, -0.8660512985181134660, 0.000000000000000000 ) ) ;
#36282=CIRCLE ( 'NONE', #8706, 0.03000000000000003011 ) ;
#36284=CARTESIAN_POINT ( 'NONE',  ( 0.1763210608552490954, -1.872198378222803106, -0.6852895742237601340 ) ) ;
#36297=CARTESIAN_POINT ( 'NONE',  ( 0.1424029337235096226, -1.400533250147911746, -0.6250000000000000000 ) ) ;
#36300=ORIENTED_EDGE ( 'NONE', *, *, #37649, .T. ) ;
#36304=TOROIDAL_SURFACE ( 'NONE', #4762, 0.04999999999999998196, 0.1700000000000000400 ) ;
#36305=CARTESIAN_POINT ( 'NONE',  ( 0.4000323062371948235, -1.610924870193226388, -0.3620271583837152418 ) ) ;
#36307=CARTESIAN_POINT ( 'NONE',  ( 0.1901749068777572604, -1.944933594392276088, -0.3001565292664163942 ) ) ;
#36311=CARTESIAN_POINT ( 'NONE',  ( 0.1734973056165642902, -1.209394307038482497, -0.5155029497116575543 ) ) ;
#36326=ORIENTED_EDGE ( 'NONE', *, *, #18291, .T. ) ;
#36335=CARTESIAN_POINT ( 'NONE',  ( 0.3639973713284520018, -1.769128485143046436, -0.4349400384763179583 ) ) ;
#36346=CARTESIAN_POINT ( 'NONE',  ( 0.6269135997112185166, -1.610086856713869308, -0.5704037409038575923 ) ) ;
#36353=CARTESIAN_POINT ( 'NONE',  ( 0.5756165940928597013, -1.567873191104453223, -0.5835715271696909623 ) ) ;
#36357=EDGE_CURVE ( 'NONE', #19345, #10240, #24267, .T. ) ;
#36359=CARTESIAN_POINT ( 'NONE',  ( 0.3625960434667522825, -1.762758894398491760, -0.5926935080085824481 ) ) ;
#36361=CARTESIAN_POINT ( 'NONE',  ( 0.6079668211846660508, -1.561367219176452714, -0.4113520219294763969 ) ) ;
#36382=CARTESIAN_POINT ( 'NONE',  ( -7.709217208076694605E-10, -2.079844940525741315, -0.6906928555465188246 ) ) ;
#36383=FACE_OUTER_BOUND ( 'NONE', #20821, .T. ) ;
#36384=ADVANCED_FACE ( 'NONE', ( #25574 ), #12212, .F. ) ;
#36394=( BOUNDED_SURFACE ( )  B_SPLINE_SURFACE ( 3, 2, ( 
 ( #21356, #8566, #33897 ),
 ( #5696, #11675, #30797 ),
 ( #2617, #5271, #40041 ),
 ( #5881, #21559, #17831 ),
 ( #12289, #27712, #24845 ),
 ( #21139, #31214, #34278 ),
 ( #40246, #37367, #9178 ),
 ( #39855, #12083, #2224 ),
 ( #11475, #21745, #24644 ),
 ( #24232, #18656, #14761 ),
 ( #33668, #24042, #36755 ),
 ( #36570, #8375, #5482 ) ),
 .UNSPECIFIED., .F., .F., .T. ) 
 B_SPLINE_SURFACE_WITH_KNOTS ( ( 4, 2, 2, 2, 2, 4 ),
 ( 3, 3 ),
 ( 0.000000000000000000, 0.0002379057407600430744, 0.0004758114815200861487, 0.0009516229630401722974, 0.001427434444560258392, 0.001903245926080344595 ),
 ( 0.000000000000000000, 1.000000000000000000 ),
 .UNSPECIFIED. ) 
 GEOMETRIC_REPRESENTATION_ITEM ( )  RATIONAL_B_SPLINE_SURFACE ( (
 ( 1.000000000000000000, 0.8659230874819799917, 1.000000000000000000),
 ( 1.000000000000000000, 0.8654830159531572420, 1.000000000000000000),
 ( 1.000000000000000000, 0.8634833282782717889, 1.000000000000000000),
 ( 1.000000000000000000, 0.8560673753524404850, 1.000000000000000000),
 ( 1.000000000000000000, 0.8505305545019991031, 1.000000000000000000),
 ( 1.000000000000000000, 0.8302514985868648667, 1.000000000000000000),
 ( 1.000000000000000000, 0.8122569203425941131, 1.000000000000000000),
 ( 1.000000000000000000, 0.7769176656627446720, 1.000000000000000000),
 ( 1.000000000000000000, 0.7592262555998681162, 1.000000000000000000),
 ( 1.000000000000000000, 0.7244430868634086362, 1.000000000000000000),
 ( 1.000000000000000000, 0.7073027160842355610, 1.000000000000000000),
 ( 1.000000000000000000, 0.6906290772346568296, 1.000000000000000000) ) ) 
 REPRESENTATION_ITEM ( '' )  SURFACE ( )  );
#36409=CARTESIAN_POINT ( 'NONE',  ( 0.3939420568793829402, -1.988526800673050321, -0.5001229575649985826 ) ) ;
#36427=CARTESIAN_POINT ( 'NONE',  ( 0.2059273467974227778, -1.283046334493782359, -0.7137159211901564770 ) ) ;
#36430=CARTESIAN_POINT ( 'NONE',  ( 0.3516101416147200953, -1.741639419776285891, -0.7019724635597545115 ) ) ;
#36445=FACE_OUTER_BOUND ( 'NONE', #18064, .T. ) ;
#36447=ADVANCED_FACE ( 'NONE', ( #28855 ), #24633, .T. ) ;
#36453=CARTESIAN_POINT ( 'NONE',  ( 0.3583927816463333693, -1.622105672670009380, -0.4230600629973198523 ) ) ;
#36463=CARTESIAN_POINT ( 'NONE',  ( 0.3894066849061866842, -1.614605012626642910, -0.6684378029408698518 ) ) ;
#36466=ORIENTED_EDGE ( 'NONE', *, *, #19064, .F. ) ;
#36467=CARTESIAN_POINT ( 'NONE',  ( 0.1999999999999788058, -2.097675824466502803, -0.7286991843995631601 ) ) ;
#36471=CARTESIAN_POINT ( 'NONE',  ( 0.3712243616927410894, -1.761250189250869180, -0.4316674211170486442 ) ) ;
#36479=CARTESIAN_POINT ( 'NONE',  ( 0.09016133453268133924, -1.373701387894656900, -0.6687768065943457962 ) ) ;
#36486=DIRECTION ( 'NONE',  ( -0.8660512985181132439, -0.4999551463232374537, 0.000000000000000000 ) ) ;
#36491=FACE_OUTER_BOUND ( 'NONE', #4177, .T. ) ;
#36495=AXIS2_PLACEMENT_3D ( 'NONE', #7375, #26933, #4500 ) ;
#36499=FACE_OUTER_BOUND ( 'NONE', #6512, .T. ) ;
#36505=CARTESIAN_POINT ( 'NONE',  ( 0.2498074192101490676, -1.572794153342251811, -0.7074376191508968681 ) ) ;
#36512=CARTESIAN_POINT ( 'NONE',  ( 0.3683934783552571535, -2.038992781902201124, -0.6813765817288593984 ) ) ;
#36519=LINE ( 'NONE', #1788, #39689 ) ;
#36521=CIRCLE ( 'NONE', #12215, 0.01500000000000001159 ) ;
#36523=EDGE_LOOP ( 'NONE', ( #23447, #25501, #26479, #11227, #31384, #38839, #21776, #6811, #4253 ) ) ;
#36537=DIRECTION ( 'NONE',  ( 0.8660512985181132439, 0.4999551463232376758, 0.000000000000000000 ) ) ;
#36542=EDGE_LOOP ( 'NONE', ( #10771, #17964, #15025, #32863, #30196, #25933, #27639 ) ) ;
#36544=CARTESIAN_POINT ( 'NONE',  ( 0.1791084308631172295, -1.789643132935252234, -0.3232808063848631175 ) ) ;
#36548=CARTESIAN_POINT ( 'NONE',  ( 0.3999999999999786504, -2.120723258816476609, -0.4622723469118392714 ) ) ;
#36551=CARTESIAN_POINT ( 'NONE',  ( 0.3957373257482387774, -1.750805605674629950, -0.5219666508750002709 ) ) ;
#36559=DIRECTION ( 'NONE',  ( -0.4999551463232377313, 0.8660512985181132439, 0.000000000000000000 ) ) ;
#36561=ADVANCED_FACE ( 'NONE', ( #27410 ), #26689, .F. ) ;
#36562=CARTESIAN_POINT ( 'NONE',  ( 0.6010837949887281040, -1.596314856062887921, -0.5078772351678970676 ) ) ;
#36563=CARTESIAN_POINT ( 'NONE',  ( 0.4676588494100126780, -1.684644990138186804, -0.6179151535550295726 ) ) ;
#36568=CARTESIAN_POINT ( 'NONE',  ( 0.4909801108973092520, -1.199306193601649362, -0.5155029497116575543 ) ) ;
#36570=CARTESIAN_POINT ( 'NONE',  ( 0.3625898815820082222, -1.763258591188420210, -0.5925135466911359838 ) ) ;
#36574=CARTESIAN_POINT ( 'NONE',  ( 0.4672376269229551182, -1.092478783799717856, -0.6267157269568994771 ) ) ;
#36585=ORIENTED_EDGE ( 'NONE', *, *, #22686, .T. ) ;
#36601=LINE ( 'NONE', #39889, #25988 ) ;
#36602=B_SPLINE_CURVE_WITH_KNOTS ( 'NONE', 3,
 ( #34971, #37867, #9684, #35573 ),
 .UNSPECIFIED., .F., .F.,
 ( 4, 4 ),
 ( 0.000000000000000000, 0.001336189563664358891 ),
 .UNSPECIFIED. ) ;
#36604=ADVANCED_FACE ( 'NONE', ( #36445 ), #11464, .F. ) ;
#36615=EDGE_LOOP ( 'NONE', ( #37126, #34914, #35983, #2934 ) ) ;
#36640=EDGE_LOOP ( 'NONE', ( #31273, #19831, #27238, #8298 ) ) ;
#36647=CARTESIAN_POINT ( 'NONE',  ( -2.119743302583864240E-14, -2.107936428766274073, -0.7005084057759867200 ) ) ;
#36648=FACE_OUTER_BOUND ( 'NONE', #1473, .T. ) ;
#36652=CARTESIAN_POINT ( 'NONE',  ( 0.1995529058109188070, -2.050896138459942009, -0.3054326997595750992 ) ) ;
#36654=CARTESIAN_POINT ( 'NONE',  ( 0.3607508412325427516, -1.620744409234910144, -0.4217444633269712417 ) ) ;
#36657=CARTESIAN_POINT ( 'NONE',  ( 0.2059273467974228333, -1.283046334493783025, -0.7462941026102624109 ) ) ;
#36665=CARTESIAN_POINT ( 'NONE',  ( 0.3577318113308060599, -1.744272611056911781, -0.4663113921787143124 ) ) ;
#36672=CARTESIAN_POINT ( 'NONE',  ( 0.3815368266015244925, -1.759003287083134692, -0.4522571440127258202 ) ) ;
#36680=CARTESIAN_POINT ( 'NONE',  ( 0.001006207230660943319, -1.919904431792509136, -0.6546587980846723109 ) ) ;
#36682=CARTESIAN_POINT ( 'NONE',  ( 0.3649706973909825347, -1.747755802025040328, -0.5186209711425785462 ) ) ;
#36695=ORIENTED_EDGE ( 'NONE', *, *, #24615, .T. ) ;
#36702=CARTESIAN_POINT ( 'NONE',  ( 0.4351352655241935152, -1.693421934718205124, -0.5229744562079222669 ) ) ;
#36707=CARTESIAN_POINT ( 'NONE',  ( 0.3638603365242920051, -1.988569641414750233, -0.6726323697083436137 ) ) ;
#36711=VERTEX_POINT ( 'NONE', #6997 ) ;
#36712=DIRECTION ( 'NONE',  ( 0.4999551463232373427, -0.8660512985181134660, 0.000000000000000000 ) ) ;
#36713=DIRECTION ( 'NONE',  ( 0.8660512985181135770, 0.4999551463232370652, 1.983296656985675225E-15 ) ) ;
#36728=DIRECTION ( 'NONE',  ( 0.000000000000000000, 0.000000000000000000, -1.000000000000000000 ) ) ;
#36729=ORIENTED_EDGE ( 'NONE', *, *, #247, .F. ) ;
#36732=CARTESIAN_POINT ( 'NONE',  ( 0.3288726549063353266, -1.639147087365691036, -0.4090903646187450948 ) ) ;
#36736=VERTEX_POINT ( 'NONE', #23051 ) ;
#36737=CARTESIAN_POINT ( 'NONE',  ( 0.3990412541384849576, -2.061965117970526951, -0.4759812377563777397 ) ) ;
#36739=CARTESIAN_POINT ( 'NONE',  ( -2.112273405726188513E-14, -2.097675824466503691, -0.6968677163258658602 ) ) ;
#36743=CARTESIAN_POINT ( 'NONE',  ( 0.6413879784614744395, -1.405912376546664122, -0.6250000000000000000 ) ) ;
#36746=CARTESIAN_POINT ( 'NONE',  ( 0.3867386822597077001, -1.692088203187593898, -0.6206395857499010793 ) ) ;
#36748=CARTESIAN_POINT ( 'NONE',  ( 0.5959760379479978054, -1.584574879541716941, -0.6027336449407405539 ) ) ;
#36749=CARTESIAN_POINT ( 'NONE',  ( 0.03318190567315884576, -1.808085944443767579, -0.6722552504361505310 ) ) ;
#36755=CARTESIAN_POINT ( 'NONE',  ( 0.4046838182303809650, -1.753375371334861654, -0.5898849750082092447 ) ) ;
#36764=CARTESIAN_POINT ( 'NONE',  ( 0.2914323826288400254, -1.233685883474753497, -0.5166151207188711680 ) ) ;
#36765=ORIENTED_EDGE ( 'NONE', *, *, #23537, .T. ) ;
#36769=CARTESIAN_POINT ( 'NONE',  ( 0.05332459779802017213, -1.470191566866195121, -0.3710607107473925526 ) ) ;
#36770=ORIENTED_EDGE ( 'NONE', *, *, #25584, .F. ) ;
#36776=EDGE_CURVE ( 'NONE', #17453, #23598, #25721, .T. ) ;
#36785=CARTESIAN_POINT ( 'NONE',  ( 0.6473787150721044270, -1.455279521797666176, -0.6250000000000000000 ) ) ;
#36786=DIRECTION ( 'NONE',  ( 0.4999551463232372317, -0.8660512985181133550, 0.000000000000000000 ) ) ;
#36793=DIRECTION ( 'NONE',  ( 1.000000000000000000, 0.000000000000000000, 0.000000000000000000 ) ) ;
#36799=CARTESIAN_POINT ( 'NONE',  ( 0.5651833292478160020, -1.583037129094509998, -0.5461299182969832078 ) ) ;
#36804=CARTESIAN_POINT ( 'NONE',  ( 0.4909801108973092520, -1.199306193601649362, -0.5155029497116575543 ) ) ;
#36822=EDGE_CURVE ( 'NONE', #38602, #32180, #36601, .T. ) ;
#36825=ORIENTED_EDGE ( 'NONE', *, *, #39112, .T. ) ;
#36826=ORIENTED_EDGE ( 'NONE', *, *, #15742, .T. ) ;
#36834=CARTESIAN_POINT ( 'NONE',  ( 0.3878387718074795543, -1.722808031660705508, -0.4381220887401267583 ) ) ;
#36842=CARTESIAN_POINT ( 'NONE',  ( 0.3545087897290576384, -1.628856737622770723, -0.3716332584104992676 ) ) ;
#36845=B_SPLINE_CURVE_WITH_KNOTS ( 'NONE', 3,
 ( #26747, #23659, #17863, #17268, #30211, #27144, #1660, #2042, #30428, #14183, #11099, #9028, #6335, #18288, #27744, #40071, #12509, #21589, #31030, #18081, #37598, #9213, #5518, #30635, #34312, #18907 ),
 .UNSPECIFIED., .F., .F.,
 ( 4, 2, 2, 2, 2, 2, 2, 2, 2, 2, 2, 2, 4 ),
 ( 0.007586643537693086789, 0.008316112212441773011, 0.009045580887190457497, 0.009775049561939141984, 0.01050451823668782821, 0.01196345558618519891, 0.01342239293568256962, 0.01634026763467730931, 0.01925814233367205419, 0.02217601703266679214, 0.02509389173166153703, 0.02801176643065627497, 0.03092964112965101986 ),
 .UNSPECIFIED. ) ;
#36861=DIRECTION ( 'NONE',  ( 0.8660512985181135770, 0.4999551463232370097, 0.000000000000000000 ) ) ;
#36867=ORIENTED_EDGE ( 'NONE', *, *, #21530, .T. ) ;
#36869=EDGE_CURVE ( 'NONE', #29183, #2065, #26631, .T. ) ;
#36872=CARTESIAN_POINT ( 'NONE',  ( 0.6533741625928966013, -1.451818462565194201, -0.4117423987689379228 ) ) ;
#36879=ORIENTED_EDGE ( 'NONE', *, *, #11903, .T. ) ;
#36884=CARTESIAN_POINT ( 'NONE',  ( 0.6984663268742642428, -1.558725849730709934, -0.5155029497116575543 ) ) ;
#36891=CARTESIAN_POINT ( 'NONE',  ( 0.1834964085430285941, -1.226715333008844055, -0.5155029497116575543 ) ) ;
#36898=CARTESIAN_POINT ( 'NONE',  ( -5.013849553589398218E-05, -2.025592738939852033, -0.6748736259139497262 ) ) ;
#36906=CARTESIAN_POINT ( 'NONE',  ( 0.3648744522289030789, -2.000369472598153564, -0.6742880656426406549 ) ) ;
#36910=CYLINDRICAL_SURFACE ( 'NONE', #11514, 0.1033070866141732880 ) ;
#36912=CARTESIAN_POINT ( 'NONE',  ( -2.112273405726188513E-14, -2.107936428766274073, -0.2870436526301869962 ) ) ;
#36918=DIRECTION ( 'NONE',  ( 0.8660512985181127998, 0.4999551463232382309, 0.000000000000000000 ) ) ;
#36921=CARTESIAN_POINT ( 'NONE',  ( 0.1994776429548950347, -2.045397862102978248, -0.3070066531183754388 ) ) ;
#36923=CIRCLE ( 'NONE', #20522, 0.1333070866141733701 ) ;
#36924=EDGE_CURVE ( 'NONE', #4721, #9760, #31106, .T. ) ;
#36927=DIRECTION ( 'NONE',  ( 1.167933802921251313E-16, 0.9396926207859072067, -0.3420201433256720991 ) ) ;
#36930=ADVANCED_FACE ( 'NONE', ( #12117 ), #5773, .T. ) ;
#36932=ORIENTED_EDGE ( 'NONE', *, *, #18291, .F. ) ;
#36934=CARTESIAN_POINT ( 'NONE',  ( 0.09701883858600784949, -1.253543889448050175, -0.5155029497116575543 ) ) ;
#36940=CARTESIAN_POINT ( 'NONE',  ( 0.3999835757944618098, -1.598096088517039437, -0.3114834528418581883 ) ) ;
#36942=CARTESIAN_POINT ( 'NONE',  ( 0.4122953444515879418, -1.719325576034882674, -0.5258118692306196218 ) ) ;
#36954=CARTESIAN_POINT ( 'NONE',  ( 0.6260944913943206069, -1.518023479389316810, -0.3975690101215826333 ) ) ;
#36962=CARTESIAN_POINT ( 'NONE',  ( 0.3659586724855932727, -1.748074482237940375, -0.5029264115039194794 ) ) ;
#36964=AXIS2_PLACEMENT_3D ( 'NONE', #35978, #13752, #26136 ) ;
#36965=CARTESIAN_POINT ( 'NONE',  ( 0.4495244212156574437, -1.660272750698808863, -0.6367136028539922554 ) ) ;
#36981=CARTESIAN_POINT ( 'NONE',  ( 0.3544495675655560118, -1.747437704060168739, -0.5520337568983563203 ) ) ;
#36994=AXIS2_PLACEMENT_3D ( 'NONE', #21603, #33719, #2269 ) ;
#36999=CARTESIAN_POINT ( 'NONE',  ( 0.3992403239432529283, -1.683235622436187073, -0.6263438071736542323 ) ) ;
#37003=CARTESIAN_POINT ( 'NONE',  ( -0.005726188848608329551, -1.958868650540482870, -0.6583431953115838065 ) ) ;
#37011=CIRCLE ( 'NONE', #19929, 0.1033070866141734129 ) ;
#37012=CARTESIAN_POINT ( 'NONE',  ( 0.2209260011871197471, -1.309027873449325918, -0.6184399470714002645 ) ) ;
#37013=CARTESIAN_POINT ( 'NONE',  ( 0.4186432780919984720, -1.612034538517055360, -0.6668481824684697745 ) ) ;
#37015=AXIS2_PLACEMENT_3D ( 'NONE', #3413, #6298, #590 ) ;
#37025=EDGE_LOOP ( 'NONE', ( #27403, #33573, #7482, #30902, #13611, #33205 ) ) ;
#37034=FACE_OUTER_BOUND ( 'NONE', #10161, .T. ) ;
#37037=ORIENTED_EDGE ( 'NONE', *, *, #12200, .T. ) ;
#37047=DIRECTION ( 'NONE',  ( -0.9713176644646462909, -0.03533109781499667312, -0.2351461422735486029 ) ) ;
#37048=CARTESIAN_POINT ( 'NONE',  ( 0.3499983029951591051, -1.626951647584141680, -0.6024333599963986874 ) ) ;
#37049=VECTOR ( 'NONE', #33227, 39.37007874015748854 ) ;
#37069=CARTESIAN_POINT ( 'NONE',  ( 0.3435345990243335312, -1.649434886652794363, -0.4420678747786416785 ) ) ;
#37070=ORIENTED_EDGE ( 'NONE', *, *, #9500, .T. ) ;
#37075=VERTEX_POINT ( 'NONE', #3665 ) ;
#37080=DIRECTION ( 'NONE',  ( 0.8660512985181132439, 0.4999551463232376203, 0.000000000000000000 ) ) ;
#37086=CARTESIAN_POINT ( 'NONE',  ( 0.1734973056165641514, -1.209394307038482497, -0.5155029497116575543 ) ) ;
#37094=FACE_OUTER_BOUND ( 'NONE', #28484, .T. ) ;
#37105=DIRECTION ( 'NONE',  ( 0.000000000000000000, 0.000000000000000000, -1.000000000000000000 ) ) ;
#37107=CARTESIAN_POINT ( 'NONE',  ( 0.05496475644004305411, -1.465908258127670338, -0.6471173864664848674 ) ) ;
#37117=CARTESIAN_POINT ( 'NONE',  ( 0.3612352339526118117, -1.954411822542491128, -0.4945793958471655927 ) ) ;
#37119=EDGE_CURVE ( 'NONE', #38511, #38598, #17818, .T. ) ;
#37120=VECTOR ( 'NONE', #35947, 39.37007874015748854 ) ;
#37126=ORIENTED_EDGE ( 'NONE', *, *, #33520, .T. ) ;
#37130=ORIENTED_EDGE ( 'NONE', *, *, #5528, .T. ) ;
#37131=CARTESIAN_POINT ( 'NONE',  ( -2.115421433687637455E-14, -2.104525754108412805, -0.6992670217217592521 ) ) ;
#37135=CARTESIAN_POINT ( 'NONE',  ( 0.3619118515909163780, -1.781044822011065731, -0.5264419442840763130 ) ) ;
#37136=CIRCLE ( 'NONE', #36495, 0.04330708661417327632 ) ;
#37139=CARTESIAN_POINT ( 'NONE',  ( 0.2059273467974226113, -1.283046334493782359, -0.7462941026102624109 ) ) ;
#37141=ORIENTED_EDGE ( 'NONE', *, *, #14680, .F. ) ;
#37144=DIRECTION ( 'NONE',  ( 0.000000000000000000, -1.000000000000000000, 0.000000000000000000 ) ) ;
#37146=DIRECTION ( 'NONE',  ( 0.4999551463232372317, -0.8660512985181135770, 0.000000000000000000 ) ) ;
#37155=CARTESIAN_POINT ( 'NONE',  ( 0.3895534942183391247, -1.799872921755753641, -0.3127170998378249189 ) ) ;
#37162=CARTESIAN_POINT ( 'NONE',  ( 0.6215274601157204648, -1.354888019438377444, -0.6250000000000000000 ) ) ;
#37167=EDGE_CURVE ( 'NONE', #37390, #2983, #39237, .T. ) ;
#37168=CARTESIAN_POINT ( 'NONE',  ( 0.6359077707932225820, -1.518635804457564520, -0.4166810063141049847 ) ) ;
#37176=CARTESIAN_POINT ( 'NONE',  ( 0.3656711388830471421, -1.748838986500312442, -0.5108124120186164907 ) ) ;
#37179=CARTESIAN_POINT ( 'NONE',  ( 0.4568194025597909769, -1.686975086019319559, -0.6191628275868227282 ) ) ;
#37182=CARTESIAN_POINT ( 'NONE',  ( 0.5383773389028485568, -1.668462205496939132, -0.5443657938344932390 ) ) ;
#37192=ORIENTED_EDGE ( 'NONE', *, *, #37336, .T. ) ;
#37193=ADVANCED_FACE ( 'NONE', ( #29563 ), #40599, .F. ) ;
#37200=DIRECTION ( 'NONE',  ( 0.8660512985181135770, 0.4999551463232370652, 1.983296656985675225E-15 ) ) ;
#37202=CIRCLE ( 'NONE', #16184, 0.1033070866141732325 ) ;
#37206=CARTESIAN_POINT ( 'NONE',  ( 0.2933751793910955863, -1.495278175259627362, -0.3326461521471292260 ) ) ;
#37210=CARTESIAN_POINT ( 'NONE',  ( 0.3534309663918363542, -1.740588291835677870, -0.3303540215336857044 ) ) ;
#37216=CARTESIAN_POINT ( 'NONE',  ( 0.1593091913372683688, -1.385766485008658622, -0.6742091435302814961 ) ) ;
#37220=EDGE_CURVE ( 'NONE', #17181, #31057, #29765, .T. ) ;
#37247=CARTESIAN_POINT ( 'NONE',  ( 0.4131084440300917815, -1.709575418134248626, -0.4213477687306632080 ) ) ;
#37249=EDGE_LOOP ( 'NONE', ( #21066, #5694, #39709, #25661 ) ) ;
#37254=DIRECTION ( 'NONE',  ( 1.000000000000000000, 0.000000000000000000, 0.000000000000000000 ) ) ;
#37258=CARTESIAN_POINT ( 'NONE',  ( 0.1999999999999789724, -2.183180860297921466, -0.4437760292030870635 ) ) ;
#37269=CARTESIAN_POINT ( 'NONE',  ( 0.3460971044594531865, -1.678560363434771663, -0.4565776378744553221 ) ) ;
#37270=ORIENTED_EDGE ( 'NONE', *, *, #19973, .T. ) ;
#37274=DIRECTION ( 'NONE',  ( -0.4999551463232372317, 0.8660512985181135770, -0.000000000000000000 ) ) ;
#37277=VERTEX_POINT ( 'NONE', #15563 ) ;
#37278=ORIENTED_EDGE ( 'NONE', *, *, #12521, .F. ) ;
#37280=CARTESIAN_POINT ( 'NONE',  ( 0.3707239397989903207, -1.673993377350394329, -0.6037758272379700752 ) ) ;
#37282=CYLINDRICAL_SURFACE ( 'NONE', #17201, 0.1033070866141732880 ) ;
#37284=EDGE_CURVE ( 'NONE', #652, #30726, #25639, .T. ) ;
#37287=CIRCLE ( 'NONE', #551, 0.1033070866141734129 ) ;
#37303=CARTESIAN_POINT ( 'NONE',  ( 0.01041184051585970598, -1.726097746008397493, -0.6357288279791224461 ) ) ;
#37308=CARTESIAN_POINT ( 'NONE',  ( 0.3560594290983791210, -1.794060577071256768, -0.5186890730419171369 ) ) ;
#37311=CARTESIAN_POINT ( 'NONE',  ( 0.3691383134885193318, -1.740927459917368303, -0.6793060835705189149 ) ) ;
#37315=ORIENTED_EDGE ( 'NONE', *, *, #6864, .F. ) ;
#37323=ORIENTED_EDGE ( 'NONE', *, *, #18964, .T. ) ;
#37328=CARTESIAN_POINT ( 'NONE',  ( 0.1825460907816478517, -1.756676529110209994, -0.3560404930609161744 ) ) ;
#37336=EDGE_CURVE ( 'NONE', #40066, #31681, #33186, .T. ) ;
#37343=EDGE_CURVE ( 'NONE', #9543, #394, #1676, .T. ) ;
#37345=CARTESIAN_POINT ( 'NONE',  ( 0.3880982458546209934, -1.816572098790980805, -0.3121909403687748719 ) ) ;
#37361=CARTESIAN_POINT ( 'NONE',  ( 0.03025322876596520452, -1.914130172580563061, -0.6840549778904242428 ) ) ;
#37367=CARTESIAN_POINT ( 'NONE',  ( 0.3864683547122780283, -1.712498712252804589, -0.5952922913290529250 ) ) ;
#37380=VERTEX_POINT ( 'NONE', #18641 ) ;
#37389=FACE_OUTER_BOUND ( 'NONE', #29552, .T. ) ;
#37390=VERTEX_POINT ( 'NONE', #3202 ) ;
#37393=ORIENTED_EDGE ( 'NONE', *, *, #2091, .F. ) ;
#37397=CARTESIAN_POINT ( 'NONE',  ( 0.2127719091618048841, -1.748736742968465485, -0.3547752604823448119 ) ) ;
#37398=CARTESIAN_POINT ( 'NONE',  ( 0.6922159527011226832, -1.545014083134421901, -0.6250000000000000000 ) ) ;
#37403=CARTESIAN_POINT ( 'NONE',  ( 0.3990191109500385025, -2.061617765760503485, -0.5133078562858378602 ) ) ;
#37406=CARTESIAN_POINT ( 'NONE',  ( 0.07836034245246617513, -1.898373411144233192, -0.6535496771068961541 ) ) ;
#37411=ADVANCED_FACE ( 'NONE', ( #26605 ), #40404, .T. ) ;
#37414=DIRECTION ( 'NONE',  ( -1.000000000000000000, 8.195543980992782950E-15, 0.000000000000000000 ) ) ;
#37417=CARTESIAN_POINT ( 'NONE',  ( 0.1989976604547370465, -2.047409678865564686, -0.7132172901365274598 ) ) ;
#37418=CARTESIAN_POINT ( 'NONE',  ( 0.3980973275624947738, -1.734594076868668067, -0.5940246208459699639 ) ) ;
#37419=ORIENTED_EDGE ( 'NONE', *, *, #9986, .F. ) ;
#37424=FACE_OUTER_BOUND ( 'NONE', #12956, .T. ) ;
#37426=CARTESIAN_POINT ( 'NONE',  ( 0.3624061103390691096, -1.968824918581854932, -0.4968426515055719972 ) ) ;
#37433=CARTESIAN_POINT ( 'NONE',  ( 0.5025602611599372382, -1.689138731673214489, -0.4231169579026368144 ) ) ;
#37449=DIRECTION ( 'NONE',  ( 0.000000000000000000, 0.000000000000000000, 1.000000000000000000 ) ) ;
#37452=CARTESIAN_POINT ( 'NONE',  ( 0.3695052819757340123, -1.758428263776099287, -0.4278193900811940176 ) ) ;
#37465=CARTESIAN_POINT ( 'NONE',  ( 0.4752104778612297187, -1.162234221663497546, -0.6186948529734399571 ) ) ;
#37469=ORIENTED_EDGE ( 'NONE', *, *, #10016, .T. ) ;
#37474=CARTESIAN_POINT ( 'NONE',  ( 0.3425232517505406027, -1.682473151710080606, -0.5664509581880096123 ) ) ;
#37481=CARTESIAN_POINT ( 'NONE',  ( 0.3779802290120621855, -1.643891170928071910, -0.3923847609905750655 ) ) ;
#37484=CARTESIAN_POINT ( 'NONE',  ( 0.6315454839751819538, -1.614677985460544640, -0.5441907603680019578 ) ) ;
#37487=CIRCLE ( 'NONE', #38806, 0.1033070866141732325 ) ;
#37488=DIRECTION ( 'NONE',  ( -0.8660512985181132439, -0.4999551463232377313, 0.000000000000000000 ) ) ;
#37498=CARTESIAN_POINT ( 'NONE',  ( 0.3590472838652598031, -1.925292734864337829, -0.5030625321385080451 ) ) ;
#37502=CIRCLE ( 'NONE', #5287, 0.02999999999999997113 ) ;
#37504=CARTESIAN_POINT ( 'NONE',  ( 0.4159916692016358830, -1.069406866067976081, -0.5155029497116575543 ) ) ;
#37506=CIRCLE ( 'NONE', #25703, 0.01000000000000002970 ) ;
#37517=CARTESIAN_POINT ( 'NONE',  ( 0.1805592728925153601, -1.816701042908541508, -0.3505378111635870098 ) ) ;
#37529=CARTESIAN_POINT ( 'NONE',  ( 0.3485603902089104977, -1.632100916239925148, -0.6568559003424170317 ) ) ;
#37531=CARTESIAN_POINT ( 'NONE',  ( 0.4243666725459964151, -1.591076223527387423, -0.4156371400837810537 ) ) ;
#37550=CARTESIAN_POINT ( 'NONE',  ( 0.6480134723046564460, -1.557673986349219941, -0.4212882653819030598 ) ) ;
#37551=DIRECTION ( 'NONE',  ( -0.8660512985181133550, -0.4999551463232372872, 0.000000000000000000 ) ) ;
#37556=VERTEX_POINT ( 'NONE', #18138 ) ;
#37559=ADVANCED_FACE ( 'NONE', ( #17717 ), #35080, .F. ) ;
#37562=CARTESIAN_POINT ( 'NONE',  ( 0.4100456123093286775, -1.725225710419908243, -0.4268450903248972028 ) ) ;
#37564=EDGE_CURVE ( 'NONE', #5039, #17175, #12166, .T. ) ;
#37565=ORIENTED_EDGE ( 'NONE', *, *, #17691, .F. ) ;
#37566=CARTESIAN_POINT ( 'NONE',  ( 0.5488242727466704496, -1.662431386828975288, -0.5397256741273313008 ) ) ;
#37581=ORIENTED_EDGE ( 'NONE', *, *, #22686, .F. ) ;
#37594=ORIENTED_EDGE ( 'NONE', *, *, #13500, .T. ) ;
#37597=CARTESIAN_POINT ( 'NONE',  ( 0.6107611075265444445, -1.468610687554505745, -0.6249999999999998890 ) ) ;
#37598=CARTESIAN_POINT ( 'NONE',  ( 0.003621456447956619175, -1.840971628676655980, -0.3528920961991032224 ) ) ;
#37605=CARTESIAN_POINT ( 'NONE',  ( 0.1589950187058418174, -2.053370087202771810, -0.6806478816540684207 ) ) ;
#37622=VERTEX_POINT ( 'NONE', #22063 ) ;
#37623=VERTEX_POINT ( 'NONE', #5975 ) ;
#37633=ORIENTED_EDGE ( 'NONE', *, *, #6627, .F. ) ;
#37634=DIRECTION ( 'NONE',  ( -0.2067069058495556444, -0.1193280138680804653, -0.9710989033977962537 ) ) ;
#37640=CARTESIAN_POINT ( 'NONE',  ( 0.5153600767897008605, -1.667753545667869153, -0.4356355497465531634 ) ) ;
#37645=TOROIDAL_SURFACE ( 'NONE', #13897, 0.04999999999999998196, 0.2000000000000000111 ) ;
#37647=EDGE_LOOP ( 'NONE', ( #89, #22467, #1286, #35514 ) ) ;
#37649=EDGE_CURVE ( 'NONE', #15269, #19872, #14151, .T. ) ;
#37650=CARTESIAN_POINT ( 'NONE',  ( 0.4761091661982407297, -1.093057945753640459, -0.4172484957075230927 ) ) ;
#37651=DIRECTION ( 'NONE',  ( 0.000000000000000000, 0.000000000000000000, -1.000000000000000000 ) ) ;
#37656=CARTESIAN_POINT ( 'NONE',  ( -2.112273405726188513E-14, -2.183180860297921466, -0.4937760292030871079 ) ) ;
#37657=CARTESIAN_POINT ( 'NONE',  ( 0.4974659133798483013, -1.692079602952080819, -0.4360564763722065140 ) ) ;
#37677=TOROIDAL_SURFACE ( 'NONE', #9427, 0.1333070866141734256, 0.02999999999999999889 ) ;
#37678=CARTESIAN_POINT ( 'NONE',  ( 0.3408697296860659920, -1.678829344471958862, -0.4023362845575238489 ) ) ;
#37680=CARTESIAN_POINT ( 'NONE',  ( 0.4475189022780061698, -1.144336077227306347, -0.3898466471268308697 ) ) ;
#37684=ORIENTED_EDGE ( 'NONE', *, *, #28854, .T. ) ;
#37687=ORIENTED_EDGE ( 'NONE', *, *, #1714, .T. ) ;
#37699=CARTESIAN_POINT ( 'NONE',  ( 0.5988768534318814618, -1.579658039218154286, -0.6073675125623819726 ) ) ;
#37704=AXIS2_PLACEMENT_3D ( 'NONE', #30774, #31574, #6474 ) ;
#37717=EDGE_CURVE ( 'NONE', #28606, #12681, #28618, .T. ) ;
#37719=EDGE_CURVE ( 'NONE', #24860, #37622, #8251, .T. ) ;
#37738=CARTESIAN_POINT ( 'NONE',  ( 0.3682921722882570026, -2.034650425189704848, -0.3093546411653611550 ) ) ;
#37742=ORIENTED_EDGE ( 'NONE', *, *, #28868, .T. ) ;
#37749=CARTESIAN_POINT ( 'NONE',  ( 0.5324218574196054599, -1.599714249701870372, -0.4411601419016027981 ) ) ;
#37756=CARTESIAN_POINT ( 'NONE',  ( 0.3917177981610598936, -1.718486023052998135, -0.3060476212702296084 ) ) ;
#37757=AXIS2_PLACEMENT_3D ( 'NONE', #25062, #31247, #33488 ) ;
#37769=CARTESIAN_POINT ( 'NONE',  ( 0.6399061864322146409, -1.581153798985416747, -0.4326948249935556046 ) ) ;
#37770=LINE ( 'NONE', #389, #6800 ) ;
#37774=ORIENTED_EDGE ( 'NONE', *, *, #34613, .T. ) ;
#37776=CARTESIAN_POINT ( 'NONE',  ( 0.3683998553492333072, -1.620410879730887599, -0.3666241388582308636 ) ) ;
#37779=CARTESIAN_POINT ( 'NONE',  ( 0.5223466852174000197, -1.671872836107813232, -0.4402217964095243574 ) ) ;
#37784=CARTESIAN_POINT ( 'NONE',  ( 0.4942245234460003744, -1.693950796473111975, -0.6125153944540959738 ) ) ;
#37792=B_SPLINE_CURVE_WITH_KNOTS ( 'NONE', 3,
 ( #40201, #37131, #21308, #34650 ),
 .UNSPECIFIED., .F., .F.,
 ( 4, 4 ),
 ( 0.000000000000000000, 0.0002765727889952716173 ),
 .UNSPECIFIED. ) ;
#37803=CARTESIAN_POINT ( 'NONE',  ( 0.1994181777622906770, -2.041053584879497063, -0.3082502591624063371 ) ) ;
#37804=B_SPLINE_CURVE_WITH_KNOTS ( 'NONE', 3,
 ( #31444, #28348, #217, #36785 ),
 .UNSPECIFIED., .F., .F.,
 ( 4, 4 ),
 ( 0.000000000000000000, 0.0005209419993945884871 ),
 .UNSPECIFIED. ) ;
#37813=EDGE_CURVE ( 'NONE', #858, #9058, #3555, .T. ) ;
#37817=DIRECTION ( 'NONE',  ( 0.8660512985181133550, 0.4999551463232372317, 0.000000000000000000 ) ) ;
#37824=CARTESIAN_POINT ( 'NONE',  ( 0.3999999999999783173, -2.047156491238096176, -0.7141923294504540776 ) ) ;
#37826=CARTESIAN_POINT ( 'NONE',  ( 0.08522533823544217735, -1.743361703470160728, -0.6409892287915732734 ) ) ;
#37861=CARTESIAN_POINT ( 'NONE',  ( -2.112273405726188513E-14, -1.835409001655643690, -0.3543101909453316156 ) ) ;
#37867=CARTESIAN_POINT ( 'NONE',  ( 0.1995969790795776300, -2.064390217781732595, -0.7176297154563284764 ) ) ;
#37872=EDGE_CURVE ( 'NONE', #29543, #3269, #32048, .T. ) ;
#37882=CARTESIAN_POINT ( 'NONE',  ( 0.1758888584962763069, -1.756691831069698173, -0.6511160423431344713 ) ) ;
#37885=DIRECTION ( 'NONE',  ( 0.4017000971270622278, 0.2318939203356582823, -0.8859245124046789543 ) ) ;
#37893=CARTESIAN_POINT ( 'NONE',  ( 0.3591498995103406533, -1.737620376665804933, -0.5147966178037263196 ) ) ;
#37897=ORIENTED_EDGE ( 'NONE', *, *, #16494, .T. ) ;
#37901=VERTEX_POINT ( 'NONE', #29423 ) ;
#37902=CARTESIAN_POINT ( 'NONE',  ( 0.6214629568584182362, -1.607011684701395993, -0.5680849726491742357 ) ) ;
#37911=CARTESIAN_POINT ( 'NONE',  ( 0.6356291811816829895, -1.489535549261238767, -0.6355727712968906040 ) ) ;
#37915=B_SPLINE_CURVE_WITH_KNOTS ( 'NONE', 3,
 ( #9673, #34756, #6563, #19140 ),
 .UNSPECIFIED., .F., .F.,
 ( 4, 4 ),
 ( 3.150947443209742121E-16, 0.0008530918207275374129 ),
 .UNSPECIFIED. ) ;
#37923=CARTESIAN_POINT ( 'NONE',  ( 0.4654555503626408020, -1.098995021068088773, -0.3936018329855539566 ) ) ;
#37930=ADVANCED_FACE ( 'NONE', ( #38481 ), #1270, .T. ) ;
#37937=VERTEX_POINT ( 'NONE', #19570 ) ;
#37945=CARTESIAN_POINT ( 'NONE',  ( 0.3812837827729997908, -1.707230790293840172, -0.3372124425115716195 ) ) ;
#37949=B_SPLINE_CURVE_WITH_KNOTS ( 'NONE', 3,
 ( #8748, #9353, #30572, #5852, #21933, #30768, #37529, #2397 ),
 .UNSPECIFIED., .F., .F.,
 ( 4, 2, 2, 4 ),
 ( 0.000000000000000000, 0.0002823184703889531472, 0.0005646369407779062944, 0.001129273881555797193 ),
 .UNSPECIFIED. ) ;
#37957=CARTESIAN_POINT ( 'NONE',  ( 0.4356662251172992439, -1.610775558009423847, -0.3686272921855577867 ) ) ;
#37959=CARTESIAN_POINT ( 'NONE',  ( 0.4924701362321921017, -1.025257283658408403, -0.5155029497116575543 ) ) ;
#37963=CARTESIAN_POINT ( 'NONE',  ( 0.3967242239788378311, -1.726942646203573517, -0.3050504165543944657 ) ) ;
#37964=ADVANCED_FACE ( 'NONE', ( #7183 ), #33497, .F. ) ;
#37967=( BOUNDED_SURFACE ( )  B_SPLINE_SURFACE ( 3, 2, ( 
 ( #32169, #26027, #16950 ),
 ( #10170, #32974, #29696 ),
 ( #32576, #36068, #3979 ),
 ( #29911, #23551, #32361 ),
 ( #1539, #23353, #14060 ),
 ( #29491, #38547, #16754 ),
 ( #10563, #14264, #22738 ),
 ( #16541, #35664, #29083 ) ),
 .UNSPECIFIED., .F., .F., .T. ) 
 B_SPLINE_SURFACE_WITH_KNOTS ( ( 4, 2, 2, 4 ),
 ( 3, 3 ),
 ( -1.735946658636840947E-05, 0.002957348748439985603, 0.004444702855953162543, 0.005932056963466339483 ),
 ( 0.000000000000000000, 1.000000000000000000 ),
 .UNSPECIFIED. ) 
 GEOMETRIC_REPRESENTATION_ITEM ( )  RATIONAL_B_SPLINE_SURFACE ( (
 ( 1.000000000000000000, 1.000000000000000000, 1.000000000000000000),
 ( 1.000000000000000000, 0.9999719623954188563, 1.000000000000000000),
 ( 1.000000000000000000, 0.9935697921326018811, 1.000000000000000000),
 ( 1.000000000000000000, 0.9839453963689780425, 1.000000000000000000),
 ( 1.000000000000000000, 0.9807074542717970633, 1.000000000000000000),
 ( 1.000000000000000000, 0.9760289094675052013, 1.000000000000000000),
 ( 1.000000000000000000, 0.9745874693094034313, 1.000000000000000000),
 ( 1.000000000000000000, 0.9750816781289051161, 1.000000000000000000) ) ) 
 REPRESENTATION_ITEM ( '' )  SURFACE ( )  );
#37976=CARTESIAN_POINT ( 'NONE',  ( 0.3999094372835061972, -2.086652961537767137, -0.4708658242691809992 ) ) ;
#37981=DIRECTION ( 'NONE',  ( 0.000000000000000000, 0.000000000000000000, -1.000000000000000000 ) ) ;
#37984=CARTESIAN_POINT ( 'NONE',  ( 0.5320511322164590551, -1.669038612624452744, -0.4503538000400599262 ) ) ;
#37988=CARTESIAN_POINT ( 'NONE',  ( 0.3959480418811466840, -1.613405948999770523, -0.6688934733077330774 ) ) ;
#37993=CARTESIAN_POINT ( 'NONE',  ( 0.4559719632891929830, -1.698713290701216350, -0.5155029497116575543 ) ) ;
#37998=B_SPLINE_CURVE_WITH_KNOTS ( 'NONE', 3,
 ( #22212, #25685, #6535, #34933, #9429, #15809, #25072, #19703, #6948, #228 ),
 .UNSPECIFIED., .F., .F.,
 ( 4, 2, 2, 2, 4 ),
 ( 0.0008171848362502084993, 0.001788850595559428845, 0.002760516354868649408, 0.003732182114177869103, 0.004703847873487089666 ),
 .UNSPECIFIED. ) ;
#38013=CARTESIAN_POINT ( 'NONE',  ( 0.4732031336055909643, -1.076730694904952434, -0.6086252408385472989 ) ) ;
#38015=CARTESIAN_POINT ( 'NONE',  ( 0.4547563268321924701, -1.664835936145135031, -0.6217598108907549381 ) ) ;
#38017=CARTESIAN_POINT ( 'NONE',  ( 0.02999999999997886302, -2.183180860297921466, -0.4937760292030871079 ) ) ;
#38021=CARTESIAN_POINT ( 'NONE',  ( 0.1968880119611848278, -2.022044081434100971, -0.7071002453052855907 ) ) ;
#38032=CARTESIAN_POINT ( 'NONE',  ( 0.4356662251172990774, -1.610775558009424735, -0.3686272921855577867 ) ) ;
#38053=ORIENTED_EDGE ( 'NONE', *, *, #29496, .T. ) ;
#38054=DIRECTION ( 'NONE',  ( 0.8660512985181132439, 0.4999551463232376758, 0.000000000000000000 ) ) ;
#38057=CARTESIAN_POINT ( 'NONE',  ( -2.112273405726188513E-14, -2.104523474114237125, -0.2882858665344287807 ) ) ;
#38058=EDGE_CURVE ( 'NONE', #7985, #30726, #27152, .T. ) ;
#38072=CARTESIAN_POINT ( 'NONE',  ( 0.3732864473234233649, -1.732922991205104735, -0.4865963089983659229 ) ) ;
#38079=DIRECTION ( 'NONE',  ( -0.4999551463232377313, 0.8660512985181132439, -0.000000000000000000 ) ) ;
#38081=EDGE_CURVE ( 'NONE', #14602, #3320, #16139, .T. ) ;
#38085=VERTEX_POINT ( 'NONE', #17485 ) ;
#38098=CARTESIAN_POINT ( 'NONE',  ( 0.6323818217483841986, -1.501417540436901454, -0.6354249433986968176 ) ) ;
#38117=LINE ( 'NONE', #35650, #9653 ) ;
#38122=CARTESIAN_POINT ( 'NONE',  ( 0.02999999999997886302, -2.183180860297921466, -0.2437760292030870524 ) ) ;
#38142=ORIENTED_EDGE ( 'NONE', *, *, #27838, .T. ) ;
#38152=EDGE_CURVE ( 'NONE', #23391, #29449, #16776, .T. ) ;
#38153=CARTESIAN_POINT ( 'NONE',  ( 0.3999999999999783729, -2.097675824466504135, -0.5196396315034577107 ) ) ;
#38154=EDGE_CURVE ( 'NONE', #13061, #29245, #22083, .T. ) ;
#38157=ADVANCED_FACE ( 'NONE', ( #11904 ), #33674, .T. ) ;
#38158=DIRECTION ( 'NONE',  ( 0.4999551463232373427, -0.8660512985181134660, 0.000000000000000000 ) ) ;
#38166=CIRCLE ( 'NONE', #17817, 0.1333070866141734534 ) ;
#38168=CARTESIAN_POINT ( 'NONE',  ( 0.4725170613493049898, -1.127650739974109584, -0.3804102490670597247 ) ) ;
#38176=CARTESIAN_POINT ( 'NONE',  ( 0.5460456802599069626, -1.663806483198842612, -0.4748870211469257141 ) ) ;
#38180=DIRECTION ( 'NONE',  ( 0.8660512985181134660, 0.4999551463232372872, 0.000000000000000000 ) ) ;
#38199=CARTESIAN_POINT ( 'NONE',  ( 0.3398694799145297596, -1.651829322229799057, -0.3839951212973800598 ) ) ;
#38202=AXIS2_PLACEMENT_3D ( 'NONE', #9387, #3630, #3419 ) ;
#38208=CARTESIAN_POINT ( 'NONE',  ( 0.3855953621615598736, -1.879051724042604121, -0.5131335247813605394 ) ) ;
#38209=DIRECTION ( 'NONE',  ( 0.000000000000000000, 0.000000000000000000, -1.000000000000000000 ) ) ;
#38212=CARTESIAN_POINT ( 'NONE',  ( 0.1757972024313168569, -1.554466423739661707, -0.3564840659511942511 ) ) ;
#38214=CARTESIAN_POINT ( 'NONE',  ( 0.1984327864668515018, -2.037394601422313212, -0.7106754852713771387 ) ) ;
#38224=AXIS2_PLACEMENT_3D ( 'NONE', #19569, #32288, #3909 ) ;
#38227=CARTESIAN_POINT ( 'NONE',  ( 0.4265385717645384100, -1.610299123943391919, -0.3658380804397534103 ) ) ;
#38243=CARTESIAN_POINT ( 'NONE',  ( 0.2034275709668185161, -1.278716077829719300, -0.3194722003129935040 ) ) ;
#38247=CARTESIAN_POINT ( 'NONE',  ( -7.749463158931491936E-06, -2.054538870594384115, -0.2740520340402112232 ) ) ;
#38249=VERTEX_POINT ( 'NONE', #32444 ) ;
#38250=DIRECTION ( 'NONE',  ( 1.000000000000000000, 0.000000000000000000, 0.000000000000000000 ) ) ;
#38261=CARTESIAN_POINT ( 'NONE',  ( 0.3223215012880607522, -1.527613999045389415, -0.7370652326885508421 ) ) ;
#38267=CARTESIAN_POINT ( 'NONE',  ( 0.2927350798623002959, -1.544518291098198715, -0.6925464747855896164 ) ) ;
#38270=CARTESIAN_POINT ( 'NONE',  ( 0.2927350798622761485, -1.544518291098210261, -0.6925464747855858416 ) ) ;
#38279=CARTESIAN_POINT ( 'NONE',  ( 0.4720092934469595769, -1.159105807646246600, -0.4122610257295769576 ) ) ;
#38292=CARTESIAN_POINT ( 'NONE',  ( -2.112273405726188513E-14, -2.107936428766272741, -0.2870436526301873847 ) ) ;
#38293=ORIENTED_EDGE ( 'NONE', *, *, #23537, .F. ) ;
#38298=CARTESIAN_POINT ( 'NONE',  ( 0.6434205324370606549, -1.429852958019900200, -0.6292195679946139819 ) ) ;
#38302=DIRECTION ( 'NONE',  ( 0.000000000000000000, 0.000000000000000000, -1.000000000000000000 ) ) ;
#38304=CARTESIAN_POINT ( 'NONE',  ( 0.1759300380180284507, -1.231083256582695684, -0.4125659523519146221 ) ) ;
#38306=CIRCLE ( 'NONE', #23246, 0.1033070866141732325 ) ;
#38314=CARTESIAN_POINT ( 'NONE',  ( 0.4567835194390648113, -1.106698506970852147, -0.3756906124113179035 ) ) ;
#38324=EDGE_LOOP ( 'NONE', ( #8943, #31471, #10165, #7362 ) ) ;
#38328=TOROIDAL_SURFACE ( 'NONE', #39011, 0.08830708661417342731, 0.01499999999999999944 ) ;
#38330=ORIENTED_EDGE ( 'NONE', *, *, #26399, .F. ) ;
#38355=ADVANCED_FACE ( 'NONE', ( #35344 ), #7135, .F. ) ;
#38367=CARTESIAN_POINT ( 'NONE',  ( 0.5353561135554193440, -1.635566321744903906, -0.5401600205605631144 ) ) ;
#38371=CIRCLE ( 'NONE', #37704, 0.05330708661417339622 ) ;
#38372=DIRECTION ( 'NONE',  ( -0.4999551463232377313, 0.8660512985181132439, -0.000000000000000000 ) ) ;
#38373=VECTOR ( 'NONE', #25683, 39.37007874015748854 ) ;
#38380=ORIENTED_EDGE ( 'NONE', *, *, #8679, .F. ) ;
#38401=CARTESIAN_POINT ( 'NONE',  ( 0.1987142792575499195, -2.031216512937317642, -0.3109074494126257138 ) ) ;
#38409=CARTESIAN_POINT ( 'NONE',  ( 0.08471508035845262685, -1.662502673085205496, -0.3682490140513268728 ) ) ;
#38410=B_SPLINE_CURVE_WITH_KNOTS ( 'NONE', 3,
 ( #34428, #28071, #12227, #34215, #8713, #30542 ),
 .UNSPECIFIED., .F., .F.,
 ( 4, 2, 4 ),
 ( -7.819781547275446803E-06, 0.0005992764336422149504, 0.001206372648831705204 ),
 .UNSPECIFIED. ) ;
#38411=DIRECTION ( 'NONE',  ( 0.4999551463232372317, -0.8660512985181135770, 0.000000000000000000 ) ) ;
#38412=DIRECTION ( 'NONE',  ( 0.4999551463232369541, -0.8660512985181135770, 8.034847040189003318E-16 ) ) ;
#38415=B_SPLINE_CURVE_WITH_KNOTS ( 'NONE', 3,
 ( #35689, #23377, #32792, #29935 ),
 .UNSPECIFIED., .F., .F.,
 ( 4, 4 ),
 ( 0.000000000000000000, 0.1653597904024633469 ),
 .UNSPECIFIED. ) ;
#38418=CARTESIAN_POINT ( 'NONE',  ( 0.3873588152119425976, -1.881242926337077348, -0.4864542591168500296 ) ) ;
#38422=AXIS2_PLACEMENT_3D ( 'NONE', #2292, #34354, #6168 ) ;
#38423=CARTESIAN_POINT ( 'NONE',  ( 0.6453025834024398444, -1.483340485508765738, -0.6195432661420555709 ) ) ;
#38436=CARTESIAN_POINT ( 'NONE',  ( 0.5431716904107454225, -1.629634126750506340, -0.5863231643301370921 ) ) ;
#38438=EDGE_CURVE ( 'NONE', #30555, #25449, #11580, .T. ) ;
#38447=CARTESIAN_POINT ( 'NONE',  ( 0.5905148994843929522, -1.592503337285391174, -0.4381592367070794580 ) ) ;
#38462=CARTESIAN_POINT ( 'NONE',  ( 0.001120871055943682042, -1.921117088193987188, -0.3378957227562057741 ) ) ;
#38481=FACE_OUTER_BOUND ( 'NONE', #16151, .T. ) ;
#38487=CARTESIAN_POINT ( 'NONE',  ( 0.3962688442617325890, -1.689744230457778773, -0.5025684713971244610 ) ) ;
#38494=ORIENTED_EDGE ( 'NONE', *, *, #5884, .T. ) ;
#38507=CARTESIAN_POINT ( 'NONE',  ( 0.3734441402355138662, -1.768196402555201052, -0.5721408755833873316 ) ) ;
#38508=CARTESIAN_POINT ( 'NONE',  ( 0.6100529622307712119, -1.615500794165734444, -0.5228307121444174532 ) ) ;
#38511=VERTEX_POINT ( 'NONE', #39027 ) ;
#38520=CARTESIAN_POINT ( 'NONE',  ( 0.4848381743978809055, -1.590261796594116150, -0.5819748978324561506 ) ) ;
#38536=CARTESIAN_POINT ( 'NONE',  ( 0.3445219659096331322, -1.630113034086819290, -0.4330379103484555681 ) ) ;
#38538=CIRCLE ( 'NONE', #3083, 0.1333070866141734534 ) ;
#38540=EDGE_CURVE ( 'NONE', #30458, #23204, #20104, .T. ) ;
#38547=CARTESIAN_POINT ( 'NONE',  ( 0.3601874435097799920, -1.787344030326375899, -0.5040241098297806310 ) ) ;
#38549=CARTESIAN_POINT ( 'NONE',  ( 0.2040530089634621236, -1.652187626897218653, -0.3590702193978799750 ) ) ;
#38550=EDGE_CURVE ( 'NONE', #28258, #24493, #29080, .T. ) ;
#38559=CARTESIAN_POINT ( 'NONE',  ( 0.4582055935369603317, -1.592191023407962813, -0.4280546469726743686 ) ) ;
#38570=AXIS2_PLACEMENT_3D ( 'NONE', #34990, #13391, #4115 ) ;
#38577=CARTESIAN_POINT ( 'NONE',  ( 0.4781934768423675708, -1.682642038360962378, -0.6151431148613255573 ) ) ;
#38591=DIRECTION ( 'NONE',  ( 0.03712106494698044767, -0.7041771612121668911, -0.7090532787910764911 ) ) ;
#38592=CARTESIAN_POINT ( 'NONE',  ( 0.2026013104559352129, -1.284966392796108803, -0.7446432428005457238 ) ) ;
#38598=VERTEX_POINT ( 'NONE', #7756 ) ;
#38602=VERTEX_POINT ( 'NONE', #20520 ) ;
#38606=CARTESIAN_POINT ( 'NONE',  ( 0.2230958589031876160, -1.614348418715432221, -0.3562888994457304448 ) ) ;
#38610=CIRCLE ( 'NONE', #20898, 0.02999999999999997807 ) ;
#38612=CARTESIAN_POINT ( 'NONE',  ( 0.3860292282735227620, -1.790736048274133685, -0.5258466387971835188 ) ) ;
#38613=CARTESIAN_POINT ( 'NONE',  ( 0.05227399809316079365, -1.457268265538602670, -0.3759856532797451467 ) ) ;
#38619=CARTESIAN_POINT ( 'NONE',  ( 0.4428400309745522123, -1.146281092196613338, -0.3830631589809549431 ) ) ;
#38621=CARTESIAN_POINT ( 'NONE',  ( 0.4149351083933472961, -1.715145687224109095, -0.4973294153635586801 ) ) ;
#38625=CARTESIAN_POINT ( 'NONE',  ( 0.6567205214941880254, -1.402512679334766643, -0.6099112297698211504 ) ) ;
#38629=DIRECTION ( 'NONE',  ( 0.4999551463232377313, -0.8660512985181132439, 0.000000000000000000 ) ) ;
#38632=CARTESIAN_POINT ( 'NONE',  ( 0.4196702119927928076, -1.647204429517209023, -0.4088696122891719575 ) ) ;
#38633=DIRECTION ( 'NONE',  ( 0.4999551463232373427, -0.8660512985181134660, 0.000000000000000000 ) ) ;
#38634=CARTESIAN_POINT ( 'NONE',  ( 0.2026534980585697476, -1.284936265343112227, -0.2885610809406460309 ) ) ;
#38638=EDGE_CURVE ( 'NONE', #13200, #37623, #16812, .T. ) ;
#38639=CARTESIAN_POINT ( 'NONE',  ( 0.3625960434667522270, -1.762758894398491982, -0.5926935080085825591 ) ) ;
#38649=DIRECTION ( 'NONE',  ( 0.000000000000000000, 0.000000000000000000, -1.000000000000000000 ) ) ;
#38657=CARTESIAN_POINT ( 'NONE',  ( 5.653807113072445720E-06, -2.020207405608465123, -0.2840335132522610051 ) ) ;
#38663=EDGE_CURVE ( 'NONE', #28258, #545, #33242, .T. ) ;
#38666=B_SPLINE_CURVE_WITH_KNOTS ( 'NONE', 3,
 ( #1053, #31876, #3694, #35553, #841, #13348, #4290, #25924, #38447, #13562, #5087, #36361, #39650, #17647, #11080, #35971, #14773, #24239 ),
 .UNSPECIFIED., .F., .F.,
 ( 4, 2, 2, 2, 2, 2, 2, 2, 4 ),
 ( 0.007419921033514278487, 0.008176191601852815169, 0.008932462170191350984, 0.009310597454360615421, 0.009688732738529879859, 0.01044500330686841567, 0.01120127387520694975, 0.01195754444354548210, 0.01347008558022255026 ),
 .UNSPECIFIED. ) ;
#38676=CARTESIAN_POINT ( 'NONE',  ( 0.1905398795079399077, -1.256391271284680533, -0.3903413229800113959 ) ) ;
#38681=CARTESIAN_POINT ( 'NONE',  ( 0.4143292853021347533, -1.740072816664171684, -0.5834784908774952594 ) ) ;
#38684=VERTEX_POINT ( 'NONE', #584 ) ;
#38694=ORIENTED_EDGE ( 'NONE', *, *, #3438, .F. ) ;
#38710=CARTESIAN_POINT ( 'NONE',  ( 0.4907610854883471818, -1.588559784271378783, -0.4568777161905970274 ) ) ;
#38721=CARTESIAN_POINT ( 'NONE',  ( 0.3609052982223109884, -1.620655244094860947, -0.5155029497116575543 ) ) ;
#38725=CARTESIAN_POINT ( 'NONE',  ( 0.3699999999999786793, -2.166079853131637645, -0.5407606602423824516 ) ) ;
#38730=CARTESIAN_POINT ( 'NONE',  ( 0.2063161596972083733, -1.283719858747340625, -0.6406645764433035461 ) ) ;
#38739=CARTESIAN_POINT ( 'NONE',  ( 0.4101084439245127333, -1.675243471201324663, -0.5124304843287676992 ) ) ;
#38750=ORIENTED_EDGE ( 'NONE', *, *, #16428, .T. ) ;
#38756=CARTESIAN_POINT ( 'NONE',  ( 0.1424029337235096226, -1.400533250147911746, -0.6250000000000000000 ) ) ;
#38772=CARTESIAN_POINT ( 'NONE',  ( 0.02999999999990876631, -2.097675084551054336, -0.7286989150923646186 ) ) ;
#38783=DIRECTION ( 'NONE',  ( 0.8660512985181133550, 0.4999551463232372317, 0.000000000000000000 ) ) ;
#38791=CARTESIAN_POINT ( 'NONE',  ( 0.1907077899473081650, -1.700082312857616351, -0.3588694632811901819 ) ) ;
#38803=CARTESIAN_POINT ( 'NONE',  ( 0.4175449395041774814, -1.738216479897680244, -0.4268450903248972028 ) ) ;
#38806=AXIS2_PLACEMENT_3D ( 'NONE', #31018, #40485, #18276 ) ;
#38815=EDGE_CURVE ( 'NONE', #27374, #28606, #24667, .T. ) ;
#38816=FACE_OUTER_BOUND ( 'NONE', #39974, .T. ) ;
#38823=CARTESIAN_POINT ( 'NONE',  ( 0.5875325861083496859, -1.566157533570999627, -0.5429603524405962611 ) ) ;
#38825=CIRCLE ( 'NONE', #2050, 0.08830708661417338567 ) ;
#38828=ORIENTED_EDGE ( 'NONE', *, *, #16685, .F. ) ;
#38830=AXIS2_PLACEMENT_3D ( 'NONE', #11830, #36927, #30958 ) ;
#38832=DIRECTION ( 'NONE',  ( -1.000000000000000000, 0.000000000000000000, 0.000000000000000000 ) ) ;
#38839=ORIENTED_EDGE ( 'NONE', *, *, #29817, .F. ) ;
#38841=FACE_OUTER_BOUND ( 'NONE', #3936, .T. ) ;
#38843=ORIENTED_EDGE ( 'NONE', *, *, #35867, .F. ) ;
#38849=CARTESIAN_POINT ( 'NONE',  ( 0.08942791728960713948, -1.375947154762177105, -0.3595196034401970664 ) ) ;
#38851=DIRECTION ( 'NONE',  ( 1.000000000000000000, 0.000000000000000000, 0.000000000000000000 ) ) ;
#38852=CARTESIAN_POINT ( 'NONE',  ( 0.3484951945142048535, -1.627819363848378220, -0.3328913857909800433 ) ) ;
#38857=AXIS2_PLACEMENT_3D ( 'NONE', #10837, #4441, #17001 ) ;
#38863=CIRCLE ( 'NONE', #262, 0.05330708661417342398 ) ;
#38864=DIRECTION ( 'NONE',  ( 1.000000000000000000, 0.000000000000000000, 0.000000000000000000 ) ) ;
#38867=AXIS2_PLACEMENT_3D ( 'NONE', #19068, #25238, #6697 ) ;
#38868=EDGE_CURVE ( 'NONE', #8591, #25449, #6338, .T. ) ;
#38871=DIRECTION ( 'NONE',  ( 0.9344312650838934031, 0.2480862795823838285, 0.2555218360858536597 ) ) ;
#38874=CARTESIAN_POINT ( 'NONE',  ( 0.4382015218937659884, -1.612541052972227940, -0.6615483979663951963 ) ) ;
#38875=CARTESIAN_POINT ( 'NONE',  ( 0.3624136781422674924, -1.762859772815410508, -0.5929287727032674926 ) ) ;
#38895=ORIENTED_EDGE ( 'NONE', *, *, #29866, .T. ) ;
#38900=CARTESIAN_POINT ( 'NONE',  ( 0.6271571286872942297, -1.601904976971373795, -0.4537812407007095206 ) ) ;
#38913=FACE_OUTER_BOUND ( 'NONE', #19605, .T. ) ;
#38919=( LENGTH_UNIT ( ) NAMED_UNIT ( * ) SI_UNIT ( $, .METRE. ) );
#38923=CARTESIAN_POINT ( 'NONE',  ( 0.6209938526331848507, -1.607187025150189186, -0.4652530029513053389 ) ) ;
#38931=CIRCLE ( 'NONE', #36964, 0.02999999999999998501 ) ;
#38934=AXIS2_PLACEMENT_3D ( 'NONE', #15958, #38158, #35470 ) ;
#38936=CARTESIAN_POINT ( 'NONE',  ( 0.3159174789885340617, -1.473577620167767277, -0.7462941026102613007 ) ) ;
#38940=CARTESIAN_POINT ( 'NONE',  ( 0.6431982980546400164, -1.414041713902329356, -0.6250000000000000000 ) ) ;
#38943=CARTESIAN_POINT ( 'NONE',  ( 0.3395132021710796644, -1.113556448477543981, -0.5155029497116575543 ) ) ;
#38945=EDGE_LOOP ( 'NONE', ( #29198, #15645, #12241, #35771 ) ) ;
#38947=CARTESIAN_POINT ( 'NONE',  ( 0.001082033974601749821, -1.915745596563056985, -0.6835195572584209511 ) ) ;
#38949=ORIENTED_EDGE ( 'NONE', *, *, #8112, .F. ) ;
#38950=CARTESIAN_POINT ( 'NONE',  ( 0.1999999999999765299, -2.090543227368257373, -0.6941777981885114412 ) ) ;
#38951=CARTESIAN_POINT ( 'NONE',  ( 0.4697623592636160361, -1.061459377010899541, -0.6056023639864149821 ) ) ;
#38954=ORIENTED_EDGE ( 'NONE', *, *, #38550, .F. ) ;
#38970=CARTESIAN_POINT ( 'NONE',  ( 0.2246635286622190308, -1.191403667735409178, -0.5155029497116575543 ) ) ;
#38971=EDGE_CURVE ( 'NONE', #26971, #39255, #38410, .T. ) ;
#38979=CARTESIAN_POINT ( 'NONE',  ( 0.06646545803895723137, -1.528777460197568328, -0.3435740225710798845 ) ) ;
#38980=CARTESIAN_POINT ( 'NONE',  ( 0.4885114638772957707, -1.656959017372544807, -0.6069631137146730415 ) ) ;
#38989=CARTESIAN_POINT ( 'NONE',  ( 0.3612374285823241049, -1.754314597143267429, -0.4836476399974993789 ) ) ;
#38994=DIRECTION ( 'NONE',  ( -0.4999551463232385085, 0.8660512985181127998, 0.000000000000000000 ) ) ;
#38997=CARTESIAN_POINT ( 'NONE',  ( 0.4751758298663427693, -1.652426242819087010, -0.6334442537810193175 ) ) ;
#39002=CARTESIAN_POINT ( 'NONE',  ( 0.5722472701422883778, -1.544651279766090957, -0.4985846812144399398 ) ) ;
#39010=EDGE_LOOP ( 'NONE', ( #7021, #27033 ) ) ;
#39011=AXIS2_PLACEMENT_3D ( 'NONE', #22423, #6156, #18720 ) ;
#39015=DIRECTION ( 'NONE',  ( 1.000000000000000000, 0.000000000000000000, 0.000000000000000000 ) ) ;
#39022=CARTESIAN_POINT ( 'NONE',  ( 0.3968672699137553161, -1.750153310133208739, -0.5142725273527540830 ) ) ;
#39027=CARTESIAN_POINT ( 'NONE',  ( 0.1424029337235096226, -1.400533250147911746, -0.3552704771134632677 ) ) ;
#39030=CARTESIAN_POINT ( 'NONE',  ( 0.6433013898879852421, -1.424917313305586131, -0.6283493189352619135 ) ) ;
#39035=( BOUNDED_SURFACE ( )  B_SPLINE_SURFACE ( 3, 2, ( 
 ( #32307, #28641, #19175 ),
 ( #512, #1097, #34791 ),
 ( #6809, #13606, #23079 ),
 ( #19985, #32516, #4338 ),
 ( #16899, #6594, #3534 ),
 ( #16298, #13006, #31926 ),
 ( #28836, #694, #37779 ),
 ( #28128, #184, #37984 ),
 ( #781, #3036, #12676 ),
 ( #24848, #399, #38176 ),
 ( #9794, #34281, #6089 ),
 ( #16194, #9600, #22177 ) ),
 .UNSPECIFIED., .F., .F., .T. ) 
 B_SPLINE_SURFACE_WITH_KNOTS ( ( 4, 2, 2, 2, 2, 4 ),
 ( 3, 3 ),
 ( 0.000000000000000000, 0.0009332466819807876948, 0.001399870022971181488, 0.001866493363961575390, 0.002799740045942362976, 0.003732986727923150779 ),
 ( 0.000000000000000000, 1.000000000000000000 ),
 .UNSPECIFIED. ) 
 GEOMETRIC_REPRESENTATION_ITEM ( )  RATIONAL_B_SPLINE_SURFACE ( (
 ( 1.000000000000000000, 0.8102556146343726784, 1.000000000000000000),
 ( 1.000000000000000000, 0.8006762349670663026, 1.000000000000000000),
 ( 1.000000000000000000, 0.7913450566296021949, 1.000000000000000000),
 ( 1.000000000000000000, 0.7775533969568005910, 1.000000000000000000),
 ( 1.000000000000000000, 0.7729619784068304522, 1.000000000000000000),
 ( 1.000000000000000000, 0.7640664544802193703, 1.000000000000000000),
 ( 1.000000000000000000, 0.7597351442530375643, 1.000000000000000000),
 ( 1.000000000000000000, 0.7469609109291713844, 1.000000000000000000),
 ( 1.000000000000000000, 0.7386488374089775766, 1.000000000000000000),
 ( 1.000000000000000000, 0.7225489873383396100, 1.000000000000000000),
 ( 1.000000000000000000, 0.7144344824572226305, 1.000000000000000000),
 ( 1.000000000000000000, 0.7071067811865492381, 1.000000000000000000) ) ) 
 REPRESENTATION_ITEM ( '' )  SURFACE ( )  );
#39037=CARTESIAN_POINT ( 'NONE',  ( 0.5927337715469158663, -1.512431713927492316, -0.6345249349069799205 ) ) ;
#39045=ORIENTED_EDGE ( 'NONE', *, *, #37336, .F. ) ;
#39052=CARTESIAN_POINT ( 'NONE',  ( 0.3460467764047484573, -1.678194475986896084, -0.4563891808276777096 ) ) ;
#39060=EDGE_LOOP ( 'NONE', ( #37419, #30234, #10558, #9048, #4519, #9680 ) ) ;
#39063=ORIENTED_EDGE ( 'NONE', *, *, #22536, .F. ) ;
#39070=CARTESIAN_POINT ( 'NONE',  ( -2.106084062615542560E-14, -2.087756091470926556, -0.2623975632731757046 ) ) ;
#39072=ADVANCED_FACE ( 'NONE', ( #24789 ), #24365, .T. ) ;
#39074=CARTESIAN_POINT ( 'NONE',  ( 0.001120486222623293246, -1.913917409099062272, -0.6537566358931722332 ) ) ;
#39083=FACE_OUTER_BOUND ( 'NONE', #17859, .T. ) ;
#39095=DIRECTION ( 'NONE',  ( 0.000000000000000000, 0.000000000000000000, -1.000000000000000000 ) ) ;
#39096=CARTESIAN_POINT ( 'NONE',  ( 0.3613982139085152312, -1.770628929897791526, -0.5799859875462475278 ) ) ;
#39104=CARTESIAN_POINT ( 'NONE',  ( 0.4620955415748976280, -1.655440927177989963, -0.3953929602407867949 ) ) ;
#39110=ORIENTED_EDGE ( 'NONE', *, *, #18256, .T. ) ;
#39112=EDGE_CURVE ( 'NONE', #24957, #20339, #21730, .T. ) ;
#39116=DIRECTION ( 'NONE',  ( 0.1858595909941346824, 0.1072932506077139692, -0.9767007580674458289 ) ) ;
#39118=FACE_OUTER_BOUND ( 'NONE', #31666, .T. ) ;
#39137=FACE_OUTER_BOUND ( 'NONE', #33204, .T. ) ;
#39140=DIRECTION ( 'NONE',  ( 0.4999551463232373427, -0.8660512985181134660, 0.000000000000000000 ) ) ;
#39150=CARTESIAN_POINT ( 'NONE',  ( 0.4038123414656494270, -1.648191853347414693, -0.6342846586131767328 ) ) ;
#39156=CARTESIAN_POINT ( 'NONE',  ( 0.2089288257737619836, -1.288245670442317525, -0.6300528582021277524 ) ) ;
#39157=CARTESIAN_POINT ( 'NONE',  ( 0.3949726910288821058, -1.765807112359412567, -0.5057413602038844935 ) ) ;
#39162=ORIENTED_EDGE ( 'NONE', *, *, #16565, .F. ) ;
#39163=CARTESIAN_POINT ( 'NONE',  ( 0.03311111702111442512, -1.809660005586617437, -0.6723719395828864354 ) ) ;
#39193=EDGE_CURVE ( 'NONE', #37380, #12338, #4340, .T. ) ;
#39195=CARTESIAN_POINT ( 'NONE',  ( 0.02999778723028691946, -2.087755359801442445, -0.2623954751430958021 ) ) ;
#39197=CARTESIAN_POINT ( 'NONE',  ( 0.5360167750696916977, -1.632603989559125557, -0.5957800154415829885 ) ) ;
#39206=CARTESIAN_POINT ( 'NONE',  ( 0.2859919059094789273, -1.317642033747133734, -0.5155029497116575543 ) ) ;
#39207=AXIS2_PLACEMENT_3D ( 'NONE', #28341, #26476, #33042 ) ;
#39212=CARTESIAN_POINT ( 'NONE',  ( 0.3771322225225746672, -1.765190303781668968, -0.4446624772603183229 ) ) ;
#39213=CARTESIAN_POINT ( 'NONE',  ( 0.3969700875656382300, -1.750093955434189663, -0.5306525527942058673 ) ) ;
#39217=CARTESIAN_POINT ( 'NONE',  ( 0.3563380670180646970, -1.791703161805209277, -0.4886643292207938361 ) ) ;
#39219=EDGE_LOOP ( 'NONE', ( #34834, #11123, #30102, #2668 ) ) ;
#39228=ORIENTED_EDGE ( 'NONE', *, *, #38540, .F. ) ;
#39230=CARTESIAN_POINT ( 'NONE',  ( -2.112273405726188513E-14, -2.183180860297921466, -0.4937760292030871079 ) ) ;
#39235=CARTESIAN_POINT ( 'NONE',  ( 0.4242133616548363628, -1.734366925052854391, -0.4397180493288433967 ) ) ;
#39237=LINE ( 'NONE', #32652, #4924 ) ;
#39241=CARTESIAN_POINT ( 'NONE',  ( 0.6284115775016231309, -1.542760345567441460, -0.6058523010359371241 ) ) ;
#39247=CARTESIAN_POINT ( 'NONE',  ( 0.5867991090592019621, -1.567604868959546760, -0.5372565133074018728 ) ) ;
#39248=CARTESIAN_POINT ( 'NONE',  ( 0.02999999999910716447, -2.094379624028320563, -0.2600525928522836039 ) ) ;
#39255=VERTEX_POINT ( 'NONE', #7051 ) ;
#39268=DIRECTION ( 'NONE',  ( 0.4999551463232373427, -0.8660512985181134660, 0.000000000000000000 ) ) ;
#39270=CARTESIAN_POINT ( 'NONE',  ( 0.1999999999999781675, -2.107936428766273629, -0.7005084057759864979 ) ) ;
#39287=CARTESIAN_POINT ( 'NONE',  ( 0.1909286924077255310, -1.257064795538239022, -0.3864493710799625781 ) ) ;
#39291=FACE_OUTER_BOUND ( 'NONE', #11277, .T. ) ;
#39294=EDGE_CURVE ( 'NONE', #28758, #39975, #19483, .T. ) ;
#39295=CARTESIAN_POINT ( 'NONE',  ( 0.5264113014007612001, -1.640729993778266893, -0.5166151207188711680 ) ) ;
#39298=ORIENTED_EDGE ( 'NONE', *, *, #10922, .T. ) ;
#39305=ORIENTED_EDGE ( 'NONE', *, *, #13191, .F. ) ;
#39312=CARTESIAN_POINT ( 'NONE',  ( 0.6410892975813305972, -1.609168521141159047, -0.4443638777805624662 ) ) ;
#39315=ORIENTED_EDGE ( 'NONE', *, *, #32187, .T. ) ;
#39316=EDGE_LOOP ( 'NONE', ( #1538, #26742, #19894, #26780, #15678, #12197, #19234, #2540 ) ) ;
#39325=CARTESIAN_POINT ( 'NONE',  ( 0.4039575731531036551, -1.662086776922496734, -0.3578710663349294330 ) ) ;
#39327=DIRECTION ( 'NONE',  ( 0.000000000000000000, 0.3420201433256707668, 0.9396926207859077618 ) ) ;
#39330=CARTESIAN_POINT ( 'NONE',  ( 0.3837623509413576883, -1.658427931343763762, -0.4031416779713772325 ) ) ;
#39340=EDGE_CURVE ( 'NONE', #29449, #29150, #16273, .T. ) ;
#39342=ADVANCED_FACE ( 'NONE', ( #18948 ), #3105, .F. ) ;
#39345=CARTESIAN_POINT ( 'NONE',  ( 0.4697228370620195048, -1.442521976758482261, -0.5166151207188711680 ) ) ;
#39348=CARTESIAN_POINT ( 'NONE',  ( 0.3892111963516278195, -1.924636834596797463, -0.5051628067631914742 ) ) ;
#39350=CARTESIAN_POINT ( 'NONE',  ( 0.5362507510587237736, -1.657686573918387252, -0.4612641151860342181 ) ) ;
#39352=EDGE_LOOP ( 'NONE', ( #35606, #26090, #35728, #1338 ) ) ;
#39354=CARTESIAN_POINT ( 'NONE',  ( 0.02991800254585390284, -1.951451259341335343, -0.6900850705760112058 ) ) ;
#39377=CARTESIAN_POINT ( 'NONE',  ( 0.3870588290862405079, -1.884497726405092832, -0.6962470674797399672 ) ) ;
#39385=ORIENTED_EDGE ( 'NONE', *, *, #13691, .T. ) ;
#39400=EDGE_CURVE ( 'NONE', #38684, #13521, #9637, .T. ) ;
#39404=DIRECTION ( 'NONE',  ( -1.000000000000000000, 0.000000000000000000, 0.000000000000000000 ) ) ;
#39408=CARTESIAN_POINT ( 'NONE',  ( 0.2059273467974225835, -1.283046334493782359, -0.4125659523519145111 ) ) ;
#39410=FACE_OUTER_BOUND ( 'NONE', #21298, .T. ) ;
#39413=CARTESIAN_POINT ( 'NONE',  ( 0.4793242053826342608, -1.117309586606285210, -0.6340321207832128048 ) ) ;
#39417=DIRECTION ( 'NONE',  ( 0.8660512985181135770, 0.4999551463232370652, -1.983296656985675225E-15 ) ) ;
#39422=CARTESIAN_POINT ( 'NONE',  ( 0.3673299760992552176, -1.767204635010063196, -0.4401329826727911620 ) ) ;
#39428=AXIS2_PLACEMENT_3D ( 'NONE', #36804, #8616, #33724 ) ;
#39431=EDGE_CURVE ( 'NONE', #37277, #8591, #504, .T. ) ;
#39432=CARTESIAN_POINT ( 'NONE',  ( 0.6156641970611075321, -1.571178582061410145, -0.5844328501603425208 ) ) ;
#39439=CARTESIAN_POINT ( 'NONE',  ( 0.5752554920797638971, -1.540183446532599643, -0.5501855072907599897 ) ) ;
#39444=CARTESIAN_POINT ( 'NONE',  ( 0.4612498305140941834, -1.075380691928112586, -0.6133311933496794488 ) ) ;
#39453=DIRECTION ( 'NONE',  ( -0.4999551463232372317, 0.8660512985181135770, -0.000000000000000000 ) ) ;
#39455=DIRECTION ( 'NONE',  ( 1.000000000000000000, 0.000000000000000000, 0.000000000000000000 ) ) ;
#39462=CARTESIAN_POINT ( 'NONE',  ( 0.1820341357843785479, -1.296823278962681902, -0.2983537100936060060 ) ) ;
#39463=ORIENTED_EDGE ( 'NONE', *, *, #7001, .T. ) ;
#39465=CARTESIAN_POINT ( 'NONE',  ( 0.0005169533006796693227, -1.951327190372867504, -0.6596122894433742445 ) ) ;
#39469=DIRECTION ( 'NONE',  ( 0.8660512985181134660, 0.4999551463232372872, 0.000000000000000000 ) ) ;
#39483=CARTESIAN_POINT ( 'NONE',  ( 0.3971095453229756544, -1.735560539021580695, -0.5931764296607824338 ) ) ;
#39494=ORIENTED_EDGE ( 'NONE', *, *, #21320, .T. ) ;
#39500=CARTESIAN_POINT ( 'NONE',  ( 0.5444814301263717349, -1.595658467509692313, -0.4724618950513508331 ) ) ;
#39504=CARTESIAN_POINT ( 'NONE',  ( 0.1909293087668044175, -1.257065863231180858, -0.7137147910705018417 ) ) ;
#39519=CARTESIAN_POINT ( 'NONE',  ( 0.1999999999696201736, -2.080276846833732929, -0.2651855839716015795 ) ) ;
#39523=CARTESIAN_POINT ( 'NONE',  ( 0.6121698487542911460, -1.614213617923458521, -0.4893840166461958519 ) ) ;
#39532=AXIS2_PLACEMENT_3D ( 'NONE', #31255, #18693, #15615 ) ;
#39537=CARTESIAN_POINT ( 'NONE',  ( 0.3891966927463759718, -1.924247350197065609, -0.4910180813531025978 ) ) ;
#39543=CARTESIAN_POINT ( 'NONE',  ( 0.02999607453758948092, -2.087869005097287900, -0.7252195465745520098 ) ) ;
#39559=ORIENTED_EDGE ( 'NONE', *, *, #22365, .F. ) ;
#39569=CARTESIAN_POINT ( 'NONE',  ( 0.3675325340839428190, -2.037914281822962081, -0.5035866893277683998 ) ) ;
#39572=CARTESIAN_POINT ( 'NONE',  ( 0.3866324372511995011, -1.865059148935370503, -0.6965146800415932260 ) ) ;
#39575=B_SPLINE_SURFACE_WITH_KNOTS ( 'NONE', 1, 3, ( 
 ( #8906, #40381, #15686, #6418 ),
 ( #21483, #28053, #22096, #15283 ),
 ( #34004, #27444, #28237, #6009 ),
 ( #5808, #2345, #24765, #21669 ) ),
 .UNSPECIFIED., .F., .F., .F.,
 ( 2, 1, 1, 2 ),
 ( 4, 4 ),
 ( -1.012000000000000233, 0.000000000000000000, 1.000000000000000000, 2.018000000000001126 ),
 ( -0.005833846140041338939, 0.005833846140041338071 ),
 .UNSPECIFIED. ) ;
#39580=CARTESIAN_POINT ( 'NONE',  ( 0.1098394514474842348, -1.393562438875942444, -0.3305732284332606463 ) ) ;
#39581=CARTESIAN_POINT ( 'NONE',  ( 0.4491687606894799178, -1.659573487732471264, -0.3947185122250792544 ) ) ;
#39606=ORIENTED_EDGE ( 'NONE', *, *, #7735, .F. ) ;
#39610=AXIS2_PLACEMENT_3D ( 'NONE', #22818, #811, #37817 ) ;
#39614=ORIENTED_EDGE ( 'NONE', *, *, #6855, .T. ) ;
#39618=ADVANCED_FACE ( 'NONE', ( #3245 ), #31438, .T. ) ;
#39625=CIRCLE ( 'NONE', #917, 0.1033070866141734129 ) ;
#39627=CARTESIAN_POINT ( 'NONE',  ( 0.3862498284634955925, -1.756282559639558372, -0.4621846277522613233 ) ) ;
#39634=CARTESIAN_POINT ( 'NONE',  ( 0.6013563731205958662, -1.595925901742404562, -0.5276017758477205000 ) ) ;
#39635=CARTESIAN_POINT ( 'NONE',  ( 0.4570244656720055532, -1.686924280111764984, -0.6191500722721138272 ) ) ;
#39636=CARTESIAN_POINT ( 'NONE',  ( 0.02999999999997910935, -2.094376243145855465, -0.2600538233928666454 ) ) ;
#39642=FACE_OUTER_BOUND ( 'NONE', #14367, .T. ) ;
#39646=CARTESIAN_POINT ( 'NONE',  ( 0.4806378395295555772, -1.105637800341301880, -0.6194292131661300882 ) ) ;
#39650=CARTESIAN_POINT ( 'NONE',  ( 0.6118928672170725891, -1.553152052717160281, -0.4073905701233934695 ) ) ;
#39651=AXIS2_PLACEMENT_3D ( 'NONE', #28468, #16146, #3784 ) ;
#39657=CARTESIAN_POINT ( 'NONE',  ( 0.02880027917499857273, -1.580366911349619263, -0.3737892410411999822 ) ) ;
#39658=VERTEX_POINT ( 'NONE', #26278 ) ;
#39666=EDGE_CURVE ( 'NONE', #23391, #8354, #24776, .T. ) ;
#39669=AXIS2_PLACEMENT_3D ( 'NONE', #7791, #18415, #34058 ) ;
#39670=CARTESIAN_POINT ( 'NONE',  ( 0.1356587054898548694, -1.302826366429101324, -0.6902430740193704617 ) ) ;
#39681=CARTESIAN_POINT ( 'NONE',  ( 0.4093192649698302321, -1.477391824278450061, -0.5625509170971489947 ) ) ;
#39684=CIRCLE ( 'NONE', #4843, 0.01000000000000002970 ) ;
#39689=VECTOR ( 'NONE', #14302, 39.37007874015748854 ) ;
#39694=CARTESIAN_POINT ( 'NONE',  ( 0.3979561296664244630, -2.043052950745618990, -0.5098141394919292191 ) ) ;
#39696=PLANE ( 'NONE',  #11822 ) ;
#39702=ORIENTED_EDGE ( 'NONE', *, *, #34902, .T. ) ;
#39705=ORIENTED_EDGE ( 'NONE', *, *, #12181, .T. ) ;
#39707=ORIENTED_EDGE ( 'NONE', *, *, #8735, .F. ) ;
#39709=ORIENTED_EDGE ( 'NONE', *, *, #16428, .F. ) ;
#39719=ORIENTED_EDGE ( 'NONE', *, *, #15527, .F. ) ;
#39729=DIRECTION ( 'NONE',  ( 0.000000000000000000, -0.9629711830670020234, -0.2696043408080414094 ) ) ;
#39730=CARTESIAN_POINT ( 'NONE',  ( 0.3857581439227468767, -1.748739094004719163, -0.4525101959494370329 ) ) ;
#39745=AXIS2_PLACEMENT_3D ( 'NONE', #18009, #30570, #2395 ) ;
#39746=ADVANCED_FACE ( 'NONE', ( #7745 ), #29756, .F. ) ;
#39749=LINE ( 'NONE', #33779, #14705 ) ;
#39750=CARTESIAN_POINT ( 'NONE',  ( 0.3622253751127866295, -1.756884464425455761, -0.4902987826081470213 ) ) ;
#39752=CARTESIAN_POINT ( 'NONE',  ( 0.3402959632056916650, -1.632552626064600165, -0.5940485371126216219 ) ) ;
#39756=CARTESIAN_POINT ( 'NONE',  ( 0.3829978824168507878, -1.758159847006225407, -0.4469636835181319268 ) ) ;
#39757=CARTESIAN_POINT ( 'NONE',  ( 0.3892048212403190210, -1.924453948264585046, -0.4980904138457005192 ) ) ;
#39760=AXIS2_PLACEMENT_3D ( 'NONE', #6534, #3466, #31450 ) ;
#39763=VERTEX_POINT ( 'NONE', #11451 ) ;
#39764=CARTESIAN_POINT ( 'NONE',  ( 0.1517790575129573938, -1.325739146886562247, -0.7195016053274172485 ) ) ;
#39783=CARTESIAN_POINT ( 'NONE',  ( 0.3699999999999786793, -2.097675824466503691, -0.5028176662824495047 ) ) ;
#39785=LENGTH_MEASURE_WITH_UNIT ( LENGTH_MEASURE( 0.02539999999999999897 ), #14688 );
#39787=CARTESIAN_POINT ( 'NONE',  ( 0.2047211543538725864, -1.633415721624318362, -0.6910012992593033143 ) ) ;
#39802=EDGE_CURVE ( 'NONE', #7589, #8591, #22144, .T. ) ;
#39814=CARTESIAN_POINT ( 'NONE',  ( 0.1925402117207221098, -1.964586866904750151, -0.2961055278315678496 ) ) ;
#39817=CARTESIAN_POINT ( 'NONE',  ( 0.1909286924077255032, -1.257064795538239022, -0.5931747813493344346 ) ) ;
#39821=CARTESIAN_POINT ( 'NONE',  ( 0.1999999999999789724, -2.183180860297921466, -0.5437760292030870968 ) ) ;
#39830=ORIENTED_EDGE ( 'NONE', *, *, #1678, .F. ) ;
#39832=CARTESIAN_POINT ( 'NONE',  ( 0.1794004326756924173, -1.813331030036754887, -0.3207468061039889795 ) ) ;
#39840=B_SPLINE_CURVE_WITH_KNOTS ( 'NONE', 3,
 ( #19866, #28731, #19476, #22780, #1184, #19663 ),
 .UNSPECIFIED., .F., .F.,
 ( 4, 2, 4 ),
 ( 0.000000000000000000, 0.0007279435479977064503, 0.001455887095995412901 ),
 .UNSPECIFIED. ) ;
#39846=CARTESIAN_POINT ( 'NONE',  ( 0.6165909760827519293, -1.623179156379430887, -0.5076586781594308873 ) ) ;
#39853=ADVANCED_FACE ( 'NONE', ( #8756 ), #25114, .T. ) ;
#39855=CARTESIAN_POINT ( 'NONE',  ( 0.3662247033611901181, -1.729352955075043941, -0.6047395896534266679 ) ) ;
#39857=CARTESIAN_POINT ( 'NONE',  ( 0.4262438152663739488, -1.592651821845864069, -0.6151431148613255573 ) ) ;
#39861=CARTESIAN_POINT ( 'NONE',  ( 0.4480646913441766466, -1.099213350020603386, -0.6275147848854657484 ) ) ;
#39867=ORIENTED_EDGE ( 'NONE', *, *, #6675, .F. ) ;
#39871=CARTESIAN_POINT ( 'NONE',  ( 0.04398552291027794936, -1.506617454199507433, -0.3728714820311309630 ) ) ;
#39879=CARTESIAN_POINT ( 'NONE',  ( 0.5264113014007612001, -1.640729993778266893, -0.5166151207188711680 ) ) ;
#39889=CARTESIAN_POINT ( 'NONE',  ( 0.4534978277988769846, -1.047755265242954037, -0.5155029497116575543 ) ) ;
#39905=ADVANCED_FACE ( 'NONE', ( #1309 ), #33495, .T. ) ;
#39906=ORIENTED_EDGE ( 'NONE', *, *, #39294, .F. ) ;
#39910=EDGE_CURVE ( 'NONE', #2065, #29909, #234, .T. ) ;
#39911=DIRECTION ( 'NONE',  ( 0.6377491006683481123, 0.000000000000000000, 0.7702441720628031563 ) ) ;
#39914=B_SPLINE_CURVE_WITH_KNOTS ( 'NONE', 3,
 ( #6770, #38243, #1444, #9862, #19348, #31886, #22648 ),
 .UNSPECIFIED., .F., .F.,
 ( 4, 3, 4 ),
 ( 0.003048000018042928624, 0.003429000018037117996, 0.003810000018031183770 ),
 .UNSPECIFIED. ) ;
#39924=ADVANCED_FACE ( 'NONE', ( #38913 ), #5373, .F. ) ;
#39929=EDGE_CURVE ( 'NONE', #17084, #2063, #903, .T. ) ;
#39931=B_SPLINE_SURFACE_WITH_KNOTS ( 'NONE', 3, 1, ( 
 ( #1700, #10945 ),
 ( #33139, #36430 ),
 ( #14218, #23902 ),
 ( #20818, #13614 ) ),
 .UNSPECIFIED., .F., .F., .F.,
 ( 4, 4 ),
 ( 2, 2 ),
 ( 0.000000000000000000, 1.000000000000000000 ),
 ( 0.000000000000000000, 1.000000000000000000 ),
 .UNSPECIFIED. ) ;
#39935=DIRECTION ( 'NONE',  ( 0.4999551463232372317, -0.8660512985181135770, 0.000000000000000000 ) ) ;
#39936=CARTESIAN_POINT ( 'NONE',  ( 0.4185715608678379218, -1.702044260100491924, -0.4179452547514317384 ) ) ;
#39939=CARTESIAN_POINT ( 'NONE',  ( 0.2409193767872376546, -1.343661558146008073, -0.2869361388274795921 ) ) ;
#39941=DIRECTION ( 'NONE',  ( 0.8660512985181140211, 0.4999551463232362880, 0.000000000000000000 ) ) ;
#39948=CARTESIAN_POINT ( 'NONE',  ( 0.4149016700119600998, -1.651544695139487429, -0.6216189332891878250 ) ) ;
#39949=EDGE_CURVE ( 'NONE', #23858, #5039, #25592, .T. ) ;
#39951=CARTESIAN_POINT ( 'NONE',  ( 0.3526243232178313258, -1.728525448788969410, -0.4459625336182188593 ) ) ;
#39952=ORIENTED_EDGE ( 'NONE', *, *, #160, .F. ) ;
#39956=CARTESIAN_POINT ( 'NONE',  ( 0.3804922947572159653, -1.758905690526931354, -0.4436857796392575382 ) ) ;
#39957=DIRECTION ( 'NONE',  ( 0.4999551463232372317, -0.8660512985181135770, 0.000000000000000000 ) ) ;
#39958=VERTEX_POINT ( 'NONE', #30688 ) ;
#39974=EDGE_LOOP ( 'NONE', ( #31170, #20061, #36167, #9454 ) ) ;
#39975=VERTEX_POINT ( 'NONE', #20830 ) ;
#39981=CARTESIAN_POINT ( 'NONE',  ( 0.07991135521492878646, -1.395945580162383459, -0.6589646420266501714 ) ) ;
#39988=CARTESIAN_POINT ( 'NONE',  ( 0.3699999999999784572, -2.097675824466503691, -0.5196396315034579327 ) ) ;
#39993=DIRECTION ( 'NONE',  ( 0.8660512985181132439, 0.4999551463232376758, 0.000000000000000000 ) ) ;
#39995=ORIENTED_EDGE ( 'NONE', *, *, #39802, .T. ) ;
#40003=CARTESIAN_POINT ( 'NONE',  ( 0.3690773559837012274, -2.063460311930843449, -0.4759771606218671236 ) ) ;
#40020=CARTESIAN_POINT ( 'NONE',  ( 0.4011831001776828831, -1.742810116944001786, -0.5289609113168958210 ) ) ;
#40032=CARTESIAN_POINT ( 'NONE',  ( 0.6536459824712800293, -1.536535929646544618, -0.4156460142788562795 ) ) ;
#40033=CARTESIAN_POINT ( 'NONE',  ( 0.4781934768423676818, -1.682642038360962600, -0.6151431148613257793 ) ) ;
#40036=CARTESIAN_POINT ( 'NONE',  ( 0.3748245490824459458, -1.104718531341411625, -0.5155029497116575543 ) ) ;
#40040=CARTESIAN_POINT ( 'NONE',  ( 0.3653812862022917662, -1.748582203572395466, -0.5147731941186001192 ) ) ;
#40041=CARTESIAN_POINT ( 'NONE',  ( 0.4132813002760061249, -1.705586778321113384, -0.6106085670228335038 ) ) ;
#40043=CARTESIAN_POINT ( 'NONE',  ( 0.3699999999999786238, -2.086845765202261394, -0.4708431600348449431 ) ) ;
#40055=CARTESIAN_POINT ( 'NONE',  ( 0.4634712904840416203, -1.711704060178988129, -0.5155029497116575543 ) ) ;
#40056=ORIENTED_EDGE ( 'NONE', *, *, #7371, .F. ) ;
#40061=CARTESIAN_POINT ( 'NONE',  ( 0.1768282059192854694, -1.460166703081138273, -0.3235079468584903251 ) ) ;
#40066=VERTEX_POINT ( 'NONE', #27197 ) ;
#40070=CIRCLE ( 'NONE', #34814, 0.01500000000000002200 ) ;
#40071=CARTESIAN_POINT ( 'NONE',  ( 0.02901502440408285088, -1.579081040833445249, -0.3765017618882691153 ) ) ;
#40083=PLANE ( 'NONE',  #31739 ) ;
#40089=CARTESIAN_POINT ( 'NONE',  ( 0.3625960434667531151, -1.762758894398492204, -0.5926935080085831142 ) ) ;
#40094=ORIENTED_EDGE ( 'NONE', *, *, #277, .F. ) ;
#40101=VERTEX_POINT ( 'NONE', #623 ) ;
#40108=CARTESIAN_POINT ( 'NONE',  ( 0.2776126715564697367, -1.634751399283275175, -0.3585985592053876903 ) ) ;
#40121=ADVANCED_FACE ( 'NONE', ( #16225 ), #25151, .T. ) ;
#40124=CARTESIAN_POINT ( 'NONE',  ( 0.4070925130139965153, -1.744250469367210288, -0.5784223492323977700 ) ) ;
#40126=CARTESIAN_POINT ( 'NONE',  ( 0.3811251628308546802, -1.654782503697128870, -0.6335434503995712729 ) ) ;
#40129=DIRECTION ( 'NONE',  ( 0.8660512985181134660, 0.4999551463232372317, 0.000000000000000000 ) ) ;
#40139=EDGE_CURVE ( 'NONE', #17084, #1239, #31082, .T. ) ;
#40162=ORIENTED_EDGE ( 'NONE', *, *, #37872, .F. ) ;
#40177=CARTESIAN_POINT ( 'NONE',  ( 0.3798895702152447762, -1.759032899055416266, -0.4429027949815931287 ) ) ;
#40183=TOROIDAL_SURFACE ( 'NONE', #38224, 0.1333070866141732314, 0.02999999999999999889 ) ;
#40188=CARTESIAN_POINT ( 'NONE',  ( 0.3665398960025421093, -2.019035390486545900, -0.6774619758396681624 ) ) ;
#40189=ADVANCED_FACE ( 'NONE', ( #19695 ), #12022, .T. ) ;
#40192=ORIENTED_EDGE ( 'NONE', *, *, #34631, .T. ) ;
#40201=CARTESIAN_POINT ( 'NONE',  ( -2.115421433687637455E-14, -2.107936428766274073, -0.7005084057759867200 ) ) ;
#40204=CARTESIAN_POINT ( 'NONE',  ( 0.3607082371247617436, -1.790100760104569311, -0.5255749062586634324 ) ) ;
#40205=CARTESIAN_POINT ( 'NONE',  ( 0.3926032618789407347, -1.756026311479913948, -0.5284552501753293496 ) ) ;
#40207=DIRECTION ( 'NONE',  ( -0.4999551463232349002, 0.8660512985181147982, 0.000000000000000000 ) ) ;
#40220=CARTESIAN_POINT ( 'NONE',  ( 0.3699999999999786793, -2.143487347926988917, -0.5325376609224018454 ) ) ;
#40224=CARTESIAN_POINT ( 'NONE',  ( 0.3958974862128058492, -2.004956072359079133, -0.2856428411439917436 ) ) ;
#40230=CARTESIAN_POINT ( 'NONE',  ( 0.2059273467974223892, -1.283046334493782137, -0.3404751839154473436 ) ) ;
#40238=CARTESIAN_POINT ( 'NONE',  ( 0.6348547142568438106, -1.593451324377852751, -0.4417161348974741886 ) ) ;
#40239=DIRECTION ( 'NONE',  ( -0.4999551463232373427, 0.8660512985181134660, -0.000000000000000000 ) ) ;
#40244=ORIENTED_EDGE ( 'NONE', *, *, #7018, .F. ) ;
#40245=CARTESIAN_POINT ( 'NONE',  ( 0.3597460184446273357, -1.737228056197862802, -0.5031880851714581881 ) ) ;
#40246=CARTESIAN_POINT ( 'NONE',  ( 0.3711010767056441284, -1.714876091213238807, -0.6102747157238272990 ) ) ;
#40247=CIRCLE ( 'NONE', #12647, 0.02999999999999995726 ) ;
#40248=CARTESIAN_POINT ( 'NONE',  ( 0.2772481421372381960, -1.634119940283012662, -0.3262497153171022291 ) ) ;
#40252=ORIENTED_EDGE ( 'NONE', *, *, #11210, .F. ) ;
#40254=CIRCLE ( 'NONE', #4106, 0.02999999999999994685 ) ;
#40260=CARTESIAN_POINT ( 'NONE',  ( 0.4997267776899617653, -1.607290330535514178, -0.6302284990903240791 ) ) ;
#40264=CARTESIAN_POINT ( 'NONE',  ( 0.1239988516143644831, -1.317835488908686292, -0.3462032427497062081 ) ) ;
#40265=EDGE_LOOP ( 'NONE', ( #10979, #7065, #5756, #12242 ) ) ;
#40268=CYLINDRICAL_SURFACE ( 'NONE', #4646, 0.2200000000000000566 ) ;
#40271=B_SPLINE_CURVE_WITH_KNOTS ( 'NONE', 3,
 ( #4099, #32486, #26332, #16666 ),
 .UNSPECIFIED., .F., .F.,
 ( 4, 4 ),
 ( 0.000000000000000000, 0.0002307501183058325222 ),
 .UNSPECIFIED. ) ;
#40278=CARTESIAN_POINT ( 'NONE',  ( 0.2145146395178117171, -1.464440183438808774, -0.3485064432216347097 ) ) ;
#40282=CARTESIAN_POINT ( 'NONE',  ( 0.2842326993135958491, -1.549395603922553155, -0.7208999815284671264 ) ) ;
#40283=CARTESIAN_POINT ( 'NONE',  ( 0.5963593927077359691, -1.484732018227884254, -0.3901058962264565833 ) ) ;
#40289=CARTESIAN_POINT ( 'NONE',  ( 0.2484857473122376870, -1.339293634572156000, -0.5155029497116575543 ) ) ;
#40303=EDGE_CURVE ( 'NONE', #22699, #2897, #40254, .T. ) ;
#40305=ORIENTED_EDGE ( 'NONE', *, *, #22571, .F. ) ;
#40306=VECTOR ( 'NONE', #21759, 39.37007874015748143 ) ;
#40310=DIRECTION ( 'NONE',  ( 1.000000000000000000, 0.000000000000000000, 0.000000000000000000 ) ) ;
#40314=ORIENTED_EDGE ( 'NONE', *, *, #37343, .F. ) ;
#40315=EDGE_CURVE ( 'NONE', #34414, #7674, #3014, .T. ) ;
#40325=ORIENTED_EDGE ( 'NONE', *, *, #16488, .F. ) ;
#40327=CARTESIAN_POINT ( 'NONE',  ( 0.4492124018919768091, -1.095000438762474770, -0.4070882247511642960 ) ) ;
#40333=CARTESIAN_POINT ( 'NONE',  ( 0.5136163780680810254, -1.682756243065421264, -0.4473473192910925600 ) ) ;
#40338=CARTESIAN_POINT ( 'NONE',  ( 0.4500303265696325439, -1.093663202047157501, -0.4076127662389720796 ) ) ;
#40343=DIRECTION ( 'NONE',  ( 0.8660512985181126888, 0.4999551463232385085, 0.000000000000000000 ) ) ;
#40354=( BOUNDED_SURFACE ( )  B_SPLINE_SURFACE ( 3, 2, ( 
 ( #11595, #36682, #24158 ),
 ( #8488, #5389, #17950 ),
 ( #15074, #27627, #8901 ),
 ( #10467, #28982, #24758 ),
 ( #13354, #26134, #2939 ),
 ( #31336, #12590, #10287 ),
 ( #23034, #18568, #16647 ),
 ( #32261, #21663, #37474 ),
 ( #25930, #12391, #40372 ),
 ( #94, #37280, #12199 ),
 ( #25150, #15681, #18978 ),
 ( #3321, #7161, #22089 ),
 ( #34190, #13567, #28044 ),
 ( #19728, #35560, #4080 ) ),
 .UNSPECIFIED., .F., .F., .F. ) 
 B_SPLINE_SURFACE_WITH_KNOTS ( ( 4, 2, 2, 2, 2, 2, 4 ),
 ( 3, 3 ),
 ( -4.206704429243757204E-17, 0.0004898451933843076282, 0.0009796903867686573234, 0.001959380773537356714, 0.002939071160306055887, 0.003428916353690405691, 0.003918761547074755061 ),
 ( 0.000000000000000000, 1.000000000000000000 ),
 .UNSPECIFIED. ) 
 GEOMETRIC_REPRESENTATION_ITEM ( )  RATIONAL_B_SPLINE_SURFACE ( (
 ( 1.000000000000000000, 0.9252764552802091869, 1.000000000000000000),
 ( 1.000000000000000000, 0.9190038079521950509, 1.000000000000000000),
 ( 1.000000000000000000, 0.9096443980271025076, 1.000000000000000000),
 ( 1.000000000000000000, 0.8863278643288117209, 1.000000000000000000),
 ( 1.000000000000000000, 0.8722306840293051478, 1.000000000000000000),
 ( 1.000000000000000000, 0.8255155620659062610, 1.000000000000000000),
 ( 1.000000000000000000, 0.7882493034320124936, 1.000000000000000000),
 ( 1.000000000000000000, 0.7036029670101283662, 1.000000000000000000),
 ( 1.000000000000000000, 0.6557983909466532646, 1.000000000000000000),
 ( 1.000000000000000000, 0.5799777945462297746, 1.000000000000000000),
 ( 1.000000000000000000, 0.5540012513858809662, 1.000000000000000000),
 ( 1.000000000000000000, 0.5013758867234165972, 1.000000000000000000),
 ( 1.000000000000000000, 0.4747208180995389215, 1.000000000000000000),
 ( 1.000000000000000000, 0.4483291926237085723, 1.000000000000000000) ) ) 
 REPRESENTATION_ITEM ( '' )  SURFACE ( )  );
#40355=CARTESIAN_POINT ( 'NONE',  ( 0.3397077535880360100, -1.654685348432988645, -0.3858274525146624390 ) ) ;
#40369=CARTESIAN_POINT ( 'NONE',  ( 0.1653577314264058906, -1.273224196838065314, -0.7336113246882153271 ) ) ;
#40372=CARTESIAN_POINT ( 'NONE',  ( 0.3408647536708550585, -1.672462434926486941, -0.5723210365178634795 ) ) ;
#40379=AXIS2_PLACEMENT_3D ( 'NONE', #23915, #8257, #21020 ) ;
#40381=CARTESIAN_POINT ( 'NONE',  ( 0.1757500541653520265, -1.230771478115229245, -0.5931747813493342125 ) ) ;
#40384=CARTESIAN_POINT ( 'NONE',  ( 0.02999999999997886302, -2.183180860297921466, -0.4937760292030871079 ) ) ;
#40387=VERTEX_POINT ( 'NONE', #7081 ) ;
#40392=DIRECTION ( 'NONE',  ( 0.4999551463232372317, -0.8660512985181134660, 0.000000000000000000 ) ) ;
#40394=CARTESIAN_POINT ( 'NONE',  ( 0.3826622209723776757, -1.758353618053019041, -0.4465348687276735062 ) ) ;
#40396=CARTESIAN_POINT ( 'NONE',  ( 0.09587768265485864527, -1.362549125761861823, -0.6668472307072548233 ) ) ;
#40403=CARTESIAN_POINT ( 'NONE',  ( 0.3697988629570628794, -1.737277537897635948, -0.6804030624709919151 ) ) ;
#40404=TOROIDAL_SURFACE ( 'NONE', #6890, 0.05330708661417342398, 0.01000000000000000021 ) ;
#40407=EDGE_LOOP ( 'NONE', ( #7772, #34309, #642, #690, #3103, #18102 ) ) ;
#40408=CARTESIAN_POINT ( 'NONE',  ( 0.4121964764379724144, -1.591045810388358905, -0.3442890830420804460 ) ) ;
#40409=CARTESIAN_POINT ( 'NONE',  ( 0.1999999999999789724, -2.183180860297921466, -0.4937760292030871079 ) ) ;
#40415=EDGE_LOOP ( 'NONE', ( #6519, #31330, #31440, #7413, #33992, #27767, #3649, #4944, #29508, #28587, #37141, #38053, #17742 ) ) ;
#40420=CARTESIAN_POINT ( 'NONE',  ( 0.3663367775733478715, -2.020566543745489607, -0.4857000487067979488 ) ) ;
#40423=CARTESIAN_POINT ( 'NONE',  ( 0.1757500541653520265, -1.230771478115229245, -0.7462941026102624109 ) ) ;
#40436=DIRECTION ( 'NONE',  ( 0.4999551463232373427, -0.8660512985181134660, 0.000000000000000000 ) ) ;
#40438=ADVANCED_FACE ( 'NONE', ( #16560 ), #15954, .T. ) ;
#40442=CARTESIAN_POINT ( 'NONE',  ( 0.3887841298280355073, -1.916107351281247873, -0.3024084733865095020 ) ) ;
#40455=CARTESIAN_POINT ( 'NONE',  ( 0.6002617396867515609, -1.576047946042514525, -0.4213240105477804587 ) ) ;
#40457=CARTESIAN_POINT ( 'NONE',  ( 0.1959265899308195724, -1.288818386415671036, -0.7414046965098800568 ) ) ;
#40467=CARTESIAN_POINT ( 'NONE',  ( 0.4108473310524629052, -1.676356312003210780, -0.6312918840655212804 ) ) ;
#40471=CARTESIAN_POINT ( 'NONE',  ( 0.5068534190187480304, -1.686660372286016729, -0.6047723693427432545 ) ) ;
#40485=DIRECTION ( 'NONE',  ( -0.4999551463232377313, 0.8660512985181132439, -0.000000000000000000 ) ) ;
#40490=AXIS2_PLACEMENT_3D ( 'NONE', #34304, #6111, #18678 ) ;
#40497=CARTESIAN_POINT ( 'NONE',  ( 0.5616069494768038961, -1.585551047948461578, -0.5092418914868334090 ) ) ;
#40503=CARTESIAN_POINT ( 'NONE',  ( 0.1865135932075447367, -1.586003729253250283, -0.6557087401434340546 ) ) ;
#40506=B_SPLINE_CURVE_WITH_KNOTS ( 'NONE', 3,
 ( #12300, #24858, #11874, #15166, #6099, #40260, #31009, #31424, #12093, #24659, #34092, #9191, #5895, #3227 ),
 .UNSPECIFIED., .F., .F.,
 ( 4, 2, 2, 2, 2, 2, 4 ),
 ( 4.300435128097903527E-16, 0.001060840485211818384, 0.001591260727817513879, 0.002121680970423209592, 0.002652101213028904871, 0.003182521455634601017, 0.004243361940845996778 ),
 .UNSPECIFIED. ) ;
#40517=ORIENTED_EDGE ( 'NONE', *, *, #20567, .T. ) ;
#40534=CARTESIAN_POINT ( 'NONE',  ( 0.1909286924077255032, -1.257064795538239022, -0.2869361388274795921 ) ) ;
#40537=CARTESIAN_POINT ( 'NONE',  ( 0.4469283285619457535, -1.099869350908817101, -0.4033480720695141741 ) ) ;
#40538=CARTESIAN_POINT ( 'NONE',  ( 0.4121862343158209652, -1.741309959742503244, -0.4470289626379757575 ) ) ;
#40549=DIRECTION ( 'NONE',  ( 0.000000000000000000, -0.2513338844154403007, 0.9679004486746795033 ) ) ;
#40557=FACE_OUTER_BOUND ( 'NONE', #12204, .T. ) ;
#40572=CARTESIAN_POINT ( 'NONE',  ( -2.112273405726188513E-14, -2.183180860297921466, -0.4937760292030871079 ) ) ;
#40578=AXIS2_PLACEMENT_3D ( 'NONE', #7415, #39116, #140 ) ;
#40592=CARTESIAN_POINT ( 'NONE',  ( 0.3853411735687863326, -1.756807109041631509, -0.4499573014711771846 ) ) ;
#40599=( BOUNDED_SURFACE ( )  B_SPLINE_SURFACE ( 3, 2, ( 
 ( #26485, #2206, #33257 ),
 ( #35736, #36551, #17219 ),
 ( #4855, #39022, #17427 ),
 ( #5067, #20730, #23429 ),
 ( #27092, #29982, #8362 ),
 ( #32839, #27311, #5259 ) ),
 .UNSPECIFIED., .F., .F., .T. ) 
 B_SPLINE_SURFACE_WITH_KNOTS ( ( 4, 2, 4 ),
 ( 3, 3 ),
 ( 3.385963384672230347E-16, 0.0006229787267328064718, 0.001245957453465274239 ),
 ( 0.000000000000000000, 1.000000000000000000 ),
 .UNSPECIFIED. ) 
 GEOMETRIC_REPRESENTATION_ITEM ( )  RATIONAL_B_SPLINE_SURFACE ( (
 ( 1.000000000000000000, 0.9231872052445554422, 1.000000000000000000),
 ( 1.000000000000000000, 0.9271591560550311861, 1.000000000000000000),
 ( 1.000000000000000000, 0.9286221054271613928, 1.000000000000000000),
 ( 1.000000000000000000, 0.9259746644423475503, 1.000000000000000000),
 ( 1.000000000000000000, 0.9219504995353200449, 1.000000000000000000),
 ( 1.000000000000000000, 0.9159177456829653563, 1.000000000000000000) ) ) 
 REPRESENTATION_ITEM ( '' )  SURFACE ( )  );
#40600=CARTESIAN_POINT ( 'NONE',  ( 0.3578407435306584228, -1.776530764634635551, -0.5202682414489888663 ) ) ;
#40605=EDGE_CURVE ( 'NONE', #10331, #4952, #19279, .T. ) ;
#40617=CARTESIAN_POINT ( 'NONE',  ( 0.1844765520120722202, -1.888974760190525570, -0.3406829697689818248 ) ) ;
#40633=CARTESIAN_POINT ( 'NONE',  ( 0.1885375905025258314, -1.930959840804365335, -0.3029267234423492772 ) ) ;
#40637=EDGE_CURVE ( 'NONE', #40066, #13700, #18627, .T. ) ;
#40640=EDGE_CURVE ( 'NONE', #33728, #32971, #23374, .T. ) ;
#40667=COLOUR_RGB('Dark Blue',0.08,0.2,0.34);
#40668=FILL_AREA_STYLE_COLOUR('',#40667);
#40669=FILL_AREA_STYLE('',(#40668));
#40670=SURFACE_STYLE_FILL_AREA(#40669);
#40671=SURFACE_SIDE_STYLE('',(#40670));
#40672=SURFACE_STYLE_USAGE(.BOTH.,#40671);
#40673=PRESENTATION_STYLE_ASSIGNMENT((#40672));
#40709=STYLED_ITEM('',(#40673),#4903);
#40721=MECHANICAL_DESIGN_GEOMETRIC_PRESENTATION_REPRESENTATION('',(#40709),#11399);
ENDSEC;
END-ISO-10303-21;
